ISO-10303-21;
HEADER;
FILE_DESCRIPTION (('STEP AP203'),
    '1' );
FILE_NAME ('Part4_Gear.step',
    '2026-10-06T15:07:10',
    ( '' ),
    ( '' ),
    'SwSTEP 2.0',
    'SolidWorks 2024',
    '' );
FILE_SCHEMA (( 'AUTOMOTIVE_DESIGN' ));
ENDSEC;

DATA;
#3=CARTESIAN_POINT ( 'NONE',  ( -8.000050800000000351, 3.673940397442060361E-16, 3.000000000000000444 ) ) ;
#18=ORIENTED_EDGE ( 'NONE', *, *, #3562, .F. ) ;
#19=ORIENTED_EDGE ( 'NONE', *, *, #12026, .T. ) ;
#20=CARTESIAN_POINT ( 'NONE',  ( -2.511343449419941365, -0.3178988483021044087, 3.024605502323848949 ) ) ;
#24=FACE_OUTER_BOUND ( 'NONE', #30613, .T. ) ;
#33=ORIENTED_EDGE ( 'NONE', *, *, #17651, .T. ) ;
#35=AXIS2_PLACEMENT_3D ( 'NONE', #30229, #18289, #20649 ) ;
#41=EDGE_CURVE ( 'NONE', #3413, #15831, #25636, .T. ) ;
#43=CARTESIAN_POINT ( 'NONE',  ( -8.000050800000000351, 0.000000000000000000, 0.000000000000000000 ) ) ;
#47=DIRECTION ( 'NONE',  ( 0.000000000000000000, -0.4226182617406998299, -0.9063077870366498257 ) ) ;
#49=CARTESIAN_POINT ( 'NONE',  ( -6.387550801365593500, 3.521866450007987037, 0.3701630799359328372 ) ) ;
#53=DIRECTION ( 'NONE',  ( 0.000000000000000000, -0.7071067811865380248, -0.7071067811865570096 ) ) ;
#58=CIRCLE ( 'NONE', #27352, 8.500000000000000000 ) ;
#66=DIRECTION ( 'NONE',  ( 0.000000000000000000, -0.7071067811865455743, -0.7071067811865495711 ) ) ;
#69=CARTESIAN_POINT ( 'NONE',  ( 5.612718761614564400, -7.013540705848206436, 4.279483796479000013 ) ) ;
#71=DIRECTION ( 'NONE',  ( 0.000000000000000000, 0.9961946980917452121, 0.08715574274766296758 ) ) ;
#76=DIRECTION ( 'NONE',  ( -1.000000000000000000, -0.000000000000000000, -0.000000000000000000 ) ) ;
#81=ADVANCED_FACE ( 'NONE', ( #26310 ), #21929, .F. ) ;
#83=AXIS2_PLACEMENT_3D ( 'NONE', #30124, #5184, #17706 ) ;
#85=PLANE ( 'NONE',  #10726 ) ;
#91=CIRCLE ( 'NONE', #29457, 2.999999999999999112 ) ;
#92=CARTESIAN_POINT ( 'NONE',  ( 7.249760686538667009, -2.789499415801756586E-14, 8.014274990069656823 ) ) ;
#95=CARTESIAN_POINT ( 'NONE',  ( -5.787550801365593856, 0.3701630799359330593, -3.521866450007987037 ) ) ;
#98=FACE_OUTER_BOUND ( 'NONE', #358, .T. ) ;
#102=CARTESIAN_POINT ( 'NONE',  ( 5.377543748152548986, -5.151476664237435443, -6.139290821770307716 ) ) ;
#109=ORIENTED_EDGE ( 'NONE', *, *, #15136, .T. ) ;
#112=VERTEX_POINT ( 'NONE', #19260 ) ;
#116=CIRCLE ( 'NONE', #24119, 8.500000000000000000 ) ;
#133=CARTESIAN_POINT ( 'NONE',  ( -6.962942409646511344, 7.727249047114547632E-16, -2.999999999999999556 ) ) ;
#135=PLANE ( 'NONE',  #7597 ) ;
#136=VERTEX_POINT ( 'NONE', #4209 ) ;
#137=VECTOR ( 'NONE', #28016, 1000.000000000000000 ) ;
#139=CARTESIAN_POINT ( 'NONE',  ( -5.712550801365594566, -1.088641768524163389, -3.675193018007246071 ) ) ;
#142=CARTESIAN_POINT ( 'NONE',  ( -4.654531657079157725, -2.846291840500172921, -1.545410377633947618 ) ) ;
#151=AXIS2_PLACEMENT_3D ( 'NONE', #26577, #18412, #21086 ) ;
#156=AXIS2_PLACEMENT_3D ( 'NONE', #22378, #9498, #26916 ) ;
#157=CARTESIAN_POINT ( 'NONE',  ( 3.499999999999999556, 0.000000000000000000, 0.000000000000000000 ) ) ;
#174=CARTESIAN_POINT ( 'NONE',  ( -5.212550801365593678, -1.828967928396026510, 3.368539882008728004 ) ) ;
#177=CARTESIAN_POINT ( 'NONE',  ( 5.377543748152548986, -6.139290821770289064, 5.151476664237455871 ) ) ;
#183=EDGE_CURVE ( 'NONE', #26433, #28176, #18018, .T. ) ;
#195=CARTESIAN_POINT ( 'NONE',  ( 3.499999999999999556, 0.000000000000000000, 0.000000000000000000 ) ) ;
#199=AXIS2_PLACEMENT_3D ( 'NONE', #1341, #6668, #6487 ) ;
#206=EDGE_LOOP ( 'NONE', ( #7867, #23805, #1516, #15326 ) ) ;
#211=ORIENTED_EDGE ( 'NONE', *, *, #28572, .F. ) ;
#225=AXIS2_PLACEMENT_3D ( 'NONE', #7662, #15180, #20362 ) ;
#235=EDGE_CURVE ( 'NONE', #10254, #1604, #2904, .T. ) ;
#237=CARTESIAN_POINT ( 'NONE',  ( 6.356381451270080696, 8.587653982362812854, -0.5733789922931548100 ) ) ;
#240=PLANE ( 'NONE',  #32748 ) ;
#241=DIRECTION ( 'NONE',  ( 0.4999999999999970579, -0.09052430460833674197, 0.8612812260087757688 ) ) ;
#242=CARTESIAN_POINT ( 'NONE',  ( -2.537550801365593411, 1.828967928396027398, -3.368539882008727115 ) ) ;
#260=ORIENTED_EDGE ( 'NONE', *, *, #26605, .T. ) ;
#261=CARTESIAN_POINT ( 'NONE',  ( -8.000050800000000351, 3.673940397442060361E-16, 3.000000000000000444 ) ) ;
#265=CARTESIAN_POINT ( 'NONE',  ( -5.500050800000000351, -2.983565686104819648, -0.3135853898029605791 ) ) ;
#268=CARTESIAN_POINT ( 'NONE',  ( 7.249760686538667009, 8.385837730238846314E-14, -8.014274990069656823 ) ) ;
#277=CARTESIAN_POINT ( 'NONE',  ( 5.885541736258995904, -3.216848386728015097, -7.752826540560539215 ) ) ;
#279=FACE_OUTER_BOUND ( 'NONE', #24858, .T. ) ;
#280=VERTEX_POINT ( 'NONE', #698 ) ;
#281=CARTESIAN_POINT ( 'NONE',  ( -7.237550801365592257, 3.675193018007247403, -1.088641768524161391 ) ) ;
#292=VERTEX_POINT ( 'NONE', #23411 ) ;
#297=CARTESIAN_POINT ( 'NONE',  ( 7.249760686538667009, 0.000000000000000000, 0.000000000000000000 ) ) ;
#299=VERTEX_POINT ( 'NONE', #30459 ) ;
#304=DIRECTION ( 'NONE',  ( 0.000000000000000000, 0.4226182617407134856, -0.9063077870366433864 ) ) ;
#306=CARTESIAN_POINT ( 'NONE',  ( 5.377543748152548986, -6.139290821770289064, 5.151476664237455871 ) ) ;
#308=CARTESIAN_POINT ( 'NONE',  ( 7.249760686538667009, -8.466096581343467875, -2.210816291636301223 ) ) ;
#309=DIRECTION ( 'NONE',  ( -1.000000000000000000, -0.000000000000000000, -0.000000000000000000 ) ) ;
#313=CARTESIAN_POINT ( 'NONE',  ( 6.037141879243260512, -6.770886333893388453, -5.096219216992919243 ) ) ;
#314=ORIENTED_EDGE ( 'NONE', *, *, #986, .T. ) ;
#315=CARTESIAN_POINT ( 'NONE',  ( -6.812550801365595099, -1.828967928396026510, 3.368539882008728004 ) ) ;
#317=CARTESIAN_POINT ( 'NONE',  ( -3.504531657079157370, 2.975847129947406522, 0.3127741368606808403 ) ) ;
#321=ORIENTED_EDGE ( 'NONE', *, *, #29783, .T. ) ;
#323=ORIENTED_EDGE ( 'NONE', *, *, #3103, .F. ) ;
#330=CARTESIAN_POINT ( 'NONE',  ( 7.249760686538667009, 0.000000000000000000, 0.000000000000000000 ) ) ;
#332=ORIENTED_EDGE ( 'NONE', *, *, #10400, .T. ) ;
#333=CARTESIAN_POINT ( 'NONE',  ( -8.000050800000002127, -3.003076289684047495, 0.02717128497728628356 ) ) ;
#334=CARTESIAN_POINT ( 'NONE',  ( 7.249760686538667009, 8.721381771256204729, -0.7071067811865423547 ) ) ;
#339=CARTESIAN_POINT ( 'NONE',  ( -7.712550801365593678, 1.088641768524161613, 3.675193018007247403 ) ) ;
#345=CARTESIAN_POINT ( 'NONE',  ( 4.749760686538667009, -7.530955069117533540, 2.741043480754901118 ) ) ;
#358=EDGE_LOOP ( 'NONE', ( #22416, #3974, #15722, #2891 ) ) ;
#362=ADVANCED_FACE ( 'NONE', ( #28114 ), #31976, .F. ) ;
#364=CYLINDRICAL_SURFACE ( 'NONE', #25143, 3.000000000000000444 ) ;
#365=CARTESIAN_POINT ( 'NONE',  ( -6.512550801365594388, -1.088641768524163611, -3.675193018007245627 ) ) ;
#379=CARTESIAN_POINT ( 'NONE',  ( 3.499999999999999556, 5.471841788314750765, -3.018103451449674068 ) ) ;
#382=CARTESIAN_POINT ( 'NONE',  ( -8.000050800000000351, 0.2618957199879418662, -2.989246278116708400 ) ) ;
#385=EDGE_LOOP ( 'NONE', ( #24811, #18638, #9529, #556 ) ) ;
#403=ORIENTED_EDGE ( 'NONE', *, *, #25920, .T. ) ;
#407=ORIENTED_EDGE ( 'NONE', *, *, #15411, .F. ) ;
#408=ORIENTED_EDGE ( 'NONE', *, *, #11645, .F. ) ;
#409=CARTESIAN_POINT ( 'NONE',  ( 7.249760686538667009, -6.940565734314570356, -4.007137495034885255 ) ) ;
#419=CARTESIAN_POINT ( 'NONE',  ( 6.037141879243264064, 5.096219216992939671, -6.770886333893373354 ) ) ;
#421=CARTESIAN_POINT ( 'NONE',  ( 5.377543748152549874, -5.151476664237518044, 6.139290821770238438 ) ) ;
#422=CARTESIAN_POINT ( 'NONE',  ( 7.249760686538667009, -8.711672189281420842, -0.8180878109962766986 ) ) ;
#423=EDGE_CURVE ( 'NONE', #9882, #10953, #9131, .T. ) ;
#427=EDGE_CURVE ( 'NONE', #20419, #3413, #32361, .T. ) ;
#440=CARTESIAN_POINT ( 'NONE',  ( 5.612973690782940395, 0.1996300861632082368, -8.213905076232775215 ) ) ;
#441=CARTESIAN_POINT ( 'NONE',  ( -2.410187303267195436, 0.5774022981078724692, 3.166406138753334876 ) ) ;
#442=VERTEX_POINT ( 'NONE', #22198 ) ;
#447=EDGE_CURVE ( 'NONE', #26968, #22574, #32221, .T. ) ;
#453=CARTESIAN_POINT ( 'NONE',  ( 3.499999999999999556, 0.000000000000000000, 0.000000000000000000 ) ) ;
#454=CARTESIAN_POINT ( 'NONE',  ( -8.000050800000003903, -2.272722698207227054, 1.977113453969371992 ) ) ;
#455=CARTESIAN_POINT ( 'NONE',  ( -7.100050802731186828, -2.853674364686378695, -1.549418761218566809 ) ) ;
#459=CARTESIAN_POINT ( 'NONE',  ( -4.612550801365593145, 3.368539882008727115, 1.828967928396026954 ) ) ;
#462=CARTESIAN_POINT ( 'NONE',  ( -4.254531657079158258, 2.846291840500173365, 1.545410377633946952 ) ) ;
#481=VERTEX_POINT ( 'NONE', #4141 ) ;
#482=CARTESIAN_POINT ( 'NONE',  ( -5.662550801365592967, 0.3701630799359330593, -3.521866450007987037 ) ) ;
#483=FACE_OUTER_BOUND ( 'NONE', #1513, .T. ) ;
#489=EDGE_CURVE ( 'NONE', #14880, #20515, #18846, .T. ) ;
#501=DIRECTION ( 'NONE',  ( 0.000000000000000000, 0.9659258262890683122, -0.2588190451025207950 ) ) ;
#506=CARTESIAN_POINT ( 'NONE',  ( -5.050050802731187005, 1.887961173149511618, 2.331437884370912705 ) ) ;
#508=VERTEX_POINT ( 'NONE', #20245 ) ;
#511=CARTESIAN_POINT ( 'NONE',  ( -7.462550801365593678, -3.521866450007987037, -0.3701630799359323931 ) ) ;
#516=VERTEX_POINT ( 'NONE', #28101 ) ;
#531=PLANE ( 'NONE',  #9140 ) ;
#533=VERTEX_POINT ( 'NONE', #7525 ) ;
#538=LINE ( 'NONE', #32993, #30655 ) ;
#549=ORIENTED_EDGE ( 'NONE', *, *, #24860, .T. ) ;
#555=ORIENTED_EDGE ( 'NONE', *, *, #27981, .T. ) ;
#556=ORIENTED_EDGE ( 'NONE', *, *, #21436, .T. ) ;
#564=CARTESIAN_POINT ( 'NONE',  ( -6.512942406915326110, 3.284080845023683730E-15, 3.000000000000000000 ) ) ;
#565=DIRECTION ( 'NONE',  ( -1.000000000000000000, -0.000000000000000000, 0.000000000000000000 ) ) ;
#569=B_SPLINE_CURVE_WITH_KNOTS ( 'NONE', 3,
 ( #22916, #20430, #30648, #17918, #6761, #28109, #15384, #16952, #27148, #25941 ),
 .UNSPECIFIED., .F., .F.,
 ( 4, 2, 2, 2, 4 ),
 ( 1.968338519001761812E-07, 0.0005467927057105467954, 0.001093388577569193469, 0.001639984449427840142, 0.002186580321286488333 ),
 .UNSPECIFIED. ) ;
#571=CARTESIAN_POINT ( 'NONE',  ( 6.880159329304571081, 5.066480354149027754, -7.110803091624010364 ) ) ;
#572=VERTEX_POINT ( 'NONE', #7365 ) ;
#583=CARTESIAN_POINT ( 'NONE',  ( -2.300050802731187449, -2.853674364686378695, -1.549418761218566809 ) ) ;
#590=CARTESIAN_POINT ( 'NONE',  ( -2.476225935960405966, -0.3178988483021057410, 3.024605502323848949 ) ) ;
#597=CARTESIAN_POINT ( 'NONE',  ( -7.712942406915323623, 7.727249047114547632E-16, -2.999999999999999556 ) ) ;
#599=ORIENTED_EDGE ( 'NONE', *, *, #16813, .F. ) ;
#605=CARTESIAN_POINT ( 'NONE',  ( 7.249760686538667009, 5.064320921489914973, -7.135485519861949122 ) ) ;
#608=VECTOR ( 'NONE', #21725, 1000.000000000000000 ) ;
#611=CARTESIAN_POINT ( 'NONE',  ( -6.607304909706597229, 1.062355717592093463, 3.000000000000000000 ) ) ;
#615=CARTESIAN_POINT ( 'NONE',  ( -8.000050799999998574, 0.5580980903926698877, 3.189890360694769278 ) ) ;
#619=CARTESIAN_POINT ( 'NONE',  ( -4.762550801365593500, 2.752080473201636845, -2.228590825266444142 ) ) ;
#620=ORIENTED_EDGE ( 'NONE', *, *, #22042, .F. ) ;
#621=CARTESIAN_POINT ( 'NONE',  ( -3.554531657079157192, 3.105402419394639235, -0.9198621039125850496 ) ) ;
#625=LINE ( 'NONE', #28375, #22614 ) ;
#633=AXIS2_PLACEMENT_3D ( 'NONE', #749, #3096, #10588 ) ;
#642=CARTESIAN_POINT ( 'NONE',  ( 5.887529755120531227, -8.194579018285280014, -1.823049025159271030 ) ) ;
#647=EDGE_CURVE ( 'NONE', #29104, #11269, #16022, .T. ) ;
#652=CARTESIAN_POINT ( 'NONE',  ( -3.312550801365593767, -1.088641768524163389, -3.675193018007246071 ) ) ;
#664=CIRCLE ( 'NONE', #2262, 8.750000000000000000 ) ;
#666=CIRCLE ( 'NONE', #7043, 6.248999999999999666 ) ;
#674=CARTESIAN_POINT ( 'NONE',  ( 5.612718622971679672, -2.621884781721320223, 7.786491723834104484 ) ) ;
#675=AXIS2_PLACEMENT_3D ( 'NONE', #17353, #9979, #19861 ) ;
#678=CIRCLE ( 'NONE', #32185, 8.500000000000000000 ) ;
#683=AXIS2_PLACEMENT_3D ( 'NONE', #25151, #12274, #10094 ) ;
#691=CARTESIAN_POINT ( 'NONE',  ( -3.262550801365593056, 0.3701630799359330593, -3.521866450007987037 ) ) ;
#698=CARTESIAN_POINT ( 'NONE',  ( 0.000000000000000000, 0.6700234925293840904, -8.473551116235670477 ) ) ;
#700=ADVANCED_FACE ( 'NONE', ( #21232 ), #3532, .T. ) ;
#702=CARTESIAN_POINT ( 'NONE',  ( 0.000000000000000000, 0.000000000000000000, 0.000000000000000000 ) ) ;
#711=AXIS2_PLACEMENT_3D ( 'NONE', #8425, #28665, #3261 ) ;
#715=DIRECTION ( 'NONE',  ( 0.000000000000000000, 0.000000000000000000, 1.000000000000000000 ) ) ;
#719=VECTOR ( 'NONE', #6939, 1000.000000000000000 ) ;
#729=AXIS2_PLACEMENT_3D ( 'NONE', #23943, #14238, #31981 ) ;
#737=ORIENTED_EDGE ( 'NONE', *, *, #21414, .T. ) ;
#749=CARTESIAN_POINT ( 'NONE',  ( 3.499999999999999556, 0.000000000000000000, 0.000000000000000000 ) ) ;
#754=CARTESIAN_POINT ( 'NONE',  ( 3.499999999999999556, 0.000000000000000000, 0.000000000000000000 ) ) ;
#757=CARTESIAN_POINT ( 'NONE',  ( 5.612718622971678784, 7.786491723834110701, 2.621884781721292246 ) ) ;
#763=CIRCLE ( 'NONE', #8227, 2.999999999999999556 ) ;
#766=ORIENTED_EDGE ( 'NONE', *, *, #18502, .F. ) ;
#783=ORIENTED_EDGE ( 'NONE', *, *, #1125, .F. ) ;
#784=CARTESIAN_POINT ( 'NONE',  ( -7.706376978575948833, 0.1572233378491243172, -2.999999999999999556 ) ) ;
#789=CARTESIAN_POINT ( 'NONE',  ( 6.524595126109736576, 0.8869162863045649825, -8.613374939462815405 ) ) ;
#793=CARTESIAN_POINT ( 'NONE',  ( -10.00000000000000000, 0.000000000000000000, 0.000000000000000000 ) ) ;
#794=B_SPLINE_CURVE_WITH_KNOTS ( 'NONE', 3,
 ( #24093, #31175, #8737, #21611, #11413, #29134 ),
 .UNSPECIFIED., .F., .F.,
 ( 4, 2, 4 ),
 ( 2.337797342572514391E-16, 0.001737887880030562987, 0.003475775760060892221 ),
 .UNSPECIFIED. ) ;
#800=CARTESIAN_POINT ( 'NONE',  ( 3.499999999999999556, 6.226349476952025341, 0.5315761383463585288 ) ) ;
#804=DIRECTION ( 'NONE',  ( -1.000000000000000000, -0.000000000000000000, -0.000000000000000000 ) ) ;
#807=CARTESIAN_POINT ( 'NONE',  ( -2.312550801365593767, 3.675193018007247403, -1.088641768524161391 ) ) ;
#809=CARTESIAN_POINT ( 'NONE',  ( -6.300050800000000173, -2.983565686104819648, -0.3135853898029605791 ) ) ;
#817=ORIENTED_EDGE ( 'NONE', *, *, #14859, .T. ) ;
#820=ADVANCED_FACE ( 'NONE', ( #14690 ), #3843, .T. ) ;
#823=CARTESIAN_POINT ( 'NONE',  ( 5.377543748152551650, -7.892520144992426268, -1.391664247347309535 ) ) ;
#826=EDGE_CURVE ( 'NONE', #25076, #23417, #2306, .T. ) ;
#830=CARTESIAN_POINT ( 'NONE',  ( 3.499999999999999556, -7.009698679648281860, -0.7308381473897611613 ) ) ;
#832=CARTESIAN_POINT ( 'NONE',  ( -2.162550801365593856, 2.228590825266444142, 2.752080473201636845 ) ) ;
#835=ORIENTED_EDGE ( 'NONE', *, *, #5183, .F. ) ;
#837=EDGE_CURVE ( 'NONE', #5413, #9418, #4165, .T. ) ;
#838=DIRECTION ( 'NONE',  ( -0.000000000000000000, -0.08715574274766219043, 0.9961946980917452121 ) ) ;
#846=CARTESIAN_POINT ( 'NONE',  ( -3.287550801365593856, 2.752080473201636845, -2.228590825266444142 ) ) ;
#850=CARTESIAN_POINT ( 'NONE',  ( 5.489343958331428297, -2.678936089601496207, 7.664144799260943053 ) ) ;
#852=ORIENTED_EDGE ( 'NONE', *, *, #8382, .T. ) ;
#862=CARTESIAN_POINT ( 'NONE',  ( -4.362550801365593145, -2.752080473201636845, 2.228590825266444586 ) ) ;
#863=CARTESIAN_POINT ( 'NONE',  ( 7.249760686538667009, -7.953573330858190182, -3.647351267791651974 ) ) ;
#867=CARTESIAN_POINT ( 'NONE',  ( -5.137550801365594388, -3.368539882008727115, -1.828967928396028064 ) ) ;
#881=LINE ( 'NONE', #23597, #20986 ) ;
#882=CARTESIAN_POINT ( 'NONE',  ( -5.887550801365593500, -2.228590825266444586, -2.752080473201636401 ) ) ;
#901=VERTEX_POINT ( 'NONE', #15003 ) ;
#904=CARTESIAN_POINT ( 'NONE',  ( 0.000000000000000000, 6.226349476952025341, 0.5315761383463585288 ) ) ;
#905=DIRECTION ( 'NONE',  ( 0.000000000000000000, 0.000000000000000000, 1.000000000000000000 ) ) ;
#912=CARTESIAN_POINT ( 'NONE',  ( -3.000050799999999906, -1.887961173149512062, -2.331437884370912261 ) ) ;
#915=CARTESIAN_POINT ( 'NONE',  ( 6.524595395369781059, -3.538595500939536009, -7.902859683906648058 ) ) ;
#916=DIRECTION ( 'NONE',  ( 0.000000000000000000, -1.224646799147352961E-16, 1.000000000000000000 ) ) ;
#924=ORIENTED_EDGE ( 'NONE', *, *, #10559, .F. ) ;
#925=CARTESIAN_POINT ( 'NONE',  ( 5.489321708267614675, 6.285661071314543769, -5.138670926724834942 ) ) ;
#928=CARTESIAN_POINT ( 'NONE',  ( 5.887530024394195038, 3.218326717262362191, -7.753515897409855029 ) ) ;
#946=DIRECTION ( 'NONE',  ( -1.000000000000000000, -0.000000000000000000, 0.000000000000000000 ) ) ;
#947=EDGE_CURVE ( 'NONE', #7301, #24368, #1667, .T. ) ;
#953=CARTESIAN_POINT ( 'NONE',  ( -2.612550801365594477, -3.368539882008727115, -1.828967928396028064 ) ) ;
#955=CARTESIAN_POINT ( 'NONE',  ( -6.550050800000000173, 0.9222479816126443186, 3.113457007523260156 ) ) ;
#960=CARTESIAN_POINT ( 'NONE',  ( 3.499999999999999556, 6.745408891279611296, -5.171987904998036178 ) ) ;
#965=CARTESIAN_POINT ( 'NONE',  ( 6.038144853276844692, -8.256557579931650181, -1.911563584435280072 ) ) ;
#969=EDGE_CURVE ( 'NONE', #6731, #481, #20377, .T. ) ;
#977=CARTESIAN_POINT ( 'NONE',  ( 0.000000000000000000, 0.000000000000000000, 0.000000000000000000 ) ) ;
#983=LINE ( 'NONE', #25918, #18347 ) ;
#986=EDGE_CURVE ( 'NONE', #29104, #19214, #32052, .T. ) ;
#988=CARTESIAN_POINT ( 'NONE',  ( -8.504531657079157370, 0.3127741368606810068, -2.975847129947406522 ) ) ;
#990=CARTESIAN_POINT ( 'NONE',  ( -4.687550801365594211, 2.228590825266444142, 2.752080473201636845 ) ) ;
#996=ORIENTED_EDGE ( 'NONE', *, *, #11125, .F. ) ;
#1002=CYLINDRICAL_SURFACE ( 'NONE', #151, 3.000000000000000444 ) ;
#1003=ORIENTED_EDGE ( 'NONE', *, *, #5273, .T. ) ;
#1006=CARTESIAN_POINT ( 'NONE',  ( -3.162550801365593856, 2.752080473201636845, -2.228590825266444142 ) ) ;
#1011=CARTESIAN_POINT ( 'NONE',  ( -6.837550801365593678, -3.675193018007246071, 1.088641768524163167 ) ) ;
#1013=CARTESIAN_POINT ( 'NONE',  ( 0.000000000000000000, 5.904264776415100613, 2.046865518294726627 ) ) ;
#1015=EDGE_CURVE ( 'NONE', #23179, #12214, #24823, .T. ) ;
#1018=EDGE_CURVE ( 'NONE', #19569, #19561, #13314, .T. ) ;
#1022=EDGE_CURVE ( 'NONE', #31391, #30146, #21347, .T. ) ;
#1027=DIRECTION ( 'NONE',  ( 0.000000000000000000, 0.2079116908177532919, 0.9781476007338069101 ) ) ;
#1028=CARTESIAN_POINT ( 'NONE',  ( -5.187550801365593323, -3.521866450007987037, -0.3701630799359323931 ) ) ;
#1030=CARTESIAN_POINT ( 'NONE',  ( 7.064423600674403225, 8.466096581344354277, -2.210816291637329734 ) ) ;
#1032=CARTESIAN_POINT ( 'NONE',  ( 7.249760686538667009, 0.000000000000000000, 0.000000000000000000 ) ) ;
#1033=ORIENTED_EDGE ( 'NONE', *, *, #16433, .F. ) ;
#1035=AXIS2_PLACEMENT_3D ( 'NONE', #12260, #29838, #22470 ) ;
#1036=PRODUCT_DEFINITION ( 'UNKNOWN', '', #17797, #7461 ) ;
#1044=DIRECTION ( 'NONE',  ( 1.000000000000000000, 0.000000000000000000, 0.000000000000000000 ) ) ;
#1052=CARTESIAN_POINT ( 'NONE',  ( -4.850050802731186828, -2.331437884370912705, 1.887961173149512062 ) ) ;
#1056=DIRECTION ( 'NONE',  ( -1.000000000000000000, -0.000000000000000000, -0.000000000000000000 ) ) ;
#1060=CARTESIAN_POINT ( 'NONE',  ( 5.612718825656738630, 5.126902779943868893, -6.420171604529136822 ) ) ;
#1063=DIRECTION ( 'NONE',  ( 0.000000000000000000, 0.000000000000000000, 1.000000000000000000 ) ) ;
#1065=ORIENTED_EDGE ( 'NONE', *, *, #22651, .T. ) ;
#1068=ORIENTED_EDGE ( 'NONE', *, *, #31884, .F. ) ;
#1078=DIRECTION ( 'NONE',  ( 0.000000000000000000, 0.9961946980917452121, 0.08715574274766220431 ) ) ;
#1082=VERTEX_POINT ( 'NONE', #29061 ) ;
#1087=DIRECTION ( 'NONE',  ( 0.000000000000000000, 0.9961946980917455452, -0.08715574274765797158 ) ) ;
#1093=CARTESIAN_POINT ( 'NONE',  ( 4.749760686538667009, 7.892520144992453801, -1.391664247347147443 ) ) ;
#1098=DIRECTION ( 'NONE',  ( 0.000000000000000000, 0.000000000000000000, 1.000000000000000000 ) ) ;
#1100=AXIS2_PLACEMENT_3D ( 'NONE', #29549, #24495, #31890 ) ;
#1102=CARTESIAN_POINT ( 'NONE',  ( 4.749760686538667009, -1.391664247347281780, 7.892520144992429820 ) ) ;
#1109=CARTESIAN_POINT ( 'NONE',  ( -2.562550801365592879, -2.228590825266444586, -2.752080473201636401 ) ) ;
#1110=ORIENTED_EDGE ( 'NONE', *, *, #1444, .T. ) ;
#1111=CARTESIAN_POINT ( 'NONE',  ( -6.000050800000000351, 2.331437884370912705, -1.887961173149511618 ) ) ;
#1116=ORIENTED_EDGE ( 'NONE', *, *, #29397, .F. ) ;
#1124=AXIS2_PLACEMENT_3D ( 'NONE', #32785, #9864, #25050 ) ;
#1125=EDGE_CURVE ( 'NONE', #15674, #3548, #10832, .T. ) ;
#1131=ADVANCED_FACE ( 'NONE', ( #26684 ), #13968, .T. ) ;
#1132=EDGE_CURVE ( 'NONE', #7771, #5615, #12546, .T. ) ;
#1135=LINE ( 'NONE', #32247, #28459 ) ;
#1137=CIRCLE ( 'NONE', #22467, 6.249000000000000554 ) ;
#1138=DIRECTION ( 'NONE',  ( -1.000000000000000000, 0.000000000000000000, 0.000000000000000000 ) ) ;
#1143=DIRECTION ( 'NONE',  ( 1.000000000000000000, 0.000000000000000000, 0.000000000000000000 ) ) ;
#1153=CARTESIAN_POINT ( 'NONE',  ( 5.612718622971679672, 2.621884781721373070, -7.786491723834085832 ) ) ;
#1156=CARTESIAN_POINT ( 'NONE',  ( -3.387550801365593056, 0.3701630799359330593, -3.521866450007987037 ) ) ;
#1161=AXIS2_PLACEMENT_3D ( 'NONE', #25032, #16900, #27564 ) ;
#1167=DIRECTION ( 'NONE',  ( 0.000000000000000000, 0.000000000000000000, 1.000000000000000000 ) ) ;
#1168=ORIENTED_EDGE ( 'NONE', *, *, #30070, .F. ) ;
#1174=CARTESIAN_POINT ( 'NONE',  ( -4.062550801365593323, 0.3701630799359330593, -3.521866450007987037 ) ) ;
#1177=LINE ( 'NONE', #26260, #11840 ) ;
#1180=CARTESIAN_POINT ( 'NONE',  ( -5.387550801365593500, -0.3701630799359326152, 3.521866450007987037 ) ) ;
#1183=EDGE_CURVE ( 'NONE', #26824, #12879, #7478, .T. ) ;
#1187=ORIENTED_EDGE ( 'NONE', *, *, #25876, .F. ) ;
#1192=CARTESIAN_POINT ( 'NONE',  ( 5.489321486716459475, -1.307389195612923327, -8.012877392144808653 ) ) ;
#1200=DIRECTION ( 'NONE',  ( 0.000000000000000000, 0.000000000000000000, -1.000000000000000000 ) ) ;
#1201=LINE ( 'NONE', #11398, #24197 ) ;
#1204=AXIS2_PLACEMENT_3D ( 'NONE', #2043, #27104, #27457 ) ;
#1208=CARTESIAN_POINT ( 'NONE',  ( 7.249760686538667009, -8.721381771256204729, 0.7071067811865423547 ) ) ;
#1211=LINE ( 'NONE', #11221, #18226 ) ;
#1214=DIRECTION ( 'NONE',  ( 0.000000000000000000, 0.2588190451025258465, -0.9659258262890669799 ) ) ;
#1222=EDGE_CURVE ( 'NONE', #24417, #4009, #22338, .T. ) ;
#1223=DIRECTION ( 'NONE',  ( 0.000000000000000000, 0.9063077870366480493, 0.4226182617407034936 ) ) ;
#1229=VECTOR ( 'NONE', #241, 1000.000000000000227 ) ;
#1241=AXIS2_PLACEMENT_3D ( 'NONE', #14417, #22656, #19987 ) ;
#1242=EDGE_CURVE ( 'NONE', #5714, #20158, #30051, .T. ) ;
#1245=VERTEX_POINT ( 'NONE', #22508 ) ;
#1256=EDGE_LOOP ( 'NONE', ( #24092, #9756, #31064, #7718 ) ) ;
#1259=ORIENTED_EDGE ( 'NONE', *, *, #3631, .T. ) ;
#1274=CARTESIAN_POINT ( 'NONE',  ( 3.499999999999999556, -1.179494851233943598, 6.136676046192483192 ) ) ;
#1276=ORIENTED_EDGE ( 'NONE', *, *, #32465, .F. ) ;
#1279=CARTESIAN_POINT ( 'NONE',  ( 4.749760686538667009, -6.139290821770219786, -5.151476664237539360 ) ) ;
#1280=DIRECTION ( 'NONE',  ( 0.000000000000000000, -0.5735764363510533759, 0.8191520442889866915 ) ) ;
#1282=VECTOR ( 'NONE', #23000, 1000.000000000000114 ) ;
#1291=LINE ( 'NONE', #17427, #17757 ) ;
#1292=LINE ( 'NONE', #14279, #2260 ) ;
#1295=CARTESIAN_POINT ( 'NONE',  ( -6.800050802731187893, 3.113457007523260156, -0.9222479816126439855 ) ) ;
#1297=CARTESIAN_POINT ( 'NONE',  ( -7.250050800000000351, -1.549418761218565477, 2.853674364686380471 ) ) ;
#1321=LINE ( 'NONE', #8648, #27925 ) ;
#1322=DIRECTION ( 'NONE',  ( -0.000000000000000000, 0.9659258262890693114, -0.2588190451025172978 ) ) ;
#1324=CARTESIAN_POINT ( 'NONE',  ( -3.662550801365593411, -0.3701630799359326152, 3.521866450007987037 ) ) ;
#1328=DIRECTION ( 'NONE',  ( 0.000000000000000000, -0.2588190451025167982, -0.9659258262890694224 ) ) ;
#1335=CARTESIAN_POINT ( 'NONE',  ( -2.650050802731187094, 1.887961173149511618, 2.331437884370912705 ) ) ;
#1338=CARTESIAN_POINT ( 'NONE',  ( -1.963030064606874792, 0.7837004005683814167, 3.199079356508811145 ) ) ;
#1339=CARTESIAN_POINT ( 'NONE',  ( -2.287550801365593856, 2.228590825266444142, 2.752080473201636845 ) ) ;
#1340=DIRECTION ( 'NONE',  ( 0.000000000000000000, 0.9961946980917459893, -0.08715574274765383600 ) ) ;
#1341=CARTESIAN_POINT ( 'NONE',  ( 3.499999999999999556, 0.000000000000000000, 0.000000000000000000 ) ) ;
#1342=ORIENTED_EDGE ( 'NONE', *, *, #8382, .F. ) ;
#1349=CARTESIAN_POINT ( 'NONE',  ( -3.650050802731187094, 2.331437884370912705, -1.887961173149511618 ) ) ;
#1352=VERTEX_POINT ( 'NONE', #28035 ) ;
#1355=CARTESIAN_POINT ( 'NONE',  ( -4.562550801365594211, 2.228590825266444142, 2.752080473201636845 ) ) ;
#1357=LINE ( 'NONE', #11377, #17711 ) ;
#1360=CARTESIAN_POINT ( 'NONE',  ( -6.537550801365592967, 1.828967928396027176, -3.368539882008727115 ) ) ;
#1362=B_SPLINE_CURVE_WITH_KNOTS ( 'NONE', 3,
 ( #14293, #17144, #27357, #26860, #4472, #14648, #3977, #21831, #32042, #9112 ),
 .UNSPECIFIED., .F., .F.,
 ( 4, 2, 2, 2, 4 ),
 ( 2.493548413911061648E-07, 0.0005478513795029414657, 0.001095453404164491943, 0.001643055428826042203, 0.002190657453487592464 ),
 .UNSPECIFIED. ) ;
#1363=CARTESIAN_POINT ( 'NONE',  ( 6.883866482134012088, 2.190971798910059221, -8.452201317944583181 ) ) ;
#1366=CARTESIAN_POINT ( 'NONE',  ( 5.377543748152549874, -6.940565734314570356, -4.007137495034885255 ) ) ;
#1375=CARTESIAN_POINT ( 'NONE',  ( -3.487550801365593589, -2.228590825266444586, -2.752080473201636401 ) ) ;
#1377=EDGE_LOOP ( 'NONE', ( #9486, #23820, #28856 ) ) ;
#1378=CYLINDRICAL_SURFACE ( 'NONE', #9161, 6.248999999999999666 ) ;
#1379=EDGE_CURVE ( 'NONE', #9138, #16840, #2521, .T. ) ;
#1381=CARTESIAN_POINT ( 'NONE',  ( 1.750000000000000222, 1.106368468154430129, 8.427689411260576691 ) ) ;
#1388=ORIENTED_EDGE ( 'NONE', *, *, #12943, .F. ) ;
#1402=EDGE_CURVE ( 'NONE', #16153, #8879, #12841, .T. ) ;
#1407=ORIENTED_EDGE ( 'NONE', *, *, #7509, .T. ) ;
#1408=DIRECTION ( 'NONE',  ( 0.000000000000000000, 0.000000000000000000, 1.000000000000000000 ) ) ;
#1412=DIRECTION ( 'NONE',  ( 0.000000000000000000, 0.5735764363510448272, -0.8191520442889927978 ) ) ;
#1413=ORIENTED_EDGE ( 'NONE', *, *, #1242, .F. ) ;
#1414=DIRECTION ( 'NONE',  ( 0.000000000000000000, 0.000000000000000000, -1.000000000000000000 ) ) ;
#1416=ORIENTED_EDGE ( 'NONE', *, *, #33000, .T. ) ;
#1419=ORIENTED_EDGE ( 'NONE', *, *, #2054, .T. ) ;
#1433=CARTESIAN_POINT ( 'NONE',  ( 5.612718383992088889, 1.229942497144144165, -8.123482740191956708 ) ) ;
#1434=LINE ( 'NONE', #1279, #9586 ) ;
#1435=LINE ( 'NONE', #9086, #19970 ) ;
#1444=EDGE_CURVE ( 'NONE', #19214, #4152, #5906, .T. ) ;
#1446=EDGE_CURVE ( 'NONE', #27971, #32312, #10186, .T. ) ;
#1447=CARTESIAN_POINT ( 'NONE',  ( -5.300050802731187005, 1.549418761218566143, -2.853674364686379583 ) ) ;
#1449=CARTESIAN_POINT ( 'NONE',  ( -6.700050800000000528, 2.983565686104819648, 0.3135853898029609677 ) ) ;
#1455=ORIENTED_EDGE ( 'NONE', *, *, #8745, .F. ) ;
#1458=CARTESIAN_POINT ( 'NONE',  ( -2.750050800000000351, 3.113457007523260156, -0.9222479816126439855 ) ) ;
#1471=CARTESIAN_POINT ( 'NONE',  ( 5.377543748152550762, -7.530955069117533540, 2.741043480754901118 ) ) ;
#1472=CARTESIAN_POINT ( 'NONE',  ( 3.499999999999999556, 6.100541242131516384, -3.528937025535512362 ) ) ;
#1480=CARTESIAN_POINT ( 'NONE',  ( 5.612718383992089777, -1.229942497144091096, 8.123482740191967366 ) ) ;
#1484=CARTESIAN_POINT ( 'NONE',  ( 6.883866557622098981, 2.328663417917440359, 8.415306967752686162 ) ) ;
#1487=( BOUNDED_CURVE ( )  B_SPLINE_CURVE ( 2, ( #25849, #18969, #15798, #2966, #23323, #26007, #3113, #583, #1562, #24128, #14399 ),
 .UNSPECIFIED., .F., .F. ) 
 B_SPLINE_CURVE_WITH_KNOTS ( ( 3, 2, 2, 2, 2, 3 ),
 ( 0.8103822619934377691, 0.8125000000000000000, 0.8281250000000000000, 0.8437500000000000000, 0.8593750000000000000, 0.8728822619934377691 ),
 .UNSPECIFIED. ) 
 CURVE ( )  GEOMETRIC_REPRESENTATION_ITEM ( )  RATIONAL_B_SPLINE_CURVE ( ( 0.9821626249036861100, 0.9896829947469995004, 1.000000000000000000, 0.9238795325112867385, 1.000000000000000000, 0.9238795325112867385, 1.000000000000000000, 0.9238795325112867385, 1.000000000000000000, 0.9341965377642872381, 0.9821626249036861100 ) ) 
 REPRESENTATION_ITEM ( '' )  );
#1491=DIRECTION ( 'NONE',  ( -1.000000000000000000, -0.000000000000000000, -0.000000000000000000 ) ) ;
#1492=ORIENTED_EDGE ( 'NONE', *, *, #30465, .T. ) ;
#1497=EDGE_CURVE ( 'NONE', #8026, #14221, #16590, .T. ) ;
#1500=CARTESIAN_POINT ( 'NONE',  ( 5.377543748152548986, -7.530955069117495349, -2.741043480755002371 ) ) ;
#1501=ORIENTED_EDGE ( 'NONE', *, *, #21502, .T. ) ;
#1503=CARTESIAN_POINT ( 'NONE',  ( 5.887530252753768067, 6.185189124321821552, 5.676096663009825072 ) ) ;
#1504=PLANE ( 'NONE',  #11782 ) ;
#1508=ORIENTED_EDGE ( 'NONE', *, *, #32177, .T. ) ;
#1509=CARTESIAN_POINT ( 'NONE',  ( -7.137550801365592612, 3.368539882008727115, 1.828967928396026954 ) ) ;
#1510=DIRECTION ( 'NONE',  ( 0.000000000000000000, 0.7071067811865466846, -0.7071067811865483499 ) ) ;
#1513=EDGE_LOOP ( 'NONE', ( #9183, #1110, #21796, #17096 ) ) ;
#1516=ORIENTED_EDGE ( 'NONE', *, *, #29780, .F. ) ;
#1520=CARTESIAN_POINT ( 'NONE',  ( 0.000000000000000000, 4.438567988583082879, 7.249076783337693008 ) ) ;
#1526=CARTESIAN_POINT ( 'NONE',  ( -3.987550801365593145, 3.521866450007987037, 0.3701630799359328372 ) ) ;
#1528=DIRECTION ( 'NONE',  ( 1.000000000000000000, -0.000000000000000000, -0.000000000000000000 ) ) ;
#1530=CARTESIAN_POINT ( 'NONE',  ( 7.249760686538667009, -1.391664247347281780, 7.892520144992429820 ) ) ;
#1531=DIRECTION ( 'NONE',  ( -1.000000000000000000, -0.000000000000000000, -0.000000000000000000 ) ) ;
#1532=CARTESIAN_POINT ( 'NONE',  ( -3.700050800000000084, 0.3135853898029611342, -2.983565686104819648 ) ) ;
#1536=VERTEX_POINT ( 'NONE', #29508 ) ;
#1551=VERTEX_POINT ( 'NONE', #24147 ) ;
#1552=CARTESIAN_POINT ( 'NONE',  ( -4.607304909706597229, -1.062355717592097015, -2.999999999999998668 ) ) ;
#1554=DIRECTION ( 'NONE',  ( 0.000000000000000000, 0.7071067811865434649, 0.7071067811865516806 ) ) ;
#1555=DIRECTION ( 'NONE',  ( -1.000000000000000000, -0.000000000000000000, -0.000000000000000000 ) ) ;
#1556=CARTESIAN_POINT ( 'NONE',  ( 0.000000000000000000, 4.058600654062850310, 7.468451026206211374 ) ) ;
#1559=DIRECTION ( 'NONE',  ( 0.000000000000000000, 0.000000000000000000, 1.000000000000000000 ) ) ;
#1562=CARTESIAN_POINT ( 'NONE',  ( -2.250050802731187183, -1.887961173149512062, -2.331437884370912261 ) ) ;
#1565=CARTESIAN_POINT ( 'NONE',  ( 7.249760686538667009, -8.014274990069656823, 8.669741416787380218E-17 ) ) ;
#1567=VERTEX_POINT ( 'NONE', #1274 ) ;
#1584=EDGE_CURVE ( 'NONE', #10995, #30996, #32023, .T. ) ;
#1586=CARTESIAN_POINT ( 'NONE',  ( -8.000050800000000351, 0.000000000000000000, -3.000000000000000444 ) ) ;
#1595=CARTESIAN_POINT ( 'NONE',  ( -6.850050802731187716, 2.331437884370912705, -1.887961173149511618 ) ) ;
#1598=CARTESIAN_POINT ( 'NONE',  ( -7.687550801365593323, -2.752080473201636845, 2.228590825266444586 ) ) ;
#1602=CARTESIAN_POINT ( 'NONE',  ( 3.499999999999999556, 3.771202944355777298, -4.982773259188332027 ) ) ;
#1604=VERTEX_POINT ( 'NONE', #13769 ) ;
#1606=CARTESIAN_POINT ( 'NONE',  ( -7.300050800000001061, -0.3135853898029607456, 2.983565686104819648 ) ) ;
#1611=CARTESIAN_POINT ( 'NONE',  ( -2.557304906975409686, 1.062355717592091686, 3.000000000000001332 ) ) ;
#1612=ORIENTED_EDGE ( 'NONE', *, *, #27716, .T. ) ;
#1614=CARTESIAN_POINT ( 'NONE',  ( -6.000050800000000351, 2.331437884370912705, -1.887961173149511618 ) ) ;
#1619=ORIENTED_EDGE ( 'NONE', *, *, #17958, .F. ) ;
#1626=CIRCLE ( 'NONE', #28847, 2.999999999999999112 ) ;
#1630=CIRCLE ( 'NONE', #20320, 6.248999999999999666 ) ;
#1635=EDGE_CURVE ( 'NONE', #14801, #31497, #24317, .T. ) ;
#1637=CARTESIAN_POINT ( 'NONE',  ( -8.000050800000002127, 3.541248556864417196, 0.01107501445590582979 ) ) ;
#1638=DIRECTION ( 'NONE',  ( 0.000000000000000000, 0.000000000000000000, 1.000000000000000000 ) ) ;
#1645=DIRECTION ( 'NONE',  ( 0.000000000000000000, 0.08715574274766293983, -0.9961946980917451011 ) ) ;
#1647=PLANE ( 'NONE',  #32162 ) ;
#1649=DIRECTION ( 'NONE',  ( 1.000000000000000000, -0.000000000000000000, -0.000000000000000000 ) ) ;
#1650=CARTESIAN_POINT ( 'NONE',  ( -8.000050800000000351, 0.3135937863663861291, -2.983645574069408557 ) ) ;
#1653=CARTESIAN_POINT ( 'NONE',  ( 3.499999999999999556, 0.000000000000000000, 0.000000000000000000 ) ) ;
#1654=AXIS2_PLACEMENT_3D ( 'NONE', #5855, #23759, #26449 ) ;
#1659=DIRECTION ( 'NONE',  ( 1.000000000000000000, -0.000000000000000000, -0.000000000000000000 ) ) ;
#1664=CARTESIAN_POINT ( 'NONE',  ( 7.064632951172269415, 6.226446564517915228, 6.147671362329237610 ) ) ;
#1665=CARTESIAN_POINT ( 'NONE',  ( 6.037141869538512395, -7.552970526864664080, -3.843044125430146174 ) ) ;
#1667=B_SPLINE_CURVE_WITH_KNOTS ( 'NONE', 3,
 ( #9661, #2653, #12671, #2343, #19886, #17374, #7180, #27567, #4666, #20211 ),
 .UNSPECIFIED., .F., .F.,
 ( 4, 2, 2, 2, 4 ),
 ( 1.968338519011545307E-07, 0.0005467926395225674360, 0.001093388445193233666, 0.001639984250863899895, 0.002186580056534566125 ),
 .UNSPECIFIED. ) ;
#1669=CARTESIAN_POINT ( 'NONE',  ( 5.885541806331896275, 3.871259391815556228, -7.447669719165293856 ) ) ;
#1670=VERTEX_POINT ( 'NONE', #30949 ) ;
#1671=CARTESIAN_POINT ( 'NONE',  ( -7.962550801365594566, 2.752080473201636845, -2.228590825266444142 ) ) ;
#1676=ORIENTED_EDGE ( 'NONE', *, *, #19097, .F. ) ;
#1679=VECTOR ( 'NONE', #13330, 1000.000000000000000 ) ;
#1686=CARTESIAN_POINT ( 'NONE',  ( -6.162942409646512409, 7.727249047114547632E-16, -2.999999999999999556 ) ) ;
#1691=CARTESIAN_POINT ( 'NONE',  ( -4.037550801365593856, 3.675193018007247403, -1.088641768524161391 ) ) ;
#1692=ORIENTED_EDGE ( 'NONE', *, *, #28673, .T. ) ;
#1694=ORIENTED_EDGE ( 'NONE', *, *, #27162, .F. ) ;
#1697=VECTOR ( 'NONE', #32166, 1000.000000000000000 ) ;
#1701=ADVANCED_FACE ( 'NONE', ( #7724 ), #13437, .T. ) ;
#1730=CARTESIAN_POINT ( 'NONE',  ( 3.499999999999999556, 6.100541242131516384, 3.528937025535512362 ) ) ;
#1739=AXIS2_PLACEMENT_3D ( 'NONE', #4236, #6750, #7255 ) ;
#1742=ORIENTED_EDGE ( 'NONE', *, *, #21414, .F. ) ;
#1747=CIRCLE ( 'NONE', #18282, 6.248999999999999666 ) ;
#1753=ORIENTED_EDGE ( 'NONE', *, *, #25497, .T. ) ;
#1764=CARTESIAN_POINT ( 'NONE',  ( 0.000000000000000000, 0.000000000000000000, 0.000000000000000000 ) ) ;
#1765=DIRECTION ( 'NONE',  ( 0.000000000000000000, 0.000000000000000000, -1.000000000000000000 ) ) ;
#1766=CARTESIAN_POINT ( 'NONE',  ( 6.038144853276843804, 1.027626812408000800, 8.412419482080409239 ) ) ;
#1773=VECTOR ( 'NONE', #10695, 1000.000000000000000 ) ;
#1775=AXIS2_PLACEMENT_3D ( 'NONE', #31225, #26180, #5639 ) ;
#1781=CARTESIAN_POINT ( 'NONE',  ( -7.100050802731186828, -2.853674364686378695, -1.549418761218566809 ) ) ;
#1784=CARTESIAN_POINT ( 'NONE',  ( -4.500050800000000351, 0.3135853898029611342, -2.983565686104819648 ) ) ;
#1786=B_SPLINE_CURVE_WITH_KNOTS ( 'NONE', 3,
 ( #3765, #4104, #26830, #19492, #14270, #1766, #24466, #32369, #29684, #4253 ),
 .UNSPECIFIED., .F., .F.,
 ( 4, 2, 2, 2, 4 ),
 ( 1.968338519010709921E-07, 0.0005467928198071728228, 0.001093388805762444439, 0.001639984791717716056, 0.002186580777672988106 ),
 .UNSPECIFIED. ) ;
#1789=CARTESIAN_POINT ( 'NONE',  ( 3.499999999999999556, 0.000000000000000000, 0.000000000000000000 ) ) ;
#1791=ORIENTED_EDGE ( 'NONE', *, *, #12541, .F. ) ;
#1794=ADVANCED_FACE ( 'NONE', ( #8029 ), #364, .T. ) ;
#1795=ORIENTED_EDGE ( 'NONE', *, *, #13088, .F. ) ;
#1805=CARTESIAN_POINT ( 'NONE',  ( 5.489321486716459475, -1.512021494499641294, 7.976795196726682136 ) ) ;
#1816=FACE_OUTER_BOUND ( 'NONE', #25502, .T. ) ;
#1817=ORIENTED_EDGE ( 'NONE', *, *, #10529, .F. ) ;
#1818=CARTESIAN_POINT ( 'NONE',  ( 6.038144483126824724, -8.463061282283012687, -0.4487862922133540877 ) ) ;
#1820=CARTESIAN_POINT ( 'NONE',  ( -10.00000000000000000, 0.000000000000000000, 0.000000000000000000 ) ) ;
#1821=EDGE_CURVE ( 'NONE', #11829, #4589, #18560, .T. ) ;
#1825=CARTESIAN_POINT ( 'NONE',  ( 5.885541416630537093, 0.3712256868992431236, 8.385500676968929312 ) ) ;
#1829=ORIENTED_EDGE ( 'NONE', *, *, #18613, .T. ) ;
#1830=EDGE_CURVE ( 'NONE', #1536, #7257, #16371, .T. ) ;
#1833=CARTESIAN_POINT ( 'NONE',  ( -8.054531657079158080, -1.545410377633946286, 2.846291840500174697 ) ) ;
#1850=CARTESIAN_POINT ( 'NONE',  ( 7.249760686538667009, 3.748318449932293905, 7.906491560603678082 ) ) ;
#1851=DIRECTION ( 'NONE',  ( 0.000000000000000000, 0.5735764363510594821, -0.8191520442889824727 ) ) ;
#1854=CARTESIAN_POINT ( 'NONE',  ( 6.357668022120092743, 6.210015626210386053, 5.959864878090697538 ) ) ;
#1861=VECTOR ( 'NONE', #23980, 1000.000000000000000 ) ;
#1862=CARTESIAN_POINT ( 'NONE',  ( -4.387550801365594388, -3.521866450007987037, -0.3701630799359323931 ) ) ;
#1868=ORIENTED_EDGE ( 'NONE', *, *, #5727, .T. ) ;
#1881=LINE ( 'NONE', #19431, #27332 ) ;
#1890=DIRECTION ( 'NONE',  ( -1.000000000000000000, -0.000000000000000000, 0.000000000000000000 ) ) ;
#1903=CYLINDRICAL_SURFACE ( 'NONE', #9030, 3.000000000000000444 ) ;
#1909=FACE_OUTER_BOUND ( 'NONE', #30106, .T. ) ;
#1911=EDGE_CURVE ( 'NONE', #25076, #31964, #6186, .T. ) ;
#1919=CARTESIAN_POINT ( 'NONE',  ( -5.287550801365593856, -2.752080473201636845, 2.228590825266444586 ) ) ;
#1926=EDGE_LOOP ( 'NONE', ( #4636, #2359, #17058, #4963 ) ) ;
#1929=CARTESIAN_POINT ( 'NONE',  ( 5.612974044843318744, -8.123783100924557132, 1.229732182294874354 ) ) ;
#1939=CARTESIAN_POINT ( 'NONE',  ( 4.749760686538667009, -5.151476664237435443, -6.139290821770307716 ) ) ;
#1944=EDGE_CURVE ( 'NONE', #30369, #3680, #23277, .T. ) ;
#1948=DIRECTION ( 'NONE',  ( 0.000000000000000000, 0.5877852522924689183, 0.8090169943749504489 ) ) ;
#1950=ADVANCED_FACE ( 'NONE', ( #32435 ), #9666, .F. ) ;
#1952=CARTESIAN_POINT ( 'NONE',  ( -6.000050802731188959, 3.113457007523260156, -0.9222479816126439855 ) ) ;
#1954=CARTESIAN_POINT ( 'NONE',  ( -3.200050800000000528, -2.331437884370912705, 1.887961173149512062 ) ) ;
#1955=B_SPLINE_CURVE_WITH_KNOTS ( 'NONE', 3,
 ( #8617, #32022, #16455, #19322, #19144, #21182, #9092, #23983, #3775, #26663 ),
 .UNSPECIFIED., .F., .F.,
 ( 4, 2, 2, 2, 4 ),
 ( 1.968338519012340988E-07, 0.0005467927057105487470, 0.001093388577569196288, 0.001639984449427843395, 0.002186580321286490502 ),
 .UNSPECIFIED. ) ;
#1961=ORIENTED_EDGE ( 'NONE', *, *, #28424, .F. ) ;
#1975=CYLINDRICAL_SURFACE ( 'NONE', #32083, 8.500000000000000000 ) ;
#1979=CARTESIAN_POINT ( 'NONE',  ( -4.300050802731187005, 2.853674364686379583, 1.549418761218565921 ) ) ;
#1988=ORIENTED_EDGE ( 'NONE', *, *, #16813, .T. ) ;
#1989=CARTESIAN_POINT ( 'NONE',  ( -5.354531657079158791, -0.9198621039125872700, -3.105402419394638791 ) ) ;
#1992=CARTESIAN_POINT ( 'NONE',  ( 3.499999999999999556, -4.147285340411824173, 5.698247474649390298 ) ) ;
#1993=DIRECTION ( 'NONE',  ( 0.000000000000000000, 0.000000000000000000, 1.000000000000000000 ) ) ;
#1996=ORIENTED_EDGE ( 'NONE', *, *, #9439, .T. ) ;
#2001=DIRECTION ( 'NONE',  ( 0.000000000000000000, -0.8191520442889993481, 0.5735764363510352792 ) ) ;
#2002=CARTESIAN_POINT ( 'NONE',  ( 5.489343555808770425, -0.1039150536217892384, -8.118190043691532409 ) ) ;
#2005=CARTESIAN_POINT ( 'NONE',  ( 5.377543748152551650, 6.139290821770257089, 5.151476664237498504 ) ) ;
#2011=CARTESIAN_POINT ( 'NONE',  ( -3.487550801365593589, -2.228590825266444586, -2.752080473201636401 ) ) ;
#2015=EDGE_CURVE ( 'NONE', #22347, #9445, #22227, .T. ) ;
#2016=EDGE_LOOP ( 'NONE', ( #25355, #28526, #8995 ) ) ;
#2017=PLANE ( 'NONE',  #28323 ) ;
#2018=ORIENTED_EDGE ( 'NONE', *, *, #4844, .T. ) ;
#2021=CARTESIAN_POINT ( 'NONE',  ( 6.883866482134012976, 8.452201317944600945, 2.190971798909973067 ) ) ;
#2024=CARTESIAN_POINT ( 'NONE',  ( -6.556376981307135310, -0.1572233378491242062, 2.999999999999999556 ) ) ;
#2026=CARTESIAN_POINT ( 'NONE',  ( 5.377543748152548986, 8.014274990069656823, -8.669741416787380218E-17 ) ) ;
#2027=PRODUCT ( 'Part4_Gear', 'Part4_Gear', '', ( #29746 ) ) ;
#2041=ORIENTED_EDGE ( 'NONE', *, *, #12215, .T. ) ;
#2043=CARTESIAN_POINT ( 'NONE',  ( 0.000000000000000000, -7.009698679648281860, -0.7308381473897611613 ) ) ;
#2051=FACE_OUTER_BOUND ( 'NONE', #27992, .T. ) ;
#2053=ORIENTED_EDGE ( 'NONE', *, *, #5956, .F. ) ;
#2054=EDGE_CURVE ( 'NONE', #16287, #14398, #28816, .T. ) ;
#2056=B_SPLINE_CURVE_WITH_KNOTS ( 'NONE', 3,
 ( #5431, #10944, #26330, #277, #13597, #23802, #915, #30862, #23639, #21292 ),
 .UNSPECIFIED., .F., .F.,
 ( 4, 2, 2, 2, 4 ),
 ( 2.740849916261192663E-07, 0.0005478761651001754851, 0.001095478245208724843, 0.001643080325317274092, 0.002190682405425823341 ),
 .UNSPECIFIED. ) ;
#2064=CYLINDRICAL_SURFACE ( 'NONE', #13985, 2.999999999999999112 ) ;
#2065=CARTESIAN_POINT ( 'NONE',  ( -5.587550801365593678, 3.521866450007987037, 0.3701630799359328372 ) ) ;
#2066=ORIENTED_EDGE ( 'NONE', *, *, #4474, .F. ) ;
#2074=ORIENTED_EDGE ( 'NONE', *, *, #2480, .T. ) ;
#2080=EDGE_CURVE ( 'NONE', #22347, #11908, #19171, .T. ) ;
#2097=CARTESIAN_POINT ( 'NONE',  ( -2.550050802731187005, -0.3135853898029607456, 2.983565686104819648 ) ) ;
#2099=CARTESIAN_POINT ( 'NONE',  ( -3.600050800000000883, 2.331437884370912705, -1.887961173149511618 ) ) ;
#2101=CARTESIAN_POINT ( 'NONE',  ( -4.512942406915326998, 4.884725290497410777E-15, -2.999999999999999556 ) ) ;
#2104=DIRECTION ( 'NONE',  ( 1.000000000000000000, 0.000000000000000000, 0.000000000000000000 ) ) ;
#2111=CARTESIAN_POINT ( 'NONE',  ( 4.749760686538667009, -4.007137495034861274, 6.940565734314584567 ) ) ;
#2113=EDGE_CURVE ( 'NONE', #9966, #24417, #15124, .T. ) ;
#2114=ORIENTED_EDGE ( 'NONE', *, *, #12286, .T. ) ;
#2121=DIRECTION ( 'NONE',  ( 0.000000000000000000, 0.000000000000000000, 1.000000000000000000 ) ) ;
#2123=CARTESIAN_POINT ( 'NONE',  ( -3.300050802731187449, -1.549418761218565255, 2.853674364686380471 ) ) ;
#2124=ORIENTED_EDGE ( 'NONE', *, *, #16433, .T. ) ;
#2125=CARTESIAN_POINT ( 'NONE',  ( 0.000000000000000000, -0.1221666339523235223, -6.247805719894684806 ) ) ;
#2130=CARTESIAN_POINT ( 'NONE',  ( -8.000050799999998574, 2.743648536415450145, 2.018700866895823065 ) ) ;
#2136=CARTESIAN_POINT ( 'NONE',  ( -7.862550801365593145, 3.521866450007987037, 0.3701630799359328372 ) ) ;
#2138=CARTESIAN_POINT ( 'NONE',  ( -7.554531657079158968, 3.105402419394639235, -0.9198621039125850496 ) ) ;
#2145=DIRECTION ( 'NONE',  ( -1.000000000000000000, 0.000000000000000000, 0.000000000000000000 ) ) ;
#2147=CARTESIAN_POINT ( 'NONE',  ( 5.612718825656738630, -5.126902779943826260, 6.420171604529170573 ) ) ;
#2151=EDGE_CURVE ( 'NONE', #13430, #28488, #2934, .T. ) ;
#2152=CIRCLE ( 'NONE', #27218, 2.999999999999999112 ) ;
#2155=CARTESIAN_POINT ( 'NONE',  ( 5.887530180601101115, 3.870837198608099161, 7.449245365665808194 ) ) ;
#2158=CARTESIAN_POINT ( 'NONE',  ( -8.000050800000003903, -2.956547957031034457, 0.5836481786531007021 ) ) ;
#2164=CARTESIAN_POINT ( 'NONE',  ( -2.337550801365593678, 3.368539882008727115, 1.828967928396026954 ) ) ;
#2172=DIRECTION ( 'NONE',  ( 0.000000000000000000, 0.4067366430758009299, -0.9135454576426005335 ) ) ;
#2173=DIRECTION ( 'NONE',  ( 0.000000000000000000, 0.000000000000000000, 1.000000000000000000 ) ) ;
#2182=EDGE_CURVE ( 'NONE', #21075, #3311, #19413, .T. ) ;
#2190=EDGE_CURVE ( 'NONE', #25433, #6855, #26216, .T. ) ;
#2191=ORIENTED_EDGE ( 'NONE', *, *, #14033, .F. ) ;
#2194=CARTESIAN_POINT ( 'NONE',  ( 0.000000000000000000, -7.851777359433977921, -3.255701506262514311 ) ) ;
#2196=ORIENTED_EDGE ( 'NONE', *, *, #8745, .T. ) ;
#2197=VECTOR ( 'NONE', #9590, 1000.000000000000114 ) ;
#2225=AXIS2_PLACEMENT_3D ( 'NONE', #10557, #32835, #7388 ) ;
#2227=CARTESIAN_POINT ( 'NONE',  ( -6.737550801365594033, -3.368539882008727115, -1.828967928396027842 ) ) ;
#2230=AXIS2_PLACEMENT_3D ( 'NONE', #28008, #22162, #9936 ) ;
#2232=CARTESIAN_POINT ( 'NONE',  ( 0.000000000000000000, 7.003298780661491918, -4.817032923780496745 ) ) ;
#2246=DIRECTION ( 'NONE',  ( 0.000000000000000000, -0.4226182617406868403, -0.9063077870366559319 ) ) ;
#2248=VERTEX_POINT ( 'NONE', #11003 ) ;
#2258=DIRECTION ( 'NONE',  ( 0.000000000000000000, 0.000000000000000000, 1.000000000000000000 ) ) ;
#2260=VECTOR ( 'NONE', #27159, 1000.000000000000000 ) ;
#2262=AXIS2_PLACEMENT_3D ( 'NONE', #21932, #22272, #32824 ) ;
#2263=CARTESIAN_POINT ( 'NONE',  ( 6.530491241813344061, 8.637950316517745364, 0.6236753264480845438 ) ) ;
#2273=EDGE_CURVE ( 'NONE', #11269, #32858, #22107, .T. ) ;
#2274=CARTESIAN_POINT ( 'NONE',  ( -3.150050802731187538, -2.983565686104819648, -0.3135853898029605791 ) ) ;
#2276=CARTESIAN_POINT ( 'NONE',  ( -4.250050800000000351, 2.853674364686379583, 1.549418761218565921 ) ) ;
#2278=CYLINDRICAL_SURFACE ( 'NONE', #21046, 8.500000000000000000 ) ;
#2282=ORIENTED_EDGE ( 'NONE', *, *, #3154, .T. ) ;
#2284=CIRCLE ( 'NONE', #11860, 6.249000000000001442 ) ;
#2291=ORIENTED_EDGE ( 'NONE', *, *, #33027, .F. ) ;
#2306=( BOUNDED_CURVE ( )  B_SPLINE_CURVE ( 2, ( #6498, #31928, #6676, #9341, #1349, #31775, #14508, #8846, #27062, #19053, #16703 ),
 .UNSPECIFIED., .F., .F. ) 
 B_SPLINE_CURVE_WITH_KNOTS ( ( 3, 2, 2, 2, 2, 3 ),
 ( 0.6228822619934377691, 0.6250000000000000000, 0.6406250000000000000, 0.6562500000000000000, 0.6718750000000000000, 0.6853822619934377691 ),
 .UNSPECIFIED. ) 
 CURVE ( )  GEOMETRIC_REPRESENTATION_ITEM ( )  RATIONAL_B_SPLINE_CURVE ( ( 0.9821626249036861100, 0.9896829947469995004, 1.000000000000000000, 0.9238795325112867385, 1.000000000000000000, 0.9238795325112867385, 1.000000000000000000, 0.9238795325112867385, 1.000000000000000000, 0.9341965377642872381, 0.9821626249036861100 ) ) 
 REPRESENTATION_ITEM ( '' )  );
#2320=ORIENTED_EDGE ( 'NONE', *, *, #32476, .T. ) ;
#2322=CARTESIAN_POINT ( 'NONE',  ( -7.312550801365594211, -1.088641768524163389, -3.675193018007246071 ) ) ;
#2325=CARTESIAN_POINT ( 'NONE',  ( -6.204531657079157547, -1.883076972206379818, -2.325406398514292761 ) ) ;
#2336=CARTESIAN_POINT ( 'NONE',  ( -3.706376978575949277, 0.1572233378491263989, -2.999999999999999556 ) ) ;
#2341=TOROIDAL_SURFACE ( 'NONE', #18867, 6.000000000000000000, 2.750000000000000444 ) ;
#2342=CIRCLE ( 'NONE', #16123, 6.248999999999998778 ) ;
#2343=CARTESIAN_POINT ( 'NONE',  ( 6.530491712438077023, 4.859093986587958547, -7.168846788212641208 ) ) ;
#2349=CARTESIAN_POINT ( 'NONE',  ( -8.000050800000000351, -1.352866546975186379, -2.692392053336499114 ) ) ;
#2355=CARTESIAN_POINT ( 'NONE',  ( -4.762550801365593500, 2.752080473201636845, -2.228590825266444142 ) ) ;
#2359=ORIENTED_EDGE ( 'NONE', *, *, #3562, .T. ) ;
#2366=VECTOR ( 'NONE', #53, 1000.000000000000114 ) ;
#2383=ORIENTED_EDGE ( 'NONE', *, *, #22399, .T. ) ;
#2384=CARTESIAN_POINT ( 'NONE',  ( -5.007304909706597584, 1.062355717592095683, 2.999999999999999112 ) ) ;
#2388=CARTESIAN_POINT ( 'NONE',  ( -1.996286585346912723, 1.323625320507515246, 3.284597389079959573 ) ) ;
#2389=FACE_OUTER_BOUND ( 'NONE', #26903, .T. ) ;
#2396=CARTESIAN_POINT ( 'NONE',  ( 6.038145077921538650, -3.316258947000913615, 7.799182446117183254 ) ) ;
#2400=EDGE_LOOP ( 'NONE', ( #9114, #15035, #17606 ) ) ;
#2409=ORIENTED_EDGE ( 'NONE', *, *, #1584, .F. ) ;
#2412=CARTESIAN_POINT ( 'NONE',  ( -6.637550801365594388, -1.088641768524163611, -3.675193018007245627 ) ) ;
#2415=CARTESIAN_POINT ( 'NONE',  ( 4.749760686538667009, 6.139290821770257089, 5.151476664237498504 ) ) ;
#2419=ORIENTED_EDGE ( 'NONE', *, *, #20954, .T. ) ;
#2421=ORIENTED_EDGE ( 'NONE', *, *, #22042, .T. ) ;
#2422=FACE_OUTER_BOUND ( 'NONE', #28113, .T. ) ;
#2423=B_SPLINE_CURVE_WITH_KNOTS ( 'NONE', 3,
 ( #26564, #3664, #8837, #19041, #29232, #3828, #14003, #1338, #21221, #21708, #29388, #26238, #31419, #18695, #6004 ),
 .UNSPECIFIED., .F., .F.,
 ( 4, 1, 2, 2, 2, 2, 2, 4 ),
 ( 0.000000000000000000, 0.1250000000000004996, 0.1875000000000005274, 0.2500000000000005551, 0.3750000000000003886, 0.5000000000000002220, 0.7500000000000001110, 1.000000000000000000 ),
 .UNSPECIFIED. ) ;
#2432=DIRECTION ( 'NONE',  ( 0.000000000000000000, -0.4226182617407029940, -0.9063077870366482713 ) ) ;
#2436=EDGE_CURVE ( 'NONE', #24201, #7257, #30554, .T. ) ;
#2438=DIRECTION ( 'NONE',  ( 0.000000000000000000, -0.9945218953682744001, 0.1045284632676436593 ) ) ;
#2439=LINE ( 'NONE', #17610, #22610 ) ;
#2441=FACE_OUTER_BOUND ( 'NONE', #5767, .T. ) ;
#2449=CARTESIAN_POINT ( 'NONE',  ( 4.749760686538667009, 1.391664247347333294, -7.892520144992419162 ) ) ;
#2450=CARTESIAN_POINT ( 'NONE',  ( -3.850050802731187272, -1.887961173149512062, -2.331437884370912261 ) ) ;
#2452=CARTESIAN_POINT ( 'NONE',  ( -4.337550801365595454, -3.368539882008727115, -1.828967928396028064 ) ) ;
#2453=DIRECTION ( 'NONE',  ( -1.000000000000000000, -0.000000000000000000, -0.000000000000000000 ) ) ;
#2454=FACE_OUTER_BOUND ( 'NONE', #2925, .T. ) ;
#2457=CARTESIAN_POINT ( 'NONE',  ( 6.524595623740805372, -6.028129343649572647, -6.215987993068505801 ) ) ;
#2463=ORIENTED_EDGE ( 'NONE', *, *, #16487, .F. ) ;
#2466=EDGE_LOOP ( 'NONE', ( #6872, #30643, #24132, #30804 ) ) ;
#2472=EDGE_CURVE ( 'NONE', #3311, #21158, #9273, .T. ) ;
#2477=FACE_OUTER_BOUND ( 'NONE', #20771, .T. ) ;
#2480=EDGE_CURVE ( 'NONE', #16558, #6094, #12789, .T. ) ;
#2487=CARTESIAN_POINT ( 'NONE',  ( -6.212550801365593678, 3.368539882008727115, 1.828967928396026954 ) ) ;
#2489=CARTESIAN_POINT ( 'NONE',  ( -6.854531657079157903, 1.545410377633947174, -2.846291840500173365 ) ) ;
#2493=CYLINDRICAL_SURFACE ( 'NONE', #18346, 8.500000000000000000 ) ;
#2494=ORIENTED_EDGE ( 'NONE', *, *, #13332, .T. ) ;
#2498=LINE ( 'NONE', #14364, #26672 ) ;
#2500=CARTESIAN_POINT ( 'NONE',  ( -3.600050800000000883, 2.331437884370912705, -1.887961173149511618 ) ) ;
#2505=CARTESIAN_POINT ( 'NONE',  ( 6.880160201030086853, -0.6895871680712554186, -8.703862158141015826 ) ) ;
#2507=CARTESIAN_POINT ( 'NONE',  ( -8.000050800000000351, -2.031504781066817422, -2.211944486005439359 ) ) ;
#2509=ADVANCED_FACE ( 'NONE', ( #10797 ), #13286, .T. ) ;
#2513=VERTEX_POINT ( 'NONE', #16134 ) ;
#2514=CARTESIAN_POINT ( 'NONE',  ( -6.862550801365594033, -0.3701630799359326152, 3.521866450007987037 ) ) ;
#2517=LINE ( 'NONE', #4681, #12874 ) ;
#2518=ORIENTED_EDGE ( 'NONE', *, *, #6096, .T. ) ;
#2521=B_SPLINE_CURVE_WITH_KNOTS ( 'NONE', 3,
 ( #21167, #21005, #31218, #2980 ),
 .UNSPECIFIED., .F., .F.,
 ( 4, 4 ),
 ( 0.000000000000000000, 0.07623956525986190502 ),
 .UNSPECIFIED. ) ;
#2522=LINE ( 'NONE', #20575, #5427 ) ;
#2523=CARTESIAN_POINT ( 'NONE',  ( 3.499999999999999556, -5.522688772756351838, -6.461416928141299643 ) ) ;
#2530=ORIENTED_EDGE ( 'NONE', *, *, #6923, .T. ) ;
#2544=CARTESIAN_POINT ( 'NONE',  ( -7.862550801365593145, 3.521866450007987037, 0.3701630799359328372 ) ) ;
#2547=DIRECTION ( 'NONE',  ( 1.000000000000000000, 0.000000000000000000, 0.000000000000000000 ) ) ;
#2566=CARTESIAN_POINT ( 'NONE',  ( -7.537550801365592967, -3.368539882008727115, -1.828967928396027842 ) ) ;
#2570=CARTESIAN_POINT ( 'NONE',  ( 6.357667975083866274, 7.724391461487844168, -3.797112024431936295 ) ) ;
#2585=FACE_OUTER_BOUND ( 'NONE', #23253, .T. ) ;
#2594=CARTESIAN_POINT ( 'NONE',  ( 3.499999999999999556, 0.6700234925293823141, -8.473551116235668701 ) ) ;
#2599=FACE_OUTER_BOUND ( 'NONE', #8922, .T. ) ;
#2600=CARTESIAN_POINT ( 'NONE',  ( -2.300050802731187449, -2.853674364686378695, -1.549418761218566809 ) ) ;
#2602=CARTESIAN_POINT ( 'NONE',  ( -6.537550801365592967, 1.828967928396027176, -3.368539882008727115 ) ) ;
#2607=DIRECTION ( 'NONE',  ( -1.000000000000000000, 0.000000000000000000, 0.000000000000000000 ) ) ;
#2627=CARTESIAN_POINT ( 'NONE',  ( 7.249760686538667009, 7.530955069117551304, -2.741043480754851380 ) ) ;
#2633=EDGE_CURVE ( 'NONE', #19839, #19445, #18642, .T. ) ;
#2634=CARTESIAN_POINT ( 'NONE',  ( -8.000050800000009232, 0.05039788597990539631, 3.202937075113939880 ) ) ;
#2639=CARTESIAN_POINT ( 'NONE',  ( -5.362550801365593145, 2.228590825266444142, 2.752080473201636845 ) ) ;
#2641=CARTESIAN_POINT ( 'NONE',  ( -8.200050800000001416, 1.887961173149511618, 2.331437884370912705 ) ) ;
#2642=CARTESIAN_POINT ( 'NONE',  ( 3.499999999999999556, 0.000000000000000000, 0.000000000000000000 ) ) ;
#2653=CARTESIAN_POINT ( 'NONE',  ( 7.064632940817594076, 4.973063321323974328, -7.199384779417069780 ) ) ;
#2657=EDGE_CURVE ( 'NONE', #9041, #21409, #1434, .T. ) ;
#2664=ORIENTED_EDGE ( 'NONE', *, *, #29397, .T. ) ;
#2665=CARTESIAN_POINT ( 'NONE',  ( -6.812550801365595099, -1.828967928396026510, 3.368539882008728004 ) ) ;
#2674=AXIS2_PLACEMENT_3D ( 'NONE', #33045, #13139, #31038 ) ;
#2680=DIRECTION ( 'NONE',  ( -1.000000000000000000, -0.000000000000000000, 0.000000000000000000 ) ) ;
#2695=CARTESIAN_POINT ( 'NONE',  ( -5.250050802731188071, 2.331437884370912705, -1.887961173149511618 ) ) ;
#2697=EDGE_LOOP ( 'NONE', ( #7451, #10386, #1742 ) ) ;
#2700=CARTESIAN_POINT ( 'NONE',  ( -6.362550801365593145, 2.752080473201636845, -2.228590825266444142 ) ) ;
#2702=DIRECTION ( 'NONE',  ( 0.000000000000000000, 0.9961946980917462113, -0.08715574274765046370 ) ) ;
#2704=VERTEX_POINT ( 'NONE', #16953 ) ;
#2728=ORIENTED_EDGE ( 'NONE', *, *, #12116, .T. ) ;
#2732=DIRECTION ( 'NONE',  ( 0.000000000000000000, 0.000000000000000000, 1.000000000000000000 ) ) ;
#2737=VECTOR ( 'NONE', #5297, 1000.000000000000000 ) ;
#2739=PLANE ( 'NONE',  #22984 ) ;
#2745=ORIENTED_EDGE ( 'NONE', *, *, #27846, .F. ) ;
#2747=ORIENTED_EDGE ( 'NONE', *, *, #28588, .F. ) ;
#2751=ORIENTED_EDGE ( 'NONE', *, *, #32175, .T. ) ;
#2752=CARTESIAN_POINT ( 'NONE',  ( 4.749760686538667009, -8.014274990069656823, 8.669741416787380218E-17 ) ) ;
#2757=CARTESIAN_POINT ( 'NONE',  ( 5.885541736258996792, 3.216848386728063947, 7.752826540560520563 ) ) ;
#2763=AXIS2_PLACEMENT_3D ( 'NONE', #16924, #27286, #22780 ) ;
#2767=CARTESIAN_POINT ( 'NONE',  ( 6.037141812302427191, 8.411869123983617413, 1.028012177296115492 ) ) ;
#2772=EDGE_CURVE ( 'NONE', #21921, #11951, #1786, .T. ) ;
#2776=CARTESIAN_POINT ( 'NONE',  ( -5.237550801365594033, -3.675193018007246071, 1.088641768524163167 ) ) ;
#2781=ORIENTED_EDGE ( 'NONE', *, *, #11663, .F. ) ;
#2782=CARTESIAN_POINT ( 'NONE',  ( 6.357668022120090079, -5.080751859797305592, -6.947679035623508526 ) ) ;
#2790=CIRCLE ( 'NONE', #16644, 3.000000000000000444 ) ;
#2792=ORIENTED_EDGE ( 'NONE', *, *, #16898, .F. ) ;
#2805=AXIS2_PLACEMENT_3D ( 'NONE', #22728, #32932, #1851 ) ;
#2812=DIRECTION ( 'NONE',  ( 0.000000000000000000, 0.4226182617406936681, 0.9063077870366527122 ) ) ;
#2817=DIRECTION ( 'NONE',  ( 0.000000000000000000, 0.4226182617406968323, 0.9063077870366511579 ) ) ;
#2821=CARTESIAN_POINT ( 'NONE',  ( -7.062550801365593323, 3.521866450007987037, 0.3701630799359328372 ) ) ;
#2826=CARTESIAN_POINT ( 'NONE',  ( -3.754531657079158258, -0.9198621039125872700, -3.105402419394638791 ) ) ;
#2830=DIRECTION ( 'NONE',  ( -1.000000000000000000, -0.000000000000000000, -0.000000000000000000 ) ) ;
#2833=AXIS2_PLACEMENT_3D ( 'NONE', #24528, #29902, #8988 ) ;
#2845=DIRECTION ( 'NONE',  ( -1.000000000000000000, 0.000000000000000000, 0.000000000000000000 ) ) ;
#2849=EDGE_LOOP ( 'NONE', ( #19340, #11154, #3448, #11215 ) ) ;
#2852=CARTESIAN_POINT ( 'NONE',  ( -8.000050800000003903, -2.998651111664708324, 0.1685590755062153223 ) ) ;
#2855=AXIS2_PLACEMENT_3D ( 'NONE', #31834, #3919, #14096 ) ;
#2858=ORIENTED_EDGE ( 'NONE', *, *, #29718, .F. ) ;
#2859=CARTESIAN_POINT ( 'NONE',  ( -6.962550801365593678, 2.228590825266444142, 2.752080473201636845 ) ) ;
#2861=EDGE_CURVE ( 'NONE', #15674, #4058, #6388, .T. ) ;
#2863=DIRECTION ( 'NONE',  ( -1.000000000000000000, 0.000000000000000000, -0.000000000000000000 ) ) ;
#2865=AXIS2_PLACEMENT_3D ( 'NONE', #14796, #7619, #2104 ) ;
#2871=ADVANCED_FACE ( 'NONE', ( #4600 ), #24973, .F. ) ;
#2881=ORIENTED_EDGE ( 'NONE', *, *, #8616, .F. ) ;
#2887=CARTESIAN_POINT ( 'NONE',  ( 0.000000000000000000, -5.979767908488853756, 1.814490771706161132 ) ) ;
#2891=ORIENTED_EDGE ( 'NONE', *, *, #2472, .T. ) ;
#2897=CARTESIAN_POINT ( 'NONE',  ( 7.249760686538667009, -1.391664247347174754, -7.892520144992448472 ) ) ;
#2899=DIRECTION ( 'NONE',  ( 0.000000000000000000, 0.08715574274765046370, 0.9961946980917462113 ) ) ;
#2901=CARTESIAN_POINT ( 'NONE',  ( 7.249760686538667009, 7.953573330858264789, -3.647351267791489882 ) ) ;
#2904=LINE ( 'NONE', #10701, #26321 ) ;
#2920=CARTESIAN_POINT ( 'NONE',  ( 6.356382399260308347, 7.150437133400997070, -4.790388219480488097 ) ) ;
#2923=LINE ( 'NONE', #20455, #20451 ) ;
#2924=LINE ( 'NONE', #29267, #4429 ) ;
#2925=EDGE_LOOP ( 'NONE', ( #6215, #27122, #18110, #31968 ) ) ;
#2934=B_SPLINE_CURVE_WITH_KNOTS ( 'NONE', 3,
 ( #5812, #31083, #10838, #16176, #28719, #6153, #13803, #18525, #15992, #26403 ),
 .UNSPECIFIED., .F., .F.,
 ( 4, 2, 2, 2, 4 ),
 ( 3.032460776720355987E-07, 0.0005479053915603968516, 0.001095507537043121683, 0.001643109682525846190, 0.002190711828008571130 ),
 .UNSPECIFIED. ) ;
#2940=ORIENTED_EDGE ( 'NONE', *, *, #26592, .T. ) ;
#2945=CARTESIAN_POINT ( 'NONE',  ( 7.249760686538667009, 5.151476664237477188, 6.139290821770273077 ) ) ;
#2946=ORIENTED_EDGE ( 'NONE', *, *, #6096, .F. ) ;
#2952=DIRECTION ( 'NONE',  ( -1.000000000000000000, 0.000000000000000000, 0.000000000000000000 ) ) ;
#2954=AXIS2_PLACEMENT_3D ( 'NONE', #15966, #309, #26187 ) ;
#2960=CARTESIAN_POINT ( 'NONE',  ( 5.887530252753766291, -5.676096663009846388, 6.185189124321802012 ) ) ;
#2965=CARTESIAN_POINT ( 'NONE',  ( -6.237550801365593145, 1.088641768524161613, 3.675193018007247403 ) ) ;
#2966=CARTESIAN_POINT ( 'NONE',  ( -2.500050802731187627, -1.549418761218565255, 2.853674364686380471 ) ) ;
#2970=CIRCLE ( 'NONE', #17354, 3.000000000000000444 ) ;
#2972=ORIENTED_EDGE ( 'NONE', *, *, #12144, .T. ) ;
#2979=ORIENTED_EDGE ( 'NONE', *, *, #3895, .T. ) ;
#2980=CARTESIAN_POINT ( 'NONE',  ( -1.773875666770781789, -0.3178988483021056854, 3.024605502323848949 ) ) ;
#2981=CARTESIAN_POINT ( 'NONE',  ( -2.438362943428902252, 0.3722612527041059827, 3.133914954463516533 ) ) ;
#2991=DIRECTION ( 'NONE',  ( 0.000000000000000000, 0.5877852522924689183, 0.8090169943749504489 ) ) ;
#2994=DIRECTION ( 'NONE',  ( 0.000000000000000000, -0.8191520442889951292, 0.5735764363510413855 ) ) ;
#3000=CARTESIAN_POINT ( 'NONE',  ( -4.312550801365593323, -3.675193018007246071, 1.088641768524163167 ) ) ;
#3002=CARTESIAN_POINT ( 'NONE',  ( -8.300050799999999285, 2.983565686104819648, 0.3135853898029609677 ) ) ;
#3004=DIRECTION ( 'NONE',  ( -1.000000000000000000, -0.000000000000000000, -0.000000000000000000 ) ) ;
#3016=VERTEX_POINT ( 'NONE', #12932 ) ;
#3017=CARTESIAN_POINT ( 'NONE',  ( 3.499999999999999556, 0.005878491403456947983, 7.047692205288324629 ) ) ;
#3022=CARTESIAN_POINT ( 'NONE',  ( -5.062550801365593323, -3.521866450007987037, -0.3701630799359323931 ) ) ;
#3030=CARTESIAN_POINT ( 'NONE',  ( 3.499999999999999556, 7.008469740302802897, 0.7425307242148009301 ) ) ;
#3036=EDGE_CURVE ( 'NONE', #2248, #18257, #22962, .T. ) ;
#3040=ORIENTED_EDGE ( 'NONE', *, *, #19183, .F. ) ;
#3051=LINE ( 'NONE', #18717, #26840 ) ;
#3060=CARTESIAN_POINT ( 'NONE',  ( 7.249760686538667009, -4.973063321323927255, 7.199384779417104419 ) ) ;
#3067=CARTESIAN_POINT ( 'NONE',  ( 0.000000000000000000, -2.652816298622381996, -5.657964889053610058 ) ) ;
#3074=CARTESIAN_POINT ( 'NONE',  ( 0.000000000000000000, 2.871924938129881699, 6.435996203144517480 ) ) ;
#3077=CARTESIAN_POINT ( 'NONE',  ( 5.612718622971679672, -7.786491723834097378, -2.621884781721345092 ) ) ;
#3082=CARTESIAN_POINT ( 'NONE',  ( -4.900050799999999818, -0.3135853898029607456, 2.983565686104819648 ) ) ;
#3091=DIRECTION ( 'NONE',  ( 0.000000000000000000, 0.4226182617407045483, -0.9063077870366476052 ) ) ;
#3095=CARTESIAN_POINT ( 'NONE',  ( -5.700050800000000528, -0.3135853898029607456, 2.983565686104819648 ) ) ;
#3096=DIRECTION ( 'NONE',  ( -1.000000000000000000, 0.000000000000000000, -0.000000000000000000 ) ) ;
#3098=LINE ( 'NONE', #8083, #20841 ) ;
#3103=EDGE_CURVE ( 'NONE', #22148, #1082, #26678, .T. ) ;
#3108=CARTESIAN_POINT ( 'NONE',  ( 0.000000000000000000, -7.009698679648292519, 3.730838147389666126 ) ) ;
#3110=LINE ( 'NONE', #13265, #4434 ) ;
#3113=CARTESIAN_POINT ( 'NONE',  ( -2.350050802731187272, -2.983565686104819648, -0.3135853898029605791 ) ) ;
#3117=ADVANCED_FACE ( 'NONE', ( #2051 ), #19759, .T. ) ;
#3118=EDGE_LOOP ( 'NONE', ( #21825, #14725, #14773, #24968 ) ) ;
#3132=CARTESIAN_POINT ( 'NONE',  ( 4.749760686538667009, 7.530955069117551304, -2.741043480754851380 ) ) ;
#3137=PLANE ( 'NONE',  #23723 ) ;
#3142=CARTESIAN_POINT ( 'NONE',  ( -7.600050802731187716, 3.113457007523260156, -0.9222479816126439855 ) ) ;
#3143=EDGE_LOOP ( 'NONE', ( #17560, #16753, #924 ) ) ;
#3144=CARTESIAN_POINT ( 'NONE',  ( -3.254531657079157370, -1.545410377633946286, 2.846291840500174697 ) ) ;
#3146=CARTESIAN_POINT ( 'NONE',  ( -5.050050800000001061, 2.853674364686379583, 1.549418761218565921 ) ) ;
#3149=EDGE_CURVE ( 'NONE', #24117, #11175, #5342, .T. ) ;
#3154=EDGE_CURVE ( 'NONE', #28488, #25776, #7467, .T. ) ;
#3165=CARTESIAN_POINT ( 'NONE',  ( -4.212550801365593678, -3.368539882008727115, -1.828967928396028064 ) ) ;
#3174=CARTESIAN_POINT ( 'NONE',  ( 7.249760686538667009, 0.000000000000000000, 0.000000000000000000 ) ) ;
#3185=CARTESIAN_POINT ( 'NONE',  ( 0.000000000000000000, 4.137773741518377513, 5.705158055754806945 ) ) ;
#3188=CIRCLE ( 'NONE', #19208, 2.999999999999999556 ) ;
#3189=ORIENTED_EDGE ( 'NONE', *, *, #12286, .F. ) ;
#3195=CARTESIAN_POINT ( 'NONE',  ( -3.862550801365593145, 3.521866450007987037, 0.3701630799359328372 ) ) ;
#3199=CARTESIAN_POINT ( 'NONE',  ( 5.377543748152550762, 7.530955069117551304, -2.741043480754851380 ) ) ;
#3208=PLANE ( 'NONE',  #20521 ) ;
#3209=EDGE_CURVE ( 'NONE', #21075, #12143, #28617, .T. ) ;
#3224=CARTESIAN_POINT ( 'NONE',  ( 6.880159790065804692, 8.451885315426457268, -2.190520500543400306 ) ) ;
#3228=CARTESIAN_POINT ( 'NONE',  ( -4.750050800000000351, -3.113457007523259268, 0.9222479816126455399 ) ) ;
#3230=DIRECTION ( 'NONE',  ( 0.000000000000000000, 0.000000000000000000, 1.000000000000000000 ) ) ;
#3240=ORIENTED_EDGE ( 'NONE', *, *, #4835, .T. ) ;
#3251=CARTESIAN_POINT ( 'NONE',  ( -6.557304906975410574, 1.062355717592095683, 2.999999999999999112 ) ) ;
#3253=CARTESIAN_POINT ( 'NONE',  ( 5.489343958331425632, 7.664144799260948382, 2.678936089601470005 ) ) ;
#3261=DIRECTION ( 'NONE',  ( 0.000000000000000000, -0.9659258262890710878, 0.2588190451025100258 ) ) ;
#3267=EDGE_LOOP ( 'NONE', ( #8390, #29992, #6022, #11558 ) ) ;
#3271=ORIENTED_EDGE ( 'NONE', *, *, #25920, .F. ) ;
#3284=CARTESIAN_POINT ( 'NONE',  ( 7.064632816082965228, -0.7071067811865714425, 8.721381771256201176 ) ) ;
#3285=VECTOR ( 'NONE', #13356, 1000.000000000000114 ) ;
#3287=LINE ( 'NONE', #2627, #15095 ) ;
#3290=ORIENTED_EDGE ( 'NONE', *, *, #17803, .T. ) ;
#3292=DIRECTION ( 'NONE',  ( 0.000000000000000000, 0.5735764363510439390, 0.8191520442889933529 ) ) ;
#3295=CARTESIAN_POINT ( 'NONE',  ( -6.700050802731188249, 2.853674364686379583, 1.549418761218565921 ) ) ;
#3296=ADVANCED_FACE ( 'NONE', ( #23415 ), #22923, .F. ) ;
#3298=DIRECTION ( 'NONE',  ( 1.000000000000000000, 0.000000000000000000, -0.000000000000000000 ) ) ;
#3300=CARTESIAN_POINT ( 'NONE',  ( -2.512942406915326110, -5.022711880624455567E-15, 2.999999999999999556 ) ) ;
#3304=CARTESIAN_POINT ( 'NONE',  ( -2.462550801365593678, 0.3701630799359330593, -3.521866450007987037 ) ) ;
#3306=CARTESIAN_POINT ( 'NONE',  ( -2.654531657079157281, 2.846291840500173365, 1.545410377633946952 ) ) ;
#3309=DIRECTION ( 'NONE',  ( 0.000000000000000000, 0.000000000000000000, 1.000000000000000000 ) ) ;
#3311=VERTEX_POINT ( 'NONE', #29373 ) ;
#3323=AXIS2_PLACEMENT_3D ( 'NONE', #6371, #7485, #12522 ) ;
#3329=FACE_OUTER_BOUND ( 'NONE', #23209, .T. ) ;
#3331=CARTESIAN_POINT ( 'NONE',  ( 0.000000000000000000, 0.000000000000000000, -3.000000000000000444 ) ) ;
#3332=ORIENTED_EDGE ( 'NONE', *, *, #25584, .T. ) ;
#3340=ORIENTED_EDGE ( 'NONE', *, *, #13637, .T. ) ;
#3343=DIRECTION ( 'NONE',  ( 0.000000000000000000, 0.000000000000000000, 1.000000000000000000 ) ) ;
#3344=VECTOR ( 'NONE', #13030, 1000.000000000000114 ) ;
#3354=CARTESIAN_POINT ( 'NONE',  ( -4.087550801365593678, 2.752080473201636845, -2.228590825266444142 ) ) ;
#3362=CIRCLE ( 'NONE', #6564, 2.999999999999999556 ) ;
#3371=ORIENTED_EDGE ( 'NONE', *, *, #15819, .F. ) ;
#3373=CARTESIAN_POINT ( 'NONE',  ( -4.862550801365594033, 0.3701630799359330593, -3.521866450007987037 ) ) ;
#3379=CARTESIAN_POINT ( 'NONE',  ( -7.387550801365593500, 0.3701630799359330593, -3.521866450007987037 ) ) ;
#3389=DIRECTION ( 'NONE',  ( 0.000000000000000000, -0.7071067811865380248, -0.7071067811865570096 ) ) ;
#3391=AXIS2_PLACEMENT_3D ( 'NONE', #8493, #28893, #8667 ) ;
#3396=PLANE ( 'NONE',  #6018 ) ;
#3397=AXIS2_PLACEMENT_3D ( 'NONE', #32560, #24358, #27038 ) ;
#3403=CARTESIAN_POINT ( 'NONE',  ( 5.489343806296449024, 7.976812024616046770, -1.512045527216122176 ) ) ;
#3407=AXIS2_PLACEMENT_3D ( 'NONE', #10087, #22473, #14428 ) ;
#3408=CARTESIAN_POINT ( 'NONE',  ( -4.906376978575949011, -0.1572233378491262878, 2.999999999999999556 ) ) ;
#3413=VERTEX_POINT ( 'NONE', #9132 ) ;
#3419=CARTESIAN_POINT ( 'NONE',  ( -6.050050802731187893, 2.331437884370912705, -1.887961173149511618 ) ) ;
#3425=DIRECTION ( 'NONE',  ( -1.000000000000000000, 0.000000000000000000, 0.000000000000000000 ) ) ;
#3429=CARTESIAN_POINT ( 'NONE',  ( 6.880159540721329847, 3.624895993596869648, 7.943102264535267132 ) ) ;
#3448=ORIENTED_EDGE ( 'NONE', *, *, #11508, .T. ) ;
#3471=CARTESIAN_POINT ( 'NONE',  ( -4.000050800000000351, -2.331437884370912705, 1.887961173149512062 ) ) ;
#3474=CARTESIAN_POINT ( 'NONE',  ( 1.750000000000000222, -5.522688772756442432, 6.461416928141223259 ) ) ;
#3477=CARTESIAN_POINT ( 'NONE',  ( 1.750000000000000222, -7.851777359433977921, -3.255701506262514311 ) ) ;
#3482=CARTESIAN_POINT ( 'NONE',  ( -3.862550801365593145, 3.521866450007987037, 0.3701630799359328372 ) ) ;
#3485=CARTESIAN_POINT ( 'NONE',  ( -5.500050800000000351, -2.983565686104819648, -0.3135853898029605791 ) ) ;
#3492=ORIENTED_EDGE ( 'NONE', *, *, #26925, .F. ) ;
#3498=CARTESIAN_POINT ( 'NONE',  ( 3.499999999999999556, 7.008469740302810891, 2.257469275785292329 ) ) ;
#3499=CARTESIAN_POINT ( 'NONE',  ( 0.000000000000000000, -8.497168642645966941, 0.2193742428684632428 ) ) ;
#3502=EDGE_CURVE ( 'NONE', #20265, #26968, #20184, .T. ) ;
#3506=DIRECTION ( 'NONE',  ( 1.000000000000000000, 0.000000000000000000, 0.000000000000000000 ) ) ;
#3508=ORIENTED_EDGE ( 'NONE', *, *, #24722, .F. ) ;
#3509=CARTESIAN_POINT ( 'NONE',  ( -2.312550801365593767, 3.675193018007247403, -1.088641768524161391 ) ) ;
#3515=DIRECTION ( 'NONE',  ( 0.000000000000000000, 0.000000000000000000, 1.000000000000000000 ) ) ;
#3519=EDGE_CURVE ( 'NONE', #18044, #23643, #28235, .T. ) ;
#3520=LINE ( 'NONE', #3826, #10841 ) ;
#3523=CARTESIAN_POINT ( 'NONE',  ( -3.487550801365593589, -2.228590825266444586, -2.752080473201636401 ) ) ;
#3532=CYLINDRICAL_SURFACE ( 'NONE', #15744, 3.000000000000000444 ) ;
#3535=ORIENTED_EDGE ( 'NONE', *, *, #11689, .F. ) ;
#3536=ORIENTED_EDGE ( 'NONE', *, *, #10798, .F. ) ;
#3538=CARTESIAN_POINT ( 'NONE',  ( -3.512550801365593944, -3.675193018007245627, 1.088641768524163389 ) ) ;
#3543=CARTESIAN_POINT ( 'NONE',  ( -5.687550801365593323, 2.752080473201636845, -2.228590825266444142 ) ) ;
#3548=VERTEX_POINT ( 'NONE', #2125 ) ;
#3557=CARTESIAN_POINT ( 'NONE',  ( -7.037550801365593856, 1.088641768524161613, 3.675193018007247403 ) ) ;
#3559=CARTESIAN_POINT ( 'NONE',  ( 6.524595126109737464, 8.397268106035244983, -2.112519041817527032 ) ) ;
#3562=EDGE_CURVE ( 'NONE', #29777, #15458, #20850, .T. ) ;
#3565=CYLINDRICAL_SURFACE ( 'NONE', #15539, 2.999999999999999112 ) ;
#3568=ADVANCED_FACE ( 'NONE', ( #28842 ), #8132, .T. ) ;
#3578=CARTESIAN_POINT ( 'NONE',  ( 3.499999999999999556, -6.700937042937042065, -2.183447440113257976 ) ) ;
#3587=DIRECTION ( 'NONE',  ( 0.000000000000000000, 0.000000000000000000, 1.000000000000000000 ) ) ;
#3590=ADVANCED_FACE ( 'NONE', ( #5943 ), #10801, .F. ) ;
#3599=EDGE_CURVE ( 'NONE', #442, #21233, #21387, .T. ) ;
#3605=VERTEX_POINT ( 'NONE', #10630 ) ;
#3612=DIRECTION ( 'NONE',  ( 1.000000000000000000, 0.000000000000000000, -0.000000000000000000 ) ) ;
#3621=CARTESIAN_POINT ( 'NONE',  ( 7.249760686538667009, 2.741043480754926875, 7.530955069117522882 ) ) ;
#3626=CARTESIAN_POINT ( 'NONE',  ( -2.912550801365593411, 1.088641768524161613, 3.675193018007247403 ) ) ;
#3627=ORIENTED_EDGE ( 'NONE', *, *, #20596, .F. ) ;
#3628=CARTESIAN_POINT ( 'NONE',  ( -6.500050800000000351, -0.3135853898029607456, 2.983565686104819648 ) ) ;
#3631=EDGE_CURVE ( 'NONE', #112, #31964, #6366, .T. ) ;
#3632=CARTESIAN_POINT ( 'NONE',  ( 3.499999999999999556, 7.008469740302802897, 0.7425307242148009301 ) ) ;
#3651=CARTESIAN_POINT ( 'NONE',  ( 4.749760686538667009, 6.940565734314597002, 4.007137495034836405 ) ) ;
#3656=VERTEX_POINT ( 'NONE', #10073 ) ;
#3657=CARTESIAN_POINT ( 'NONE',  ( 3.499999999999999556, -7.009698679648292519, 0.7308381473896670144 ) ) ;
#3660=EDGE_LOOP ( 'NONE', ( #1413, #2946, #17487, #27296 ) ) ;
#3663=FACE_OUTER_BOUND ( 'NONE', #9917, .T. ) ;
#3664=CARTESIAN_POINT ( 'NONE',  ( -2.102220961135812693, 1.255248584792989064, 3.273767578062598105 ) ) ;
#3665=CARTESIAN_POINT ( 'NONE',  ( -4.337550801365594566, -3.368539882008727115, -1.828967928396027842 ) ) ;
#3669=ORIENTED_EDGE ( 'NONE', *, *, #15669, .F. ) ;
#3671=ADVANCED_FACE ( 'NONE', ( #30984 ), #2739, .F. ) ;
#3680=VERTEX_POINT ( 'NONE', #12742 ) ;
#3681=CARTESIAN_POINT ( 'NONE',  ( -8.000050800000000351, 0.000000000000000000, -3.000000000000000444 ) ) ;
#3682=CARTESIAN_POINT ( 'NONE',  ( -5.112550801365594033, -3.675193018007245627, 1.088641768524163389 ) ) ;
#3688=DIRECTION ( 'NONE',  ( -1.000000000000000000, 0.000000000000000000, -0.000000000000000000 ) ) ;
#3690=CARTESIAN_POINT ( 'NONE',  ( -6.137550801365595277, -1.828967928396026510, 3.368539882008728004 ) ) ;
#3695=ORIENTED_EDGE ( 'NONE', *, *, #24874, .T. ) ;
#3711=ORIENTED_EDGE ( 'NONE', *, *, #7202, .T. ) ;
#3713=FACE_OUTER_BOUND ( 'NONE', #1256, .T. ) ;
#3721=FACE_OUTER_BOUND ( 'NONE', #31944, .T. ) ;
#3736=CARTESIAN_POINT ( 'NONE',  ( -8.000050800000000351, 0.000000000000000000, 0.000000000000000000 ) ) ;
#3738=ORIENTED_EDGE ( 'NONE', *, *, #4844, .F. ) ;
#3740=ADVANCED_FACE ( 'NONE', ( #2422 ), #4914, .F. ) ;
#3743=DIRECTION ( 'NONE',  ( 1.000000000000000000, 0.000000000000000000, 0.000000000000000000 ) ) ;
#3748=AXIS2_PLACEMENT_3D ( 'NONE', #30855, #7300, #5256 ) ;
#3760=CARTESIAN_POINT ( 'NONE',  ( 6.530491627857222703, -7.903708701126667791, -3.540416224243748466 ) ) ;
#3762=ORIENTED_EDGE ( 'NONE', *, *, #8415, .T. ) ;
#3765=CARTESIAN_POINT ( 'NONE',  ( 7.249760686538667009, 0.8180878109961843281, 8.711672189281429723 ) ) ;
#3772=EDGE_CURVE ( 'NONE', #31510, #10995, #29942, .T. ) ;
#3775=CARTESIAN_POINT ( 'NONE',  ( 5.489321606599601111, 7.593050043411109229, 2.874206582856435599 ) ) ;
#3781=CARTESIAN_POINT ( 'NONE',  ( -7.400050802731187538, 0.9222479816126443186, 3.113457007523260156 ) ) ;
#3783=CARTESIAN_POINT ( 'NONE',  ( -5.150050800000000706, 3.113457007523260156, -0.9222479816126439855 ) ) ;
#3784=CIRCLE ( 'NONE', #9102, 2.999999999999999112 ) ;
#3786=PLANE ( 'NONE',  #19329 ) ;
#3789=CARTESIAN_POINT ( 'NONE',  ( -7.050050800000001061, -2.853674364686378695, -1.549418761218566809 ) ) ;
#3798=AXIS2_PLACEMENT_3D ( 'NONE', #32907, #33053, #17847 ) ;
#3804=ORIENTED_EDGE ( 'NONE', *, *, #8813, .F. ) ;
#3806=DIRECTION ( 'NONE',  ( 0.000000000000000000, 0.000000000000000000, 1.000000000000000000 ) ) ;
#3811=VERTEX_POINT ( 'NONE', #16400 ) ;
#3812=CARTESIAN_POINT ( 'NONE',  ( -2.862550801365593145, -0.3701630799359326152, 3.521866450007987037 ) ) ;
#3813=FACE_OUTER_BOUND ( 'NONE', #19385, .T. ) ;
#3821=VECTOR ( 'NONE', #3298, 1000.000000000000000 ) ;
#3824=ORIENTED_EDGE ( 'NONE', *, *, #10565, .F. ) ;
#3826=CARTESIAN_POINT ( 'NONE',  ( -2.093800801365593323, -0.3135853898029608011, 2.983565686104819648 ) ) ;
#3827=( BOUNDED_CURVE ( )  B_SPLINE_CURVE ( 2, ( #17173, #12009, #4498 ),
 .UNSPECIFIED., .F., .F. ) 
 B_SPLINE_CURVE_WITH_KNOTS ( ( 3, 3 ),
 ( 0.9353822619934377691, 0.9375000000000000000 ),
 .UNSPECIFIED. ) 
 CURVE ( )  GEOMETRIC_REPRESENTATION_ITEM ( )  RATIONAL_B_SPLINE_CURVE ( ( 0.9821626249036861100, 0.9896829947469995004, 1.000000000000000000 ) ) 
 REPRESENTATION_ITEM ( '' )  );
#3828=CARTESIAN_POINT ( 'NONE',  ( -2.010643812441442968, 0.9556990460818173272, 3.226324136115746644 ) ) ;
#3831=CARTESIAN_POINT ( 'NONE',  ( -2.637550801365593056, -1.088641768524163611, -3.675193018007245627 ) ) ;
#3839=EDGE_LOOP ( 'NONE', ( #5518, #25266, #5761 ) ) ;
#3843=CYLINDRICAL_SURFACE ( 'NONE', #20861, 8.500000000000000000 ) ;
#3850=CARTESIAN_POINT ( 'NONE',  ( 5.612974441954676763, 6.163896661468974969, 5.432722698947179296 ) ) ;
#3851=CARTESIAN_POINT ( 'NONE',  ( -5.162550801365593856, -2.752080473201636845, 2.228590825266444586 ) ) ;
#3852=AXIS2_PLACEMENT_3D ( 'NONE', #13296, #5950, #31532 ) ;
#3855=CARTESIAN_POINT ( 'NONE',  ( 6.037141869538511507, 3.843044125430171931, -7.552970526864650758 ) ) ;
#3857=CARTESIAN_POINT ( 'NONE',  ( -5.837550801365594566, -1.088641768524163389, -3.675193018007246071 ) ) ;
#3858=AXIS2_PLACEMENT_3D ( 'NONE', #12684, #2863, #23236 ) ;
#3861=ADVANCED_FACE ( 'NONE', ( #13877 ), #15912, .F. ) ;
#3862=ORIENTED_EDGE ( 'NONE', *, *, #10983, .F. ) ;
#3865=EDGE_CURVE ( 'NONE', #10650, #7898, #26029, .T. ) ;
#3869=CARTESIAN_POINT ( 'NONE',  ( -6.562942409646512765, -8.831141768130910875E-16, 2.999999999999999556 ) ) ;
#3872=LINE ( 'NONE', #21901, #18869 ) ;
#3873=VECTOR ( 'NONE', #29531, 1000.000000000000000 ) ;
#3874=CIRCLE ( 'NONE', #23081, 8.750000000000000000 ) ;
#3876=CARTESIAN_POINT ( 'NONE',  ( -3.587550801365593678, -3.521866450007987037, -0.3701630799359323931 ) ) ;
#3878=EDGE_LOOP ( 'NONE', ( #31123, #20396, #8363 ) ) ;
#3883=CARTESIAN_POINT ( 'NONE',  ( 7.249760686538667009, 8.466096581343512284, -2.210816291636124475 ) ) ;
#3885=FACE_OUTER_BOUND ( 'NONE', #29669, .T. ) ;
#3886=CARTESIAN_POINT ( 'NONE',  ( 7.249760686538667009, -7.906491560603691404, 3.748318449932265484 ) ) ;
#3893=ORIENTED_EDGE ( 'NONE', *, *, #5307, .F. ) ;
#3895=EDGE_CURVE ( 'NONE', #15207, #30146, #28332, .T. ) ;
#3897=CARTESIAN_POINT ( 'NONE',  ( 3.499999999999999556, -2.417132211460119251, 8.149077976821791580 ) ) ;
#3908=VERTEX_POINT ( 'NONE', #31467 ) ;
#3909=ADVANCED_FACE ( 'NONE', ( #8546 ), #3565, .T. ) ;
#3910=CARTESIAN_POINT ( 'NONE',  ( -4.950050802731188249, -0.3135853898029607456, 2.983565686104819648 ) ) ;
#3919=DIRECTION ( 'NONE',  ( -1.000000000000000000, -0.000000000000000000, -0.000000000000000000 ) ) ;
#3923=ADVANCED_FACE ( 'NONE', ( #3713 ), #11408, .T. ) ;
#3926=AXIS2_PLACEMENT_3D ( 'NONE', #14174, #9650, #27396 ) ;
#3927=CARTESIAN_POINT ( 'NONE',  ( 0.000000000000000000, -7.009698679648292519, 0.7308381473896670144 ) ) ;
#3934=ORIENTED_EDGE ( 'NONE', *, *, #13642, .T. ) ;
#3941=EDGE_CURVE ( 'NONE', #10995, #16442, #14220, .T. ) ;
#3951=VECTOR ( 'NONE', #6880, 1000.000000000000000 ) ;
#3956=AXIS2_PLACEMENT_3D ( 'NONE', #3927, #6397, #1414 ) ;
#3961=VECTOR ( 'NONE', #18221, 1000.000000000000000 ) ;
#3965=CARTESIAN_POINT ( 'NONE',  ( -5.850050802731187716, 1.887961173149511618, 2.331437884370912705 ) ) ;
#3966=EDGE_LOOP ( 'NONE', ( #28334, #20833, #28132 ) ) ;
#3967=CARTESIAN_POINT ( 'NONE',  ( -7.600050800000000883, 2.331437884370912705, -1.887961173149511618 ) ) ;
#3974=ORIENTED_EDGE ( 'NONE', *, *, #15179, .F. ) ;
#3977=CARTESIAN_POINT ( 'NONE',  ( 6.524595623740805372, 6.028129343649612615, 6.215987993068464945 ) ) ;
#3981=EDGE_CURVE ( 'NONE', #19878, #30724, #3784, .T. ) ;
#3982=CARTESIAN_POINT ( 'NONE',  ( -5.950050800000000528, 3.113457007523260156, -0.9222479816126439855 ) ) ;
#3991=CARTESIAN_POINT ( 'NONE',  ( 5.885541736258998569, -7.752826540560528557, 3.216848386728037745 ) ) ;
#3994=CARTESIAN_POINT ( 'NONE',  ( 5.489321289187128805, -8.118169347437836691, -0.1038943573681802152 ) ) ;
#3997=CARTESIAN_POINT ( 'NONE',  ( 5.377543748152549874, -2.741043480754977946, 7.530955069117504230 ) ) ;
#3999=LINE ( 'NONE', #16676, #11290 ) ;
#4000=CARTESIAN_POINT ( 'NONE',  ( 0.000000000000000000, 0.6700234925292696264, 8.473551116235677583 ) ) ;
#4002=DIRECTION ( 'NONE',  ( 0.000000000000000000, 0.000000000000000000, 1.000000000000000000 ) ) ;
#4007=FACE_OUTER_BOUND ( 'NONE', #21164, .T. ) ;
#4009=VERTEX_POINT ( 'NONE', #11559 ) ;
#4022=FACE_OUTER_BOUND ( 'NONE', #21715, .T. ) ;
#4026=VERTEX_POINT ( 'NONE', #22106 ) ;
#4027=CARTESIAN_POINT ( 'NONE',  ( -6.637550801365594388, -1.088641768524163389, -3.675193018007246071 ) ) ;
#4034=DIRECTION ( 'NONE',  ( 0.000000000000000000, -0.9659258262890701996, 0.2588190451025139671 ) ) ;
#4035=DIRECTION ( 'NONE',  ( -1.000000000000000000, -0.000000000000000000, -0.000000000000000000 ) ) ;
#4047=LINE ( 'NONE', #18934, #11332 ) ;
#4050=CARTESIAN_POINT ( 'NONE',  ( 5.885541615502094537, -1.821712961073290726, -8.193643496140870397 ) ) ;
#4058=VERTEX_POINT ( 'NONE', #14065 ) ;
#4060=EDGE_CURVE ( 'NONE', #24044, #21075, #1137, .T. ) ;
#4071=CARTESIAN_POINT ( 'NONE',  ( -4.700050802731189137, -2.853674364686378695, -1.549418761218566809 ) ) ;
#4073=B_SPLINE_CURVE_WITH_KNOTS ( 'NONE', 3,
 ( #22961, #5257, #25642, #2757, #26318, #21621, #9048, #3429, #16578, #26790 ),
 .UNSPECIFIED., .F., .F.,
 ( 4, 2, 2, 2, 4 ),
 ( 2.740849916261192663E-07, 0.0005478761651001754851, 0.001095478245208724843, 0.001643080325317274092, 0.002190682405425823341 ),
 .UNSPECIFIED. ) ;
#4074=LINE ( 'NONE', #31671, #26259 ) ;
#4075=DIRECTION ( 'NONE',  ( -1.000000000000000000, -0.000000000000000000, -0.000000000000000000 ) ) ;
#4077=DIRECTION ( 'NONE',  ( 1.000000000000000000, 0.000000000000000000, 0.000000000000000000 ) ) ;
#4079=CARTESIAN_POINT ( 'NONE',  ( -6.500050800000000351, -0.3135853898029607456, 2.983565686104819648 ) ) ;
#4088=EDGE_CURVE ( 'NONE', #4337, #23656, #26727, .T. ) ;
#4089=ORIENTED_EDGE ( 'NONE', *, *, #13721, .T. ) ;
#4092=DIRECTION ( 'NONE',  ( -1.000000000000000000, -0.000000000000000000, 0.000000000000000000 ) ) ;
#4093=VERTEX_POINT ( 'NONE', #24924 ) ;
#4097=ORIENTED_EDGE ( 'NONE', *, *, #13527, .F. ) ;
#4104=CARTESIAN_POINT ( 'NONE',  ( 7.064632879756603145, 0.8180878109961848832, 8.711672189281427947 ) ) ;
#4105=CARTESIAN_POINT ( 'NONE',  ( 5.377543748152549874, 5.151476664237477188, 6.139290821770273077 ) ) ;
#4108=DIRECTION ( 'NONE',  ( 0.000000000000000000, 0.000000000000000000, 1.000000000000000000 ) ) ;
#4109=CARTESIAN_POINT ( 'NONE',  ( -10.00000000000000000, 0.000000000000000000, 0.000000000000000000 ) ) ;
#4112=CARTESIAN_POINT ( 'NONE',  ( 3.499999999999999556, 0.000000000000000000, 0.000000000000000000 ) ) ;
#4114=LINE ( 'NONE', #16635, #15580 ) ;
#4115=CARTESIAN_POINT ( 'NONE',  ( -5.500050802731188071, -2.853674364686378695, -1.549418761218566809 ) ) ;
#4117=CARTESIAN_POINT ( 'NONE',  ( -7.887550801365593500, 2.228590825266444142, 2.752080473201636845 ) ) ;
#4120=CARTESIAN_POINT ( 'NONE',  ( -5.650050802731187538, -2.331437884370912705, 1.887961173149512062 ) ) ;
#4123=DIRECTION ( 'NONE',  ( 0.000000000000000000, 0.000000000000000000, 1.000000000000000000 ) ) ;
#4139=DIRECTION ( 'NONE',  ( 0.000000000000000000, 0.000000000000000000, -1.000000000000000000 ) ) ;
#4141=CARTESIAN_POINT ( 'NONE',  ( 7.249760686538667009, 5.151476664237558900, -6.139290821770204687 ) ) ;
#4147=DIRECTION ( 'NONE',  ( -1.000000000000000000, -0.000000000000000000, -0.000000000000000000 ) ) ;
#4151=CARTESIAN_POINT ( 'NONE',  ( -2.900050802731187538, 1.549418761218566143, -2.853674364686379583 ) ) ;
#4152=VERTEX_POINT ( 'NONE', #30139 ) ;
#4155=FACE_OUTER_BOUND ( 'NONE', #3966, .T. ) ;
#4157=DIRECTION ( 'NONE',  ( 0.000000000000000000, 0.000000000000000000, 1.000000000000000000 ) ) ;
#4158=CARTESIAN_POINT ( 'NONE',  ( -5.312942406915326821, -3.366872799099910998E-15, -3.000000000000000000 ) ) ;
#4161=CYLINDRICAL_SURFACE ( 'NONE', #18297, 6.248999999999999666 ) ;
#4165=LINE ( 'NONE', #14331, #13338 ) ;
#4166=CARTESIAN_POINT ( 'NONE',  ( 6.356382477965132338, 6.209963745178092687, -5.959271875177088340 ) ) ;
#4174=CARTESIAN_POINT ( 'NONE',  ( -2.537550801365592967, 1.828967928396027176, -3.368539882008727115 ) ) ;
#4175=CARTESIAN_POINT ( 'NONE',  ( 4.749760686538667009, -2.789499415801756586E-14, 8.014274990069656823 ) ) ;
#4177=DIRECTION ( 'NONE',  ( 0.000000000000000000, 0.000000000000000000, 1.000000000000000000 ) ) ;
#4182=CARTESIAN_POINT ( 'NONE',  ( 3.499999999999999556, 4.137773741518454784, -5.705158055754753654 ) ) ;
#4191=CARTESIAN_POINT ( 'NONE',  ( -3.837550801365593234, 1.088641768524161613, 3.675193018007247403 ) ) ;
#4205=B_SPLINE_CURVE_WITH_KNOTS ( 'NONE', 3,
 ( #10271, #20491, #4934, #2263, #17800, #30704, #17968, #7777, #27503, #7267 ),
 .UNSPECIFIED., .F., .F.,
 ( 4, 2, 2, 2, 4 ),
 ( 1.968338519010778477E-07, 0.0005467930078056964724, 0.001093389181759491739, 0.001639985355713287222, 0.002186581529667082704 ),
 .UNSPECIFIED. ) ;
#4209=CARTESIAN_POINT ( 'NONE',  ( 3.499999999999999556, -6.700937042937042065, 0.8165525598867410251 ) ) ;
#4224=ADVANCED_FACE ( 'NONE', ( #14560 ), #12062, .T. ) ;
#4226=FACE_OUTER_BOUND ( 'NONE', #5838, .T. ) ;
#4228=( BOUNDED_CURVE ( )  B_SPLINE_CURVE ( 2, ( #3869, #2024, #24562, #4362, #22091, #12196, #16733, #11882, #19423, #9514, #1686 ),
 .UNSPECIFIED., .F., .F. ) 
 B_SPLINE_CURVE_WITH_KNOTS ( ( 3, 2, 2, 2, 2, 3 ),
 ( 0.1853822619934377414, 0.1875000000000000000, 0.2031250000000000000, 0.2187500000000000000, 0.2343750000000000000, 0.2478822619934377414 ),
 .UNSPECIFIED. ) 
 CURVE ( )  GEOMETRIC_REPRESENTATION_ITEM ( )  RATIONAL_B_SPLINE_CURVE ( ( 0.9821626249036861100, 0.9896829947469993893, 1.000000000000000000, 0.9238795325112867385, 1.000000000000000000, 0.9238795325112867385, 1.000000000000000000, 0.9238795325112867385, 1.000000000000000000, 0.9341965377642873491, 0.9821626249036861100 ) ) 
 REPRESENTATION_ITEM ( '' )  );
#4232=ORIENTED_EDGE ( 'NONE', *, *, #33046, .F. ) ;
#4236=CARTESIAN_POINT ( 'NONE',  ( 3.499999999999999556, 0.000000000000000000, 0.000000000000000000 ) ) ;
#4239=ORIENTED_EDGE ( 'NONE', *, *, #5401, .F. ) ;
#4246=CARTESIAN_POINT ( 'NONE',  ( 5.612974259723586989, -7.650268724902040240, -2.996912441296252005 ) ) ;
#4249=DIRECTION ( 'NONE',  ( -1.000000000000000000, -0.000000000000000000, -0.000000000000000000 ) ) ;
#4253=CARTESIAN_POINT ( 'NONE',  ( 5.377543748152548986, 1.391664247347228045, 7.892520144992438702 ) ) ;
#4255=CARTESIAN_POINT ( 'NONE',  ( -8.000050800000002127, 3.541248556864417196, 0.01107501445590582979 ) ) ;
#4262=DIRECTION ( 'NONE',  ( 0.000000000000000000, 0.000000000000000000, 1.000000000000000000 ) ) ;
#4263=FACE_OUTER_BOUND ( 'NONE', #2466, .T. ) ;
#4265=DIRECTION ( 'NONE',  ( -1.000000000000000000, 0.000000000000000000, 0.000000000000000000 ) ) ;
#4267=CARTESIAN_POINT ( 'NONE',  ( -5.550050802731187893, -2.983565686104819648, -0.3135853898029605791 ) ) ;
#4269=CARTESIAN_POINT ( 'NONE',  ( -2.750050800000000351, 3.113457007523260156, -0.9222479816126439855 ) ) ;
#4271=AXIS2_PLACEMENT_3D ( 'NONE', #7634, #20175, #18328 ) ;
#4273=CARTESIAN_POINT ( 'NONE',  ( -4.157304906975410219, 1.062355717592091686, 3.000000000000001332 ) ) ;
#4275=DIRECTION ( 'NONE',  ( -1.000000000000000000, 0.000000000000000000, 0.000000000000000000 ) ) ;
#4276=CARTESIAN_POINT ( 'NONE',  ( 7.249760686538667009, -7.199384779417084879, -4.973063321323951236 ) ) ;
#4288=CARTESIAN_POINT ( 'NONE',  ( 6.038144853276843804, -1.911563584435252539, 8.256557579931657287 ) ) ;
#4289=CARTESIAN_POINT ( 'NONE',  ( 3.499999999999999556, 6.704570150426983233, 2.172265885002680808 ) ) ;
#4299=CARTESIAN_POINT ( 'NONE',  ( 5.612973690782940395, -8.213905076232780544, -0.1996300861631225554 ) ) ;
#4302=CARTESIAN_POINT ( 'NONE',  ( -4.450050802731187360, 2.331437884370912705, -1.887961173149511618 ) ) ;
#4305=EDGE_CURVE ( 'NONE', #19445, #32003, #31565, .T. ) ;
#4307=ADVANCED_FACE ( 'NONE', ( #8209 ), #10871, .F. ) ;
#4308=AXIS2_PLACEMENT_3D ( 'NONE', #8304, #29029, #3292 ) ;
#4310=( BOUNDED_CURVE ( )  B_SPLINE_CURVE ( 2, ( #22550, #2336, #1532, #12516, #2500, #33074, #26947, #19246, #25216, #29445, #32926 ),
 .UNSPECIFIED., .F., .F. ) 
 B_SPLINE_CURVE_WITH_KNOTS ( ( 3, 2, 2, 2, 2, 3 ),
 ( 0.7478822619934377691, 0.7500000000000000000, 0.7656250000000000000, 0.7812500000000000000, 0.7968750000000000000, 0.8103822619934377691 ),
 .UNSPECIFIED. ) 
 CURVE ( )  GEOMETRIC_REPRESENTATION_ITEM ( )  RATIONAL_B_SPLINE_CURVE ( ( 0.9821626249036861100, 0.9896829947469995004, 1.000000000000000000, 0.9238795325112867385, 1.000000000000000000, 0.9238795325112867385, 1.000000000000000000, 0.9238795325112867385, 1.000000000000000000, 0.9341965377642872381, 0.9821626249036861100 ) ) 
 REPRESENTATION_ITEM ( '' )  );
#4314=VERTEX_POINT ( 'NONE', #2887 ) ;
#4315=FACE_OUTER_BOUND ( 'NONE', #11760, .T. ) ;
#4317=CARTESIAN_POINT ( 'NONE',  ( -7.504531657079157370, 2.975847129947406522, 0.3127741368606808403 ) ) ;
#4326=AXIS2_PLACEMENT_3D ( 'NONE', #21017, #28544, #16452 ) ;
#4337=VERTEX_POINT ( 'NONE', #13051 ) ;
#4338=CARTESIAN_POINT ( 'NONE',  ( -8.125050801365594211, 0.3135853898029611342, -2.983565686104819648 ) ) ;
#4339=CARTESIAN_POINT ( 'NONE',  ( -2.512550801365593056, -1.088641768524163611, -3.675193018007245627 ) ) ;
#4345=CARTESIAN_POINT ( 'NONE',  ( -3.387550801365593056, 0.3701630799359330593, -3.521866450007987037 ) ) ;
#4352=CARTESIAN_POINT ( 'NONE',  ( 6.530491712438077023, -7.168846788212658971, -4.859093986587931013 ) ) ;
#4355=VECTOR ( 'NONE', #22703, 1000.000000000000000 ) ;
#4356=DIRECTION ( 'NONE',  ( 0.000000000000000000, 0.000000000000000000, -1.000000000000000000 ) ) ;
#4362=CARTESIAN_POINT ( 'NONE',  ( -6.500050802731188959, -1.549418761218565255, 2.853674364686380471 ) ) ;
#4367=CARTESIAN_POINT ( 'NONE',  ( -2.437550801365593767, 3.675193018007247403, -1.088641768524161391 ) ) ;
#4372=AXIS2_PLACEMENT_3D ( 'NONE', #43, #27780, #30313 ) ;
#4387=EDGE_CURVE ( 'NONE', #4009, #12812, #6015, .T. ) ;
#4399=VERTEX_POINT ( 'NONE', #8845 ) ;
#4409=LINE ( 'NONE', #17277, #1697 ) ;
#4412=DIRECTION ( 'NONE',  ( 1.000000000000000000, 0.000000000000000000, -0.000000000000000000 ) ) ;
#4415=CIRCLE ( 'NONE', #8155, 8.750000000000000000 ) ;
#4419=AXIS2_PLACEMENT_3D ( 'NONE', #330, #10503, #18183 ) ;
#4421=CARTESIAN_POINT ( 'NONE',  ( 0.000000000000000000, 5.471841788314708133, 3.018103451449746899 ) ) ;
#4426=CIRCLE ( 'NONE', #13982, 8.500000000000000000 ) ;
#4428=FACE_OUTER_BOUND ( 'NONE', #9884, .T. ) ;
#4429=VECTOR ( 'NONE', #24258, 1000.000000000000114 ) ;
#4434=VECTOR ( 'NONE', #28813, 1000.000000000000114 ) ;
#4442=AXIS2_PLACEMENT_3D ( 'NONE', #7153, #32251, #9313 ) ;
#4457=PLANE ( 'NONE',  #28427 ) ;
#4458=CARTESIAN_POINT ( 'NONE',  ( -6.350050802731187716, -2.983565686104819648, -0.3135853898029605791 ) ) ;
#4462=CARTESIAN_POINT ( 'NONE',  ( -4.150050799999999818, 0.9222479816126443186, 3.113457007523260156 ) ) ;
#4465=CARTESIAN_POINT ( 'NONE',  ( 3.499999999999999556, -0.1221666339524086348, 6.247805719894683918 ) ) ;
#4467=ORIENTED_EDGE ( 'NONE', *, *, #21807, .F. ) ;
#4468=CARTESIAN_POINT ( 'NONE',  ( -2.156376981307136287, 0.1572233378491263989, -2.999999999999999556 ) ) ;
#4470=DIRECTION ( 'NONE',  ( 0.000000000000000000, -0.9510565162951502005, -0.3090169943749573878 ) ) ;
#4472=CARTESIAN_POINT ( 'NONE',  ( 6.037141879243262288, 5.783072176360644079, 6.194548269014904740 ) ) ;
#4474=EDGE_CURVE ( 'NONE', #9606, #16325, #7290, .T. ) ;
#4478=CIRCLE ( 'NONE', #5002, 8.750000000000000000 ) ;
#4481=DIRECTION ( 'NONE',  ( 0.000000000000000000, 0.000000000000000000, 1.000000000000000000 ) ) ;
#4487=FACE_OUTER_BOUND ( 'NONE', #14201, .T. ) ;
#4488=ORIENTED_EDGE ( 'NONE', *, *, #16769, .F. ) ;
#4491=DIRECTION ( 'NONE',  ( 0.000000000000000000, 0.000000000000000000, 1.000000000000000000 ) ) ;
#4497=CARTESIAN_POINT ( 'NONE',  ( 6.357668022120090079, -6.210015626210345197, -5.959864878090739282 ) ) ;
#4498=CARTESIAN_POINT ( 'NONE',  ( -2.500050800000000351, -0.3135853898029607456, 2.983565686104819648 ) ) ;
#4499=PLANE ( 'NONE',  #24113 ) ;
#4503=CARTESIAN_POINT ( 'NONE',  ( -5.904531657079157725, 2.975847129947406522, 0.3127741368606808403 ) ) ;
#4504=VECTOR ( 'NONE', #31906, 1000.000000000000114 ) ;
#4510=ORIENTED_EDGE ( 'NONE', *, *, #25925, .F. ) ;
#4517=CARTESIAN_POINT ( 'NONE',  ( 5.612718761614564400, 7.212912035758809459, 3.934162523501257613 ) ) ;
#4518=DIRECTION ( 'NONE',  ( -0.000000000000000000, -0.7071067811865516806, 0.7071067811865434649 ) ) ;
#4527=CARTESIAN_POINT ( 'NONE',  ( -2.987550801365593145, -0.3701630799359326152, 3.521866450007987037 ) ) ;
#4536=CARTESIAN_POINT ( 'NONE',  ( 0.000000000000000000, 0.000000000000000000, 0.000000000000000000 ) ) ;
#4537=CARTESIAN_POINT ( 'NONE',  ( 6.038144853276842916, 8.256557579931664392, 1.911563584435225005 ) ) ;
#4544=EDGE_LOOP ( 'NONE', ( #21828, #31758, #20018, #27758 ) ) ;
#4564=LINE ( 'NONE', #31975, #30953 ) ;
#4578=PLANE ( 'NONE',  #16118 ) ;
#4579=ADVANCED_FACE ( 'NONE', ( #15809 ), #4965, .T. ) ;
#4580=CARTESIAN_POINT ( 'NONE',  ( -6.137550801365595277, -1.828967928396026732, 3.368539882008728004 ) ) ;
#4589=VERTEX_POINT ( 'NONE', #25860 ) ;
#4590=LINE ( 'NONE', #12101, #25214 ) ;
#4591=LINE ( 'NONE', #26815, #21854 ) ;
#4596=CARTESIAN_POINT ( 'NONE',  ( 4.749760686538667009, 7.530955069117513112, 2.741043480754951744 ) ) ;
#4600=FACE_OUTER_BOUND ( 'NONE', #29901, .T. ) ;
#4613=CARTESIAN_POINT ( 'NONE',  ( -3.100050802731187272, -2.853674364686378695, -1.549418761218566809 ) ) ;
#4616=CARTESIAN_POINT ( 'NONE',  ( -4.600050799999999995, -1.887961173149512062, -2.331437884370912261 ) ) ;
#4620=CARTESIAN_POINT ( 'NONE',  ( -2.050050802731187449, 2.331437884370912705, -1.887961173149511618 ) ) ;
#4622=DIRECTION ( 'NONE',  ( -1.000000000000000000, -0.000000000000000000, 0.000000000000000000 ) ) ;
#4624=CARTESIAN_POINT ( 'NONE',  ( 0.000000000000000000, 5.471841788314749877, -3.018103451449674068 ) ) ;
#4635=LINE ( 'NONE', #31001, #30991 ) ;
#4636=ORIENTED_EDGE ( 'NONE', *, *, #11276, .F. ) ;
#4649=CARTESIAN_POINT ( 'NONE',  ( -2.700050802731186916, 2.853674364686379583, 1.549418761218565921 ) ) ;
#4651=CARTESIAN_POINT ( 'NONE',  ( -7.304531657079158080, -0.3127741368606806738, 2.975847129947406522 ) ) ;
#4656=CARTESIAN_POINT ( 'NONE',  ( 7.249760686538666121, 0.000000000000000000, 0.000000000000000000 ) ) ;
#4660=CARTESIAN_POINT ( 'NONE',  ( 5.377543748152549874, -5.151476664237518044, 6.139290821770238438 ) ) ;
#4666=CARTESIAN_POINT ( 'NONE',  ( 5.489321676144490958, 4.149060317827602873, -6.978593840069401644 ) ) ;
#4667=CARTESIAN_POINT ( 'NONE',  ( 7.249760686538667009, 6.226446564518003157, -6.147671362329155009 ) ) ;
#4669=ORIENTED_EDGE ( 'NONE', *, *, #7010, .T. ) ;
#4670=CARTESIAN_POINT ( 'NONE',  ( -8.000050800000000351, -2.754924098389954779, -1.195686321225201576 ) ) ;
#4671=CARTESIAN_POINT ( 'NONE',  ( 7.249760686538667009, -5.064320921489771976, -7.135485519862050374 ) ) ;
#4677=CARTESIAN_POINT ( 'NONE',  ( -2.837550801365592790, -3.675193018007246071, 1.088641768524163167 ) ) ;
#4680=DIRECTION ( 'NONE',  ( 0.000000000000000000, 0.000000000000000000, 1.000000000000000000 ) ) ;
#4681=CARTESIAN_POINT ( 'NONE',  ( 7.249760686538667009, -7.892520144992426268, -1.391664247347309535 ) ) ;
#4686=DIRECTION ( 'NONE',  ( -1.000000000000000000, -0.000000000000000000, -0.000000000000000000 ) ) ;
#4693=CARTESIAN_POINT ( 'NONE',  ( 7.249760686538667009, 7.199384779417119518, 4.973063321323901498 ) ) ;
#4697=EDGE_LOOP ( 'NONE', ( #26250, #2972, #15379, #28472 ) ) ;
#4701=CARTESIAN_POINT ( 'NONE',  ( 3.499999999999999556, -5.979767908488853756, 1.814490771706161354 ) ) ;
#4708=VERTEX_POINT ( 'NONE', #27493 ) ;
#4716=EDGE_LOOP ( 'NONE', ( #10045, #23819, #18674 ) ) ;
#4718=CARTESIAN_POINT ( 'NONE',  ( 7.249760686538667009, -2.210816291636156006, -8.466096581343503402 ) ) ;
#4722=ORIENTED_EDGE ( 'NONE', *, *, #1018, .T. ) ;
#4731=ORIENTED_EDGE ( 'NONE', *, *, #20687, .T. ) ;
#4734=CARTESIAN_POINT ( 'NONE',  ( -7.137550801365592612, 3.368539882008727115, 1.828967928396027176 ) ) ;
#4738=CARTESIAN_POINT ( 'NONE',  ( 3.499999999999999556, 0.000000000000000000, 0.000000000000000000 ) ) ;
#4742=ORIENTED_EDGE ( 'NONE', *, *, #19419, .T. ) ;
#4747=ORIENTED_EDGE ( 'NONE', *, *, #20616, .F. ) ;
#4753=ORIENTED_EDGE ( 'NONE', *, *, #5915, .T. ) ;
#4755=DIRECTION ( 'NONE',  ( -1.000000000000000000, 0.000000000000000000, 0.000000000000000000 ) ) ;
#4767=CARTESIAN_POINT ( 'NONE',  ( 4.749760686538667009, 4.007137495034812424, 6.940565734314612101 ) ) ;
#4768=CARTESIAN_POINT ( 'NONE',  ( -3.200050802731187360, -3.113457007523259268, 0.9222479816126455399 ) ) ;
#4770=CARTESIAN_POINT ( 'NONE',  ( -4.350050800000000883, 3.113457007523260156, -0.9222479816126439855 ) ) ;
#4777=ORIENTED_EDGE ( 'NONE', *, *, #26555, .F. ) ;
#4780=CARTESIAN_POINT ( 'NONE',  ( 6.749760686538667009, 0.000000000000000000, 0.000000000000000000 ) ) ;
#4781=ORIENTED_EDGE ( 'NONE', *, *, #5491, .T. ) ;
#4787=CARTESIAN_POINT ( 'NONE',  ( 7.249760686538667009, -2.210816291636271025, 8.466096581343474980 ) ) ;
#4789=ADVANCED_FACE ( 'NONE', ( #7406 ), #18278, .F. ) ;
#4797=CIRCLE ( 'NONE', #18134, 2.999999999999999556 ) ;
#4798=CARTESIAN_POINT ( 'NONE',  ( -8.000050799999993245, 1.538656665208432806, 2.942827626578075950 ) ) ;
#4805=CARTESIAN_POINT ( 'NONE',  ( -7.112550801365592257, 3.675193018007247403, -1.088641768524161391 ) ) ;
#4806=EDGE_LOOP ( 'NONE', ( #17638, #29586, #25669 ) ) ;
#4807=CARTESIAN_POINT ( 'NONE',  ( -6.804531657079157192, 2.325406398514293205, -1.883076972206379374 ) ) ;
#4810=CARTESIAN_POINT ( 'NONE',  ( 5.377543748152548986, -5.151476664237435443, -6.139290821770307716 ) ) ;
#4813=ORIENTED_EDGE ( 'NONE', *, *, #2182, .F. ) ;
#4814=CARTESIAN_POINT ( 'NONE',  ( 0.000000000000000000, -4.147285340411824173, 5.698247474649390298 ) ) ;
#4816=CARTESIAN_POINT ( 'NONE',  ( 5.489343806296447248, 1.512045527216204110, 7.976812024616029895 ) ) ;
#4827=CARTESIAN_POINT ( 'NONE',  ( -7.998722633285748174, -2.371517779863575370, 1.837526800715260533 ) ) ;
#4833=CARTESIAN_POINT ( 'NONE',  ( -4.087550801365593678, 2.752080473201636845, -2.228590825266444142 ) ) ;
#4835=EDGE_CURVE ( 'NONE', #12982, #8819, #26245, .T. ) ;
#4836=CARTESIAN_POINT ( 'NONE',  ( 5.612974441954674099, -6.420536856479970744, 5.126870824538740656 ) ) ;
#4838=EDGE_LOOP ( 'NONE', ( #32322, #1187, #17155 ) ) ;
#4844=EDGE_CURVE ( 'NONE', #16537, #8026, #13553, .T. ) ;
#4852=DIRECTION ( 'NONE',  ( -1.000000000000000000, -0.000000000000000000, -0.000000000000000000 ) ) ;
#4854=ORIENTED_EDGE ( 'NONE', *, *, #16281, .T. ) ;
#4856=AXIS2_PLACEMENT_3D ( 'NONE', #25974, #1214, #8399 ) ;
#4862=VERTEX_POINT ( 'NONE', #25631 ) ;
#4865=ORIENTED_EDGE ( 'NONE', *, *, #31653, .F. ) ;
#4872=PLANE ( 'NONE',  #28873 ) ;
#4873=VECTOR ( 'NONE', #16496, 1000.000000000000000 ) ;
#4882=CARTESIAN_POINT ( 'NONE',  ( 6.530491627857223591, -3.540416224243723597, 7.903708701126678449 ) ) ;
#4888=CARTESIAN_POINT ( 'NONE',  ( 5.612974259723586101, -2.621729824970331357, -7.786824029658790280 ) ) ;
#4893=CARTESIAN_POINT ( 'NONE',  ( 6.880159396099836400, 7.192972099401698571, -4.949130873693301957 ) ) ;
#4895=ORIENTED_EDGE ( 'NONE', *, *, #9647, .F. ) ;
#4897=CARTESIAN_POINT ( 'NONE',  ( 7.249760686538667009, 1.391664247347228045, 7.892520144992438702 ) ) ;
#4898=CARTESIAN_POINT ( 'NONE',  ( -6.987550801365594033, -0.3701630799359326152, 3.521866450007987037 ) ) ;
#4902=( BOUNDED_CURVE ( )  B_SPLINE_CURVE ( 2, ( #7136, #27525, #14800, #14456, #19670, #1458, #24846, #29862, #22332, #1611, #16977 ),
 .UNSPECIFIED., .F., .F. ) 
 B_SPLINE_CURVE_WITH_KNOTS ( ( 3, 2, 2, 2, 2, 3 ),
 ( 0.8728822619934377691, 0.8750000000000000000, 0.8906250000000000000, 0.9062500000000000000, 0.9218750000000000000, 0.9353822619934377691 ),
 .UNSPECIFIED. ) 
 CURVE ( )  GEOMETRIC_REPRESENTATION_ITEM ( )  RATIONAL_B_SPLINE_CURVE ( ( 0.9821626249036861100, 0.9896829947469995004, 1.000000000000000000, 0.9238795325112867385, 1.000000000000000000, 0.9238795325112867385, 1.000000000000000000, 0.9238795325112867385, 1.000000000000000000, 0.9341965377642872381, 0.9821626249036861100 ) ) 
 REPRESENTATION_ITEM ( '' )  );
#4914=PLANE ( 'NONE',  #20325 ) ;
#4923=ORIENTED_EDGE ( 'NONE', *, *, #22535, .F. ) ;
#4931=AXIS2_PLACEMENT_3D ( 'NONE', #3736, #13901, #11431 ) ;
#4934=CARTESIAN_POINT ( 'NONE',  ( 6.883866357751288412, 8.704251636488463006, 0.6899766464187978565 ) ) ;
#4944=DIRECTION ( 'NONE',  ( 0.000000000000000000, -0.9945218953682742891, 0.1045284632676437286 ) ) ;
#4945=CARTESIAN_POINT ( 'NONE',  ( -4.250050802731187183, 1.887961173149511618, 2.331437884370912705 ) ) ;
#4946=EDGE_LOOP ( 'NONE', ( #13574, #19189, #28106, #26641 ) ) ;
#4947=CARTESIAN_POINT ( 'NONE',  ( -5.037550801365593856, -1.088641768524163389, -3.675193018007246071 ) ) ;
#4956=EDGE_CURVE ( 'NONE', #19712, #11907, #794, .T. ) ;
#4959=VERTEX_POINT ( 'NONE', #18763 ) ;
#4963=ORIENTED_EDGE ( 'NONE', *, *, #19908, .T. ) ;
#4965=CYLINDRICAL_SURFACE ( 'NONE', #13916, 3.000000000000000444 ) ;
#4980=LINE ( 'NONE', #23008, #4355 ) ;
#4986=CARTESIAN_POINT ( 'NONE',  ( 5.612717990268491164, 0.1993707932846012776, 8.213645783354285967 ) ) ;
#4991=CARTESIAN_POINT ( 'NONE',  ( -7.162550801365593856, 2.752080473201636845, -2.228590825266444142 ) ) ;
#4993=CARTESIAN_POINT ( 'NONE',  ( -8.204531657079158435, 1.883076972206379374, 2.325406398514293205 ) ) ;
#4998=ORIENTED_EDGE ( 'NONE', *, *, #18380, .F. ) ;
#5002=AXIS2_PLACEMENT_3D ( 'NONE', #18115, #76, #28004 ) ;
#5011=CIRCLE ( 'NONE', #31717, 0.5000000000000004441 ) ;
#5012=CIRCLE ( 'NONE', #27874, 8.500000000000000000 ) ;
#5015=CARTESIAN_POINT ( 'NONE',  ( 6.356381451270080696, -0.5733789922930644378, -8.587653982362821736 ) ) ;
#5016=ORIENTED_EDGE ( 'NONE', *, *, #25752, .T. ) ;
#5018=CARTESIAN_POINT ( 'NONE',  ( -8.000050800000000351, -2.415348148595104938, -1.802067931085318930 ) ) ;
#5021=LINE ( 'NONE', #30773, #21981 ) ;
#5024=CARTESIAN_POINT ( 'NONE',  ( -7.162550801365593856, 2.752080473201636845, -2.228590825266444142 ) ) ;
#5031=VECTOR ( 'NONE', #14967, 1000.000000000000000 ) ;
#5041=CARTESIAN_POINT ( 'NONE',  ( -1.762942409646513164, -5.022711880624455567E-15, 2.999999999999999556 ) ) ;
#5055=CARTESIAN_POINT ( 'NONE',  ( -6.462550801365593678, 0.3701630799359330593, -3.521866450007987037 ) ) ;
#5072=CARTESIAN_POINT ( 'NONE',  ( 7.064423659272770273, 7.199384779417568048, -4.973063321325217778 ) ) ;
#5074=CIRCLE ( 'NONE', #25911, 2.999999999999999112 ) ;
#5075=VERTEX_POINT ( 'NONE', #25223 ) ;
#5079=CARTESIAN_POINT ( 'NONE',  ( -6.337550801365593678, 3.368539882008727115, 1.828967928396027176 ) ) ;
#5080=ORIENTED_EDGE ( 'NONE', *, *, #12575, .T. ) ;
#5082=DIRECTION ( 'NONE',  ( -1.000000000000000000, -0.000000000000000000, 0.000000000000000000 ) ) ;
#5083=CARTESIAN_POINT ( 'NONE',  ( 6.524594682510452159, -8.636529731786344755, 0.6222547417166852668 ) ) ;
#5093=ORIENTED_EDGE ( 'NONE', *, *, #8866, .T. ) ;
#5094=DIRECTION ( 'NONE',  ( -1.000000000000000000, -0.000000000000000000, -0.000000000000000000 ) ) ;
#5096=ORIENTED_EDGE ( 'NONE', *, *, #947, .T. ) ;
#5097=DIRECTION ( 'NONE',  ( 0.000000000000000000, 0.9063077870366476052, 0.4226182617407045483 ) ) ;
#5098=LINE ( 'NONE', #2945, #26722 ) ;
#5099=ORIENTED_EDGE ( 'NONE', *, *, #10708, .F. ) ;
#5113=ADVANCED_FACE ( 'NONE', ( #17688 ), #27569, .T. ) ;
#5116=CARTESIAN_POINT ( 'NONE',  ( -6.287550801365593856, 2.228590825266444142, 2.752080473201636845 ) ) ;
#5129=DIRECTION ( 'NONE',  ( 0.000000000000000000, 0.000000000000000000, -1.000000000000000000 ) ) ;
#5130=EDGE_CURVE ( 'NONE', #4589, #25021, #12367, .T. ) ;
#5131=ORIENTED_EDGE ( 'NONE', *, *, #13527, .T. ) ;
#5133=LINE ( 'NONE', #9965, #6403 ) ;
#5143=FACE_OUTER_BOUND ( 'NONE', #29624, .T. ) ;
#5151=ADVANCED_FACE ( 'NONE', ( #7182 ), #12029, .F. ) ;
#5152=CARTESIAN_POINT ( 'NONE',  ( -7.512550801365593500, -3.675193018007246071, 1.088641768524163167 ) ) ;
#5154=CARTESIAN_POINT ( 'NONE',  ( -8.400050800000000706, 2.331437884370912705, -1.887961173149511618 ) ) ;
#5162=CARTESIAN_POINT ( 'NONE',  ( 5.377543748152548986, -1.391664247347174754, -7.892520144992448472 ) ) ;
#5165=EDGE_CURVE ( 'NONE', #13430, #31497, #27715, .T. ) ;
#5170=CARTESIAN_POINT ( 'NONE',  ( -8.000050799999998574, -2.808468352995062478, -1.064040931622213249 ) ) ;
#5173=FACE_OUTER_BOUND ( 'NONE', #5524, .T. ) ;
#5175=ORIENTED_EDGE ( 'NONE', *, *, #33085, .F. ) ;
#5176=CARTESIAN_POINT ( 'NONE',  ( -5.612550801365594033, 1.828967928396027176, -3.368539882008727115 ) ) ;
#5183=EDGE_CURVE ( 'NONE', #8879, #6622, #25955, .T. ) ;
#5184=DIRECTION ( 'NONE',  ( 1.000000000000000000, 0.000000000000000000, 0.000000000000000000 ) ) ;
#5186=EDGE_CURVE ( 'NONE', #21400, #30724, #11845, .T. ) ;
#5193=DIRECTION ( 'NONE',  ( 1.000000000000000000, -0.000000000000000000, -0.000000000000000000 ) ) ;
#5200=ORIENTED_EDGE ( 'NONE', *, *, #29783, .F. ) ;
#5201=CARTESIAN_POINT ( 'NONE',  ( -5.300050802731187893, 1.549418761218566143, -2.853674364686379583 ) ) ;
#5206=CARTESIAN_POINT ( 'NONE',  ( -7.562550801365593323, -2.752080473201636845, 2.228590825266444586 ) ) ;
#5210=ORIENTED_EDGE ( 'NONE', *, *, #8031, .F. ) ;
#5221=EDGE_CURVE ( 'NONE', #24971, #25459, #22877, .T. ) ;
#5229=FACE_OUTER_BOUND ( 'NONE', #16440, .T. ) ;
#5230=CARTESIAN_POINT ( 'NONE',  ( -4.887550801365593500, 2.752080473201636845, -2.228590825266444142 ) ) ;
#5231=ORIENTED_EDGE ( 'NONE', *, *, #25504, .F. ) ;
#5236=EDGE_CURVE ( 'NONE', #16153, #22005, #29910, .T. ) ;
#5246=ORIENTED_EDGE ( 'NONE', *, *, #10345, .F. ) ;
#5256=DIRECTION ( 'NONE',  ( 0.000000000000000000, 0.000000000000000000, 1.000000000000000000 ) ) ;
#5257=CARTESIAN_POINT ( 'NONE',  ( 5.489343958331425632, 2.874233210898364366, 7.593062460271006842 ) ) ;
#5270=VERTEX_POINT ( 'NONE', #15345 ) ;
#5271=CARTESIAN_POINT ( 'NONE',  ( -6.087550801365593678, -2.752080473201636845, 2.228590825266444586 ) ) ;
#5272=CARTESIAN_POINT ( 'NONE',  ( -10.00000000000000000, 0.000000000000000000, 0.000000000000000000 ) ) ;
#5273=EDGE_CURVE ( 'NONE', #30224, #21233, #13018, .T. ) ;
#5277=ORIENTED_EDGE ( 'NONE', *, *, #14179, .T. ) ;
#5279=EDGE_CURVE ( 'NONE', #3680, #19129, #29903, .T. ) ;
#5286=CARTESIAN_POINT ( 'NONE',  ( -7.500050800000000351, 2.983565686104819648, 0.3135853898029609677 ) ) ;
#5297=DIRECTION ( 'NONE',  ( 1.000000000000000000, -0.000000000000000000, 0.000000000000000000 ) ) ;
#5299=EDGE_CURVE ( 'NONE', #20515, #3016, #25744, .T. ) ;
#5304=VERTEX_POINT ( 'NONE', #10157 ) ;
#5305=FACE_OUTER_BOUND ( 'NONE', #21481, .T. ) ;
#5307=EDGE_CURVE ( 'NONE', #2513, #27551, #26298, .T. ) ;
#5308=CARTESIAN_POINT ( 'NONE',  ( -4.104531657079157014, -0.3127741368606806738, 2.975847129947406522 ) ) ;
#5309=PLANE ( 'NONE',  #225 ) ;
#5313=DIRECTION ( 'NONE',  ( 0.000000000000000000, 0.000000000000000000, -1.000000000000000000 ) ) ;
#5327=CARTESIAN_POINT ( 'NONE',  ( -8.000050800000000351, -1.836970198721030181E-16, -3.000000000000000444 ) ) ;
#5335=CARTESIAN_POINT ( 'NONE',  ( -4.912550801365593856, -1.088641768524163389, -3.675193018007246071 ) ) ;
#5342=CIRCLE ( 'NONE', #21883, 2.999999999999999556 ) ;
#5343=DIRECTION ( 'NONE',  ( 0.000000000000000000, 0.000000000000000000, 1.000000000000000000 ) ) ;
#5344=FACE_OUTER_BOUND ( 'NONE', #6791, .T. ) ;
#5348=LINE ( 'NONE', #12696, #23655 ) ;
#5367=CARTESIAN_POINT ( 'NONE',  ( -7.012550801365592612, 3.368539882008727115, 1.828967928396027176 ) ) ;
#5371=ORIENTED_EDGE ( 'NONE', *, *, #10634, .T. ) ;
#5380=LINE ( 'NONE', #25784, #12482 ) ;
#5381=AXIS2_PLACEMENT_3D ( 'NONE', #16721, #6519, #29260 ) ;
#5386=DIRECTION ( 'NONE',  ( 0.000000000000000000, 0.7071067811865431318, 0.7071067811865520136 ) ) ;
#5396=AXIS2_PLACEMENT_3D ( 'NONE', #19720, #17215, #24900 ) ;
#5397=CARTESIAN_POINT ( 'NONE',  ( 6.037141848526921706, -8.105561522824292098, -2.473100090966245279 ) ) ;
#5401=EDGE_CURVE ( 'NONE', #24311, #3908, #9122, .T. ) ;
#5403=EDGE_CURVE ( 'NONE', #25459, #17821, #20927, .T. ) ;
#5407=VECTOR ( 'NONE', #26866, 1000.000000000000000 ) ;
#5413=VERTEX_POINT ( 'NONE', #19023 ) ;
#5421=DIRECTION ( 'NONE',  ( -1.000000000000000000, -0.000000000000000000, -0.000000000000000000 ) ) ;
#5422=CARTESIAN_POINT ( 'NONE',  ( 5.377543748152548986, 1.391664247347228045, 7.892520144992438702 ) ) ;
#5427=VECTOR ( 'NONE', #18047, 1000.000000000000114 ) ;
#5430=CARTESIAN_POINT ( 'NONE',  ( 7.249760686538667009, 0.000000000000000000, 0.000000000000000000 ) ) ;
#5431=CARTESIAN_POINT ( 'NONE',  ( 5.377543748152549874, -2.741043480754877582, -7.530955069117540646 ) ) ;
#5433=B_SPLINE_CURVE_WITH_KNOTS ( 'NONE', 3,
 ( #32840, #9911, #6891, #24605 ),
 .UNSPECIFIED., .F., .F.,
 ( 4, 4 ),
 ( 0.000000000000000000, 1.000000000000000000 ),
 .UNSPECIFIED. ) ;
#5438=CARTESIAN_POINT ( 'NONE',  ( -7.337550801365593678, 1.828967928396027176, -3.368539882008727115 ) ) ;
#5444=ORIENTED_EDGE ( 'NONE', *, *, #31925, .F. ) ;
#5446=( LENGTH_UNIT ( ) NAMED_UNIT ( * ) SI_UNIT ( .MILLI., .METRE. ) );
#5456=CIRCLE ( 'NONE', #10788, 6.000000000000000000 ) ;
#5457=B_SPLINE_CURVE_WITH_KNOTS ( 'NONE', 3,
 ( #5918, #11266, #8431, #6104, #26809, #21156, #5768, #16430, #925, #11102 ),
 .UNSPECIFIED., .F., .F.,
 ( 4, 2, 2, 2, 4 ),
 ( 1.968338519003748898E-07, 0.0005467926089500447324, 0.001093388384048189126, 0.001639984159146333411, 0.002186579934244477913 ),
 .UNSPECIFIED. ) ;
#5458=ORIENTED_EDGE ( 'NONE', *, *, #25745, .T. ) ;
#5459=CARTESIAN_POINT ( 'NONE',  ( 6.038144483126824724, 0.4487862922134418509, -8.463061282283007358 ) ) ;
#5460=DIRECTION ( 'NONE',  ( -1.000000000000000000, 0.000000000000000000, 0.000000000000000000 ) ) ;
#5470=CARTESIAN_POINT ( 'NONE',  ( -3.757304906975410308, -1.062355717592093463, -3.000000000000000888 ) ) ;
#5471=LINE ( 'NONE', #15663, #2737 ) ;
#5473=FACE_OUTER_BOUND ( 'NONE', #16920, .T. ) ;
#5478=UNCERTAINTY_MEASURE_WITH_UNIT (LENGTH_MEASURE( 1.000000000000000082E-05 ), #5446, 'distance_accuracy_value', 'NONE');
#5480=VERTEX_POINT ( 'NONE', #16481 ) ;
#5484=CARTESIAN_POINT ( 'NONE',  ( -3.462550801365593678, -3.521866450007987037, -0.3701630799359323931 ) ) ;
#5486=AXIS2_PLACEMENT_3D ( 'NONE', #22130, #29656, #8902 ) ;
#5488=CARTESIAN_POINT ( 'NONE',  ( -4.554531657079158080, -0.9198621039125872700, -3.105402419394638791 ) ) ;
#5491=EDGE_CURVE ( 'NONE', #12355, #6855, #23860, .T. ) ;
#5514=VECTOR ( 'NONE', #8194, 1000.000000000000114 ) ;
#5516=DIRECTION ( 'NONE',  ( -1.000000000000000000, 0.000000000000000000, 0.000000000000000000 ) ) ;
#5518=ORIENTED_EDGE ( 'NONE', *, *, #22001, .T. ) ;
#5519=CARTESIAN_POINT ( 'NONE',  ( -6.162550801365593856, 2.228590825266444142, 2.752080473201636845 ) ) ;
#5521=CARTESIAN_POINT ( 'NONE',  ( 7.249760686538667009, 7.530955069117551304, -2.741043480754851380 ) ) ;
#5524=EDGE_LOOP ( 'NONE', ( #30300, #12553, #11331 ) ) ;
#5530=AXIS2_PLACEMENT_3D ( 'NONE', #32736, #17842, #9816 ) ;
#5535=AXIS2_PLACEMENT_3D ( 'NONE', #25890, #2830, #12510 ) ;
#5539=CARTESIAN_POINT ( 'NONE',  ( 5.377543748152549874, -2.741043480754977946, 7.530955069117504230 ) ) ;
#5547=ORIENTED_EDGE ( 'NONE', *, *, #25035, .F. ) ;
#5558=ORIENTED_EDGE ( 'NONE', *, *, #17254, .F. ) ;
#5565=VECTOR ( 'NONE', #5082, 1000.000000000000000 ) ;
#5581=VERTEX_POINT ( 'NONE', #20029 ) ;
#5584=CARTESIAN_POINT ( 'NONE',  ( 0.000000000000000000, 6.704570150426983233, 2.172265885002680808 ) ) ;
#5585=CARTESIAN_POINT ( 'NONE',  ( 5.377543748152548986, -8.014274990069656823, 8.669741416787380218E-17 ) ) ;
#5600=ORIENTED_EDGE ( 'NONE', *, *, #25073, .F. ) ;
#5604=DIRECTION ( 'NONE',  ( 1.000000000000000000, -0.000000000000000000, -0.000000000000000000 ) ) ;
#5607=VECTOR ( 'NONE', #31230, 1000.000000000000000 ) ;
#5608=CARTESIAN_POINT ( 'NONE',  ( -6.600050800000000883, 1.887961173149511618, 2.331437884370912705 ) ) ;
#5611=ADVANCED_FACE ( 'NONE', ( #30223 ), #32398, .T. ) ;
#5615=VERTEX_POINT ( 'NONE', #12486 ) ;
#5618=DIRECTION ( 'NONE',  ( 0.000000000000000000, 0.000000000000000000, 1.000000000000000000 ) ) ;
#5620=VERTEX_POINT ( 'NONE', #7446 ) ;
#5632=ORIENTED_EDGE ( 'NONE', *, *, #11934, .T. ) ;
#5633=CARTESIAN_POINT ( 'NONE',  ( 7.249760686538667009, 0.7071067811866343922, -8.721381771256197624 ) ) ;
#5639=DIRECTION ( 'NONE',  ( 0.000000000000000000, 0.9510565162951544194, -0.3090169943749448977 ) ) ;
#5643=LINE ( 'NONE', #3474, #5607 ) ;
#5645=ADVANCED_FACE ( 'NONE', ( #29716 ), #7144, .F. ) ;
#5649=CARTESIAN_POINT ( 'NONE',  ( -8.000050800000000351, 0.000000000000000000, -3.000000000000000444 ) ) ;
#5650=CARTESIAN_POINT ( 'NONE',  ( -4.162550801365592967, -2.228590825266444586, -2.752080473201636401 ) ) ;
#5652=CARTESIAN_POINT ( 'NONE',  ( -3.904531657079157725, -2.975847129947406522, -0.3127741368606805072 ) ) ;
#5656=ORIENTED_EDGE ( 'NONE', *, *, #18670, .T. ) ;
#5657=FACE_OUTER_BOUND ( 'NONE', #32989, .T. ) ;
#5663=DIRECTION ( 'NONE',  ( 0.000000000000000000, 0.7431448254773954654, -0.6691306063588569053 ) ) ;
#5667=LINE ( 'NONE', #26218, #17678 ) ;
#5672=CARTESIAN_POINT ( 'NONE',  ( -5.262550801365593500, -0.3701630799359326152, 3.521866450007987037 ) ) ;
#5680=CARTESIAN_POINT ( 'NONE',  ( 3.499999999999999556, 6.745408891279539354, 5.171987904998129437 ) ) ;
#5683=DIRECTION ( 'NONE',  ( -1.000000000000000000, -0.000000000000000000, -0.000000000000000000 ) ) ;
#5692=ORIENTED_EDGE ( 'NONE', *, *, #27160, .F. ) ;
#5702=CARTESIAN_POINT ( 'NONE',  ( -4.162550801365592967, -2.228590825266444586, -2.752080473201636401 ) ) ;
#5704=FACE_OUTER_BOUND ( 'NONE', #28233, .T. ) ;
#5706=ORIENTED_EDGE ( 'NONE', *, *, #13683, .T. ) ;
#5714=VERTEX_POINT ( 'NONE', #17839 ) ;
#5715=ADVANCED_FACE ( 'NONE', ( #18148 ), #10119, .T. ) ;
#5721=FACE_OUTER_BOUND ( 'NONE', #6661, .T. ) ;
#5726=ORIENTED_EDGE ( 'NONE', *, *, #16466, .F. ) ;
#5727=EDGE_CURVE ( 'NONE', #21443, #21158, #20830, .T. ) ;
#5730=CARTESIAN_POINT ( 'NONE',  ( 6.356381935169121533, 8.357622142800114062, -2.055898738447909047 ) ) ;
#5733=ORIENTED_EDGE ( 'NONE', *, *, #23776, .F. ) ;
#5738=EDGE_LOOP ( 'NONE', ( #17736, #22892, #21302, #2728 ) ) ;
#5742=CARTESIAN_POINT ( 'NONE',  ( 7.064423659272771161, -7.199384779417533409, 4.973063321325270181 ) ) ;
#5748=ADVANCED_FACE ( 'NONE', ( #10795 ), #28188, .T. ) ;
#5752=DIRECTION ( 'NONE',  ( -1.000000000000000000, 0.000000000000000000, 0.000000000000000000 ) ) ;
#5761=ORIENTED_EDGE ( 'NONE', *, *, #1015, .F. ) ;
#5767=EDGE_LOOP ( 'NONE', ( #27140, #24786, #20434, #27598, #4813, #28605, #21113, #25533, #16939, #29415, #5246, #4923, #323, #31814, #4747, #24771, #23140, #2745, #13440, #5856, #24180, #16586, #15846, #18758, #7175, #5962, #2881, #10599, #9404, #23031, #19094, #19016, #29871, #28078, #6141, #14718, #12063, #7557, #20246, #21492, #7609, #30871, #27311, #21133, #19489, #25579, #4467, #27603, #22259, #10768, #1033, #16040, #27514, #6694, #10737, #8045, #29064, #27229, #23299, #25846, #19590, #26304, #11643, #1276 ) ) ;
#5768=CARTESIAN_POINT ( 'NONE',  ( 5.887530252753768067, 6.663910820542653823, -5.105578361685848776 ) ) ;
#5779=CARTESIAN_POINT ( 'NONE',  ( 6.530491241813344061, 0.6236753264481750270, -8.637950316517738258 ) ) ;
#5782=CARTESIAN_POINT ( 'NONE',  ( 7.064423600674403225, 0.8180878109954562438, -8.711672189282621659 ) ) ;
#5787=CARTESIAN_POINT ( 'NONE',  ( -4.100050799999999995, -0.3135853898029607456, 2.983565686104819648 ) ) ;
#5788=DIRECTION ( 'NONE',  ( 1.000000000000000000, -0.000000000000000000, -0.000000000000000000 ) ) ;
#5791=CARTESIAN_POINT ( 'NONE',  ( -8.000050800000003903, -1.538925392562835892, 2.674518376515694129 ) ) ;
#5796=CARTESIAN_POINT ( 'NONE',  ( -4.012550801365593500, 1.828967928396027176, -3.368539882008727115 ) ) ;
#5798=CARTESIAN_POINT ( 'NONE',  ( -5.104531657079157014, 2.975847129947406522, 0.3127741368606808403 ) ) ;
#5799=CARTESIAN_POINT ( 'NONE',  ( 4.749760686538667009, -2.741043480754877582, -7.530955069117540646 ) ) ;
#5800=CARTESIAN_POINT ( 'NONE',  ( -5.300050800000001061, 0.3135853898029611342, -2.983565686104819648 ) ) ;
#5804=ORIENTED_EDGE ( 'NONE', *, *, #22651, .F. ) ;
#5808=EDGE_CURVE ( 'NONE', #23747, #8809, #7560, .T. ) ;
#5812=CARTESIAN_POINT ( 'NONE',  ( 5.377543748152549874, -7.892520144992443143, 1.391664247347202288 ) ) ;
#5814=CARTESIAN_POINT ( 'NONE',  ( 3.500000000000000000, 0.000000000000000000, 0.000000000000000000 ) ) ;
#5820=ORIENTED_EDGE ( 'NONE', *, *, #31243, .F. ) ;
#5821=ORIENTED_EDGE ( 'NONE', *, *, #30324, .T. ) ;
#5823=FACE_OUTER_BOUND ( 'NONE', #32593, .T. ) ;
#5833=EDGE_LOOP ( 'NONE', ( #1753, #6937, #2191 ) ) ;
#5837=AXIS2_PLACEMENT_3D ( 'NONE', #14216, #1531, #30401 ) ;
#5838=EDGE_LOOP ( 'NONE', ( #15131, #10010, #11034 ) ) ;
#5843=CARTESIAN_POINT ( 'NONE',  ( -5.862550801365593145, -3.521866450007987037, -0.3701630799359323931 ) ) ;
#5849=CARTESIAN_POINT ( 'NONE',  ( -5.787550801365593856, 0.3701630799359330593, -3.521866450007987037 ) ) ;
#5855=CARTESIAN_POINT ( 'NONE',  ( 3.499999999999999556, 0.000000000000000000, 0.000000000000000000 ) ) ;
#5856=ORIENTED_EDGE ( 'NONE', *, *, #28624, .F. ) ;
#5863=CARTESIAN_POINT ( 'NONE',  ( -8.000050800000000351, 0.000000000000000000, 0.000000000000000000 ) ) ;
#5864=FACE_OUTER_BOUND ( 'NONE', #26985, .T. ) ;
#5874=DIRECTION ( 'NONE',  ( -1.000000000000000000, 0.000000000000000000, 0.000000000000000000 ) ) ;
#5878=CARTESIAN_POINT ( 'NONE',  ( -4.912942406915327354, -5.022711880624455567E-15, 2.999999999999999556 ) ) ;
#5883=ORIENTED_EDGE ( 'NONE', *, *, #14674, .F. ) ;
#5887=CARTESIAN_POINT ( 'NONE',  ( -5.807304909706597407, 1.062355717592095683, 2.999999999999999112 ) ) ;
#5888=CARTESIAN_POINT ( 'NONE',  ( 0.000000000000000000, -2.417132211460010005, -8.149077976821821778 ) ) ;
#5890=EDGE_LOOP ( 'NONE', ( #27128, #3340, #4895, #12730 ) ) ;
#5896=CARTESIAN_POINT ( 'NONE',  ( 3.499999999999999556, 0.000000000000000000, 0.000000000000000000 ) ) ;
#5898=AXIS2_PLACEMENT_3D ( 'NONE', #15412, #25624, #19088 ) ;
#5906=CIRCLE ( 'NONE', #24061, 2.999999999999999556 ) ;
#5910=ORIENTED_EDGE ( 'NONE', *, *, #22660, .F. ) ;
#5915=EDGE_CURVE ( 'NONE', #27064, #7973, #29326, .T. ) ;
#5918=CARTESIAN_POINT ( 'NONE',  ( 7.249760686538667009, 7.135485519862069914, -5.064320921489747995 ) ) ;
#5920=ORIENTED_EDGE ( 'NONE', *, *, #24908, .T. ) ;
#5927=ORIENTED_EDGE ( 'NONE', *, *, #30261, .T. ) ;
#5930=CARTESIAN_POINT ( 'NONE',  ( -7.312942406915325044, -8.831141768130910875E-16, 2.999999999999999556 ) ) ;
#5932=ORIENTED_EDGE ( 'NONE', *, *, #6930, .F. ) ;
#5934=CARTESIAN_POINT ( 'NONE',  ( 6.357667408475527360, -0.5738000813810182343, 8.588075071450647968 ) ) ;
#5942=CIRCLE ( 'NONE', #19313, 8.750000000000000000 ) ;
#5943=FACE_OUTER_BOUND ( 'NONE', #3839, .T. ) ;
#5946=VECTOR ( 'NONE', #28493, 1000.000000000000000 ) ;
#5950=DIRECTION ( 'NONE',  ( 1.000000000000000000, 0.000000000000000000, 0.000000000000000000 ) ) ;
#5952=CARTESIAN_POINT ( 'NONE',  ( 6.880159329304569304, -7.110803091624023686, -5.066480354149003773 ) ) ;
#5954=CARTESIAN_POINT ( 'NONE',  ( -3.512550801365593944, -3.675193018007246071, 1.088641768524163167 ) ) ;
#5956=EDGE_CURVE ( 'NONE', #15425, #3908, #16321, .T. ) ;
#5957=CARTESIAN_POINT ( 'NONE',  ( -6.800050800000000173, 2.331437884370912705, -1.887961173149511618 ) ) ;
#5962=ORIENTED_EDGE ( 'NONE', *, *, #20640, .F. ) ;
#5974=CARTESIAN_POINT ( 'NONE',  ( 7.249760686538667009, -8.466096581343467875, -2.210816291636301223 ) ) ;
#5984=AXIS2_PLACEMENT_3D ( 'NONE', #11656, #1143, #16846 ) ;
#5985=CARTESIAN_POINT ( 'NONE',  ( -4.362550801365593145, -2.752080473201636845, 2.228590825266444586 ) ) ;
#5986=AXIS2_PLACEMENT_3D ( 'NONE', #20315, #31200, #5618 ) ;
#6002=CIRCLE ( 'NONE', #24676, 6.248999999999998778 ) ;
#6003=CARTESIAN_POINT ( 'NONE',  ( 7.249760686538667009, 2.318425219014346172, -8.437262856154140067 ) ) ;
#6004=CARTESIAN_POINT ( 'NONE',  ( -1.773875666770781789, -0.3178988483021056854, 3.024605502323848949 ) ) ;
#6005=EDGE_CURVE ( 'NONE', #18566, #2513, #27734, .T. ) ;
#6006=CARTESIAN_POINT ( 'NONE',  ( -3.237550801365593145, 3.675193018007246959, -1.088641768524161391 ) ) ;
#6015=LINE ( 'NONE', #21230, #12337 ) ;
#6016=AXIS2_PLACEMENT_3D ( 'NONE', #27968, #22929, #5386 ) ;
#6018=AXIS2_PLACEMENT_3D ( 'NONE', #13085, #47, #25798 ) ;
#6022=ORIENTED_EDGE ( 'NONE', *, *, #1125, .T. ) ;
#6023=ORIENTED_EDGE ( 'NONE', *, *, #19387, .F. ) ;
#6025=CARTESIAN_POINT ( 'NONE',  ( -4.262550801365594388, -3.521866450007987037, -0.3701630799359323931 ) ) ;
#6031=CARTESIAN_POINT ( 'NONE',  ( -6.437550801365593323, 3.675193018007247403, -1.088641768524161391 ) ) ;
#6035=CARTESIAN_POINT ( 'NONE',  ( 0.000000000000000000, 6.704570150426983233, 2.172265885002680808 ) ) ;
#6040=VECTOR ( 'NONE', #23734, 1000.000000000000000 ) ;
#6044=EDGE_CURVE ( 'NONE', #22148, #32347, #9581, .T. ) ;
#6046=CARTESIAN_POINT ( 'NONE',  ( 6.357667697713671018, -0.9262207444595329520, -8.557242355892498153 ) ) ;
#6048=EDGE_CURVE ( 'NONE', #9165, #9138, #7447, .T. ) ;
#6053=CARTESIAN_POINT ( 'NONE',  ( 7.249760686538667009, 8.014274990069656823, -8.669741416787380218E-17 ) ) ;
#6054=CARTESIAN_POINT ( 'NONE',  ( -5.987550801365593145, -3.521866450007987037, -0.3701630799359323931 ) ) ;
#6060=DIRECTION ( 'NONE',  ( 0.000000000000000000, 0.000000000000000000, 1.000000000000000000 ) ) ;
#6062=AXIS2_PLACEMENT_3D ( 'NONE', #20797, #2952, #7925 ) ;
#6063=CARTESIAN_POINT ( 'NONE',  ( -4.850050800000000883, -1.549418761218565255, 2.853674364686380471 ) ) ;
#6072=VECTOR ( 'NONE', #6816, 1000.000000000000000 ) ;
#6073=CARTESIAN_POINT ( 'NONE',  ( -6.000050802731188959, 3.113457007523260156, -0.9222479816126439855 ) ) ;
#6078=EDGE_CURVE ( 'NONE', #14302, #21638, #22391, .T. ) ;
#6083=DIRECTION ( 'NONE',  ( -1.000000000000000000, -0.000000000000000000, -0.000000000000000000 ) ) ;
#6087=CARTESIAN_POINT ( 'NONE',  ( 7.249760686538667009, 0.000000000000000000, 0.000000000000000000 ) ) ;
#6091=CARTESIAN_POINT ( 'NONE',  ( -3.150050800000000262, -3.113457007523259268, 0.9222479816126455399 ) ) ;
#6094=VERTEX_POINT ( 'NONE', #14424 ) ;
#6096=EDGE_CURVE ( 'NONE', #21274, #5714, #20005, .T. ) ;
#6097=PLANE ( 'NONE',  #21993 ) ;
#6099=VERTEX_POINT ( 'NONE', #9269 ) ;
#6104=CARTESIAN_POINT ( 'NONE',  ( 6.530491751506348308, 7.017944781892023975, -5.074604403564599409 ) ) ;
#6121=CARTESIAN_POINT ( 'NONE',  ( 7.064632951172269415, 5.064320921489821714, 7.135485519862013959 ) ) ;
#6124=DIRECTION ( 'NONE',  ( -1.000000000000000000, -0.000000000000000000, 0.000000000000000000 ) ) ;
#6126=EDGE_CURVE ( 'NONE', #5615, #9418, #32665, .T. ) ;
#6134=CARTESIAN_POINT ( 'NONE',  ( -4.262550801365594388, -3.521866450007987037, -0.3701630799359323931 ) ) ;
#6136=CARTESIAN_POINT ( 'NONE',  ( -7.000050800000001239, -1.887961173149512062, -2.331437884370912261 ) ) ;
#6141=ORIENTED_EDGE ( 'NONE', *, *, #22846, .F. ) ;
#6153=CARTESIAN_POINT ( 'NONE',  ( 6.356381935169119757, -8.357622142800098075, 2.055898738447969887 ) ) ;
#6156=DIRECTION ( 'NONE',  ( 0.000000000000000000, -0.5877852522924797984, 0.8090169943749426773 ) ) ;
#6162=CARTESIAN_POINT ( 'NONE',  ( -4.162942409646514186, -5.022711880624455567E-15, 2.999999999999999556 ) ) ;
#6167=ORIENTED_EDGE ( 'NONE', *, *, #11202, .T. ) ;
#6171=CARTESIAN_POINT ( 'NONE',  ( -3.037550801365593856, 1.088641768524161613, 3.675193018007246959 ) ) ;
#6174=VERTEX_POINT ( 'NONE', #409 ) ;
#6182=EDGE_LOOP ( 'NONE', ( #12435, #783, #32029, #23861 ) ) ;
#6185=ORIENTED_EDGE ( 'NONE', *, *, #26925, .T. ) ;
#6186=LINE ( 'NONE', #3681, #1773 ) ;
#6187=CARTESIAN_POINT ( 'NONE',  ( -2.862550801365593145, -0.3701630799359326152, 3.521866450007987037 ) ) ;
#6193=CARTESIAN_POINT ( 'NONE',  ( -7.437550801365595099, -1.088641768524163389, -3.675193018007246071 ) ) ;
#6197=DIRECTION ( 'NONE',  ( 0.000000000000000000, 0.000000000000000000, 1.000000000000000000 ) ) ;
#6200=DIRECTION ( 'NONE',  ( 1.000000000000000000, -0.000000000000000000, -0.000000000000000000 ) ) ;
#6208=B_SPLINE_CURVE_WITH_KNOTS ( 'NONE', 3,
 ( #25661, #12624, #22828, #13125, #2782, #23177, #33032, #10105, #20324, #30533 ),
 .UNSPECIFIED., .F., .F.,
 ( 4, 2, 2, 2, 4 ),
 ( 1.968338519012285402E-07, 0.0005467926089500459250, 0.001093388384048190644, 0.001639984159146335363, 0.002186579934244480081 ),
 .UNSPECIFIED. ) ;
#6212=CARTESIAN_POINT ( 'NONE',  ( 5.612974384376776982, -7.213266193303285334, 3.934067627273179824 ) ) ;
#6215=ORIENTED_EDGE ( 'NONE', *, *, #32033, .F. ) ;
#6216=CARTESIAN_POINT ( 'NONE',  ( -7.757304906975409864, -1.062355717592095017, -2.999999999999999556 ) ) ;
#6222=EDGE_CURVE ( 'NONE', #136, #5270, #15925, .T. ) ;
#6232=CARTESIAN_POINT ( 'NONE',  ( -4.956376981307138330, -0.1572233378491221800, 3.000000000000000000 ) ) ;
#6238=LINE ( 'NONE', #19277, #30602 ) ;
#6255=ORIENTED_EDGE ( 'NONE', *, *, #26381, .F. ) ;
#6262=DIRECTION ( 'NONE',  ( -1.000000000000000000, 0.000000000000000000, 0.000000000000000000 ) ) ;
#6265=CARTESIAN_POINT ( 'NONE',  ( 7.249760686538667009, 5.064320921489820826, 7.135485519862015735 ) ) ;
#6267=B_SPLINE_CURVE_WITH_KNOTS ( 'NONE', 3,
 ( #26806, #26637, #9249, #24446, #21950, #24610 ),
 .UNSPECIFIED., .F., .F.,
 ( 4, 2, 4 ),
 ( 0.000000000000000000, 0.0008472833942745525669, 0.001694566788549105134 ),
 .UNSPECIFIED. ) ;
#6278=CARTESIAN_POINT ( 'NONE',  ( -6.450050802731187360, -2.331437884370912705, 1.887961173149512062 ) ) ;
#6280=CARTESIAN_POINT ( 'NONE',  ( -5.250050800000000351, 1.549418761218566143, -2.853674364686379583 ) ) ;
#6281=ADVANCED_FACE ( 'NONE', ( #32151 ), #1903, .T. ) ;
#6283=DIRECTION ( 'NONE',  ( 0.000000000000000000, -0.9945218953682734009, -0.1045284632676536235 ) ) ;
#6284=PLANE ( 'NONE',  #12991 ) ;
#6286=CARTESIAN_POINT ( 'NONE',  ( -7.250050800000000351, -1.549418761218565255, 2.853674364686380471 ) ) ;
#6291=EDGE_CURVE ( 'NONE', #7973, #32003, #20805, .T. ) ;
#6293=EDGE_CURVE ( 'NONE', #2704, #19221, #4564, .T. ) ;
#6294=CARTESIAN_POINT ( 'NONE',  ( -6.100050799999999995, 0.3135853898029611342, -2.983565686104819648 ) ) ;
#6301=ORIENTED_EDGE ( 'NONE', *, *, #3519, .T. ) ;
#6306=CARTESIAN_POINT ( 'NONE',  ( 4.749760686538667009, 6.940565734314597002, 4.007137495034836405 ) ) ;
#6308=LINE ( 'NONE', #24019, #14509 ) ;
#6309=LINE ( 'NONE', #24020, #4873 ) ;
#6312=EDGE_LOOP ( 'NONE', ( #4669, #6432, #13345, #9011 ) ) ;
#6313=LINE ( 'NONE', #16006, #20479 ) ;
#6317=CARTESIAN_POINT ( 'NONE',  ( -2.487550801365593589, 2.752080473201636845, -2.228590825266444142 ) ) ;
#6321=CARTESIAN_POINT ( 'NONE',  ( 7.249760686538667009, 1.391664247347228045, 7.892520144992438702 ) ) ;
#6329=VERTEX_POINT ( 'NONE', #4718 ) ;
#6332=EDGE_LOOP ( 'NONE', ( #31353, #3695, #14727 ) ) ;
#6334=CARTESIAN_POINT ( 'NONE',  ( -4.762550801365593500, 2.752080473201636845, -2.228590825266444142 ) ) ;
#6338=ORIENTED_EDGE ( 'NONE', *, *, #27124, .F. ) ;
#6339=CARTESIAN_POINT ( 'NONE',  ( -8.137550801365593500, 1.828967928396027176, -3.368539882008727115 ) ) ;
#6353=DIRECTION ( 'NONE',  ( -1.000000000000000000, -0.000000000000000000, -0.000000000000000000 ) ) ;
#6355=ORIENTED_EDGE ( 'NONE', *, *, #15919, .T. ) ;
#6366=( BOUNDED_CURVE ( )  B_SPLINE_CURVE ( 2, ( #15963, #13291, #5787, #20835, #3471, #26365, #11121, #23497, #31049, #5470, #15822 ),
 .UNSPECIFIED., .F., .F. ) 
 B_SPLINE_CURVE_WITH_KNOTS ( ( 3, 2, 2, 2, 2, 3 ),
 ( 0.6853822619934377691, 0.6875000000000000000, 0.7031250000000000000, 0.7187500000000000000, 0.7343750000000000000, 0.7478822619934377691 ),
 .UNSPECIFIED. ) 
 CURVE ( )  GEOMETRIC_REPRESENTATION_ITEM ( )  RATIONAL_B_SPLINE_CURVE ( ( 0.9821626249036861100, 0.9896829947469995004, 1.000000000000000000, 0.9238795325112867385, 1.000000000000000000, 0.9238795325112867385, 1.000000000000000000, 0.9238795325112867385, 1.000000000000000000, 0.9341965377642872381, 0.9821626249036861100 ) ) 
 REPRESENTATION_ITEM ( '' )  );
#6369=ORIENTED_EDGE ( 'NONE', *, *, #8526, .T. ) ;
#6371=CARTESIAN_POINT ( 'NONE',  ( 7.249760686538667009, 0.000000000000000000, 0.000000000000000000 ) ) ;
#6374=EDGE_LOOP ( 'NONE', ( #2751, #18604, #17302 ) ) ;
#6379=CARTESIAN_POINT ( 'NONE',  ( -3.150050802731187538, -2.983565686104819648, -0.3135853898029605791 ) ) ;
#6381=CARTESIAN_POINT ( 'NONE',  ( -4.650050802731187538, -1.887961173149512062, -2.331437884370912261 ) ) ;
#6382=AXIS2_PLACEMENT_3D ( 'NONE', #27586, #4686, #2173 ) ;
#6388=CIRCLE ( 'NONE', #15463, 6.248999999999999666 ) ;
#6393=CARTESIAN_POINT ( 'NONE',  ( -8.000050800000000351, 0.000000000000000000, 0.000000000000000000 ) ) ;
#6397=DIRECTION ( 'NONE',  ( 1.000000000000000000, 0.000000000000000000, 0.000000000000000000 ) ) ;
#6402=AXIS2_PLACEMENT_3D ( 'NONE', #25991, #32558, #15430 ) ;
#6403=VECTOR ( 'NONE', #25512, 1000.000000000000000 ) ;
#6408=ORIENTED_EDGE ( 'NONE', *, *, #15769, .F. ) ;
#6415=CARTESIAN_POINT ( 'NONE',  ( -2.319264028778656339, 1.051699019630317755, 3.241526370156308623 ) ) ;
#6423=CARTESIAN_POINT ( 'NONE',  ( 3.499999999999999556, -5.349675154362342866, 3.229702268444914370 ) ) ;
#6428=LINE ( 'NONE', #3477, #3821 ) ;
#6429=DIRECTION ( 'NONE',  ( -1.000000000000000000, 0.000000000000000000, 0.000000000000000000 ) ) ;
#6431=CARTESIAN_POINT ( 'NONE',  ( -6.050050802731187893, 2.331437884370912705, -1.887961173149511618 ) ) ;
#6432=ORIENTED_EDGE ( 'NONE', *, *, #22454, .T. ) ;
#6433=CARTESIAN_POINT ( 'NONE',  ( -5.950050799999999640, 3.113457007523260156, -0.9222479816126439855 ) ) ;
#6435=DIRECTION ( 'NONE',  ( 0.000000000000000000, -0.9063077870366448296, -0.4226182617407104325 ) ) ;
#6436=CARTESIAN_POINT ( 'NONE',  ( -5.700050802731187360, -1.549418761218565255, 2.853674364686380471 ) ) ;
#6453=DIRECTION ( 'NONE',  ( -1.000000000000000000, 0.000000000000000000, -0.000000000000000000 ) ) ;
#6458=CARTESIAN_POINT ( 'NONE',  ( 5.612718622971682336, -7.650113768151195259, 2.996580135471498707 ) ) ;
#6460=DIRECTION ( 'NONE',  ( 0.000000000000000000, -0.2588190451025240701, -0.9659258262890673130 ) ) ;
#6462=CARTESIAN_POINT ( 'NONE',  ( -3.912550801365593856, 3.675193018007247403, -1.088641768524161391 ) ) ;
#6465=CARTESIAN_POINT ( 'NONE',  ( 7.249760686538667009, -3.748318449932238838, -7.906491560603703839 ) ) ;
#6467=LINE ( 'NONE', #10898, #4504 ) ;
#6479=CYLINDRICAL_SURFACE ( 'NONE', #21510, 2.999999999999998224 ) ;
#6481=CIRCLE ( 'NONE', #23570, 2.999999999999999556 ) ;
#6484=VECTOR ( 'NONE', #13499, 1000.000000000000227 ) ;
#6486=DIRECTION ( 'NONE',  ( 0.000000000000000000, -0.08715574274765383600, -0.9961946980917459893 ) ) ;
#6487=DIRECTION ( 'NONE',  ( 0.000000000000000000, -0.5877852522924799095, 0.8090169943749425663 ) ) ;
#6489=ORIENTED_EDGE ( 'NONE', *, *, #19908, .F. ) ;
#6498=CARTESIAN_POINT ( 'NONE',  ( -3.762942409646513386, 4.884725290497410777E-15, -2.999999999999999556 ) ) ;
#6499=ORIENTED_EDGE ( 'NONE', *, *, #20666, .T. ) ;
#6500=CARTESIAN_POINT ( 'NONE',  ( 5.489321676144491846, 3.969109389279964262, 7.082488557107303961 ) ) ;
#6509=CARTESIAN_POINT ( 'NONE',  ( 3.499999999999999556, -5.522688772756441544, 6.461416928141223259 ) ) ;
#6512=CARTESIAN_POINT ( 'NONE',  ( -6.737550801365594033, -3.368539882008727115, -1.828967928396028064 ) ) ;
#6519=DIRECTION ( 'NONE',  ( 0.000000000000000000, -0.9961946980917457672, -0.08715574274765541807 ) ) ;
#6523=CARTESIAN_POINT ( 'NONE',  ( -8.000050800000000351, 3.673940397442060361E-16, 3.000000000000000444 ) ) ;
#6532=AXIS2_PLACEMENT_3D ( 'NONE', #15575, #28125, #7743 ) ;
#6535=ADVANCED_FACE ( 'NONE', ( #7002 ), #29606, .T. ) ;
#6537=ORIENTED_EDGE ( 'NONE', *, *, #14602, .T. ) ;
#6540=DIRECTION ( 'NONE',  ( -1.000000000000000000, -0.000000000000000000, 0.000000000000000000 ) ) ;
#6543=AXIS2_PLACEMENT_3D ( 'NONE', #22593, #20093, #30285 ) ;
#6544=CARTESIAN_POINT ( 'NONE',  ( 6.524595126109739240, 2.112519041817613630, 8.397268106035218338 ) ) ;
#6545=CARTESIAN_POINT ( 'NONE',  ( 6.038145208238973716, -7.553619661406936636, 3.842870190353671944 ) ) ;
#6553=CARTESIAN_POINT ( 'NONE',  ( 7.249760686538667009, 0.000000000000000000, 0.000000000000000000 ) ) ;
#6557=CARTESIAN_POINT ( 'NONE',  ( 7.249760686538667009, 6.147671362329302447, -6.226446564517854831 ) ) ;
#6560=ORIENTED_EDGE ( 'NONE', *, *, #24542, .T. ) ;
#6564=AXIS2_PLACEMENT_3D ( 'NONE', #13716, #11550, #1027 ) ;
#6573=VECTOR ( 'NONE', #28093, 1000.000000000000114 ) ;
#6579=CARTESIAN_POINT ( 'NONE',  ( -6.300050800000000173, -2.983565686104819648, -0.3135853898029605791 ) ) ;
#6583=AXIS2_PLACEMENT_3D ( 'NONE', #6918, #33015, #2258 ) ;
#6588=ORIENTED_EDGE ( 'NONE', *, *, #4956, .T. ) ;
#6594=CARTESIAN_POINT ( 'NONE',  ( 5.489321606599602887, 2.874206582856514203, -7.593050043411082584 ) ) ;
#6612=DIRECTION ( 'NONE',  ( -1.000000000000000000, 0.000000000000000000, 0.000000000000000000 ) ) ;
#6613=CYLINDRICAL_SURFACE ( 'NONE', #12357, 2.999999999999999112 ) ;
#6616=CARTESIAN_POINT ( 'NONE',  ( 7.249760686538667009, 6.940565734314653845, -4.007137495034738706 ) ) ;
#6621=CARTESIAN_POINT ( 'NONE',  ( -6.300050802731188782, -2.853674364686378695, -1.549418761218566809 ) ) ;
#6622=VERTEX_POINT ( 'NONE', #31940 ) ;
#6623=CARTESIAN_POINT ( 'NONE',  ( -7.500050800000000351, 2.983565686104819648, 0.3135853898029609677 ) ) ;
#6624=DIRECTION ( 'NONE',  ( 0.000000000000000000, -0.4226182617407104325, 0.9063077870366448296 ) ) ;
#6636=DIRECTION ( 'NONE',  ( 0.000000000000000000, 0.000000000000000000, -1.000000000000000000 ) ) ;
#6643=ADVANCED_FACE ( 'NONE', ( #27421 ), #22076, .F. ) ;
#6648=DIRECTION ( 'NONE',  ( 0.000000000000000000, -0.8191520442889975717, 0.5735764363510378328 ) ) ;
#6649=VERTEX_POINT ( 'NONE', #32293 ) ;
#6652=CARTESIAN_POINT ( 'NONE',  ( -4.400050802731187538, 3.113457007523260156, -0.9222479816126439855 ) ) ;
#6661=EDGE_LOOP ( 'NONE', ( #19006, #2074, #26066 ) ) ;
#6668=DIRECTION ( 'NONE',  ( -1.000000000000000000, 0.000000000000000000, 0.000000000000000000 ) ) ;
#6673=B_SPLINE_CURVE_WITH_KNOTS ( 'NONE', 3,
 ( #20452, #10408, #7555, #23118, #20271, #237, #20618, #18251, #30824, #15757 ),
 .UNSPECIFIED., .F., .F.,
 ( 4, 2, 2, 2, 4 ),
 ( 3.512955445812634541E-07, 0.0005479535487286800108, 0.001095555801912778812, 0.001643158055096877613, 0.002190760308280976631 ),
 .UNSPECIFIED. ) ;
#6674=DIRECTION ( 'NONE',  ( 0.000000000000000000, 0.08715574274767322327, -0.9961946980917442129 ) ) ;
#6676=CARTESIAN_POINT ( 'NONE',  ( -3.750050802731187627, 0.3135853898029611342, -2.983565686104819648 ) ) ;
#6677=CARTESIAN_POINT ( 'NONE',  ( 5.377543748152550762, 6.139290821770327256, -5.151476664237414127 ) ) ;
#6687=CARTESIAN_POINT ( 'NONE',  ( -4.987550801365594033, 0.3701630799359330593, -3.521866450007987037 ) ) ;
#6692=ORIENTED_EDGE ( 'NONE', *, *, #1830, .F. ) ;
#6694=ORIENTED_EDGE ( 'NONE', *, *, #25321, .F. ) ;
#6697=EDGE_CURVE ( 'NONE', #136, #21332, #17115, .T. ) ;
#6703=CARTESIAN_POINT ( 'NONE',  ( -3.437550801365593767, -1.088641768524163389, -3.675193018007246071 ) ) ;
#6704=ORIENTED_EDGE ( 'NONE', *, *, #5130, .T. ) ;
#6710=DIRECTION ( 'NONE',  ( 0.000000000000000000, -0.9659258262890652036, -0.2588190451025326189 ) ) ;
#6713=DIRECTION ( 'NONE',  ( 0.000000000000000000, 0.000000000000000000, 1.000000000000000000 ) ) ;
#6721=CARTESIAN_POINT ( 'NONE',  ( 5.489321708267612898, 5.297846913781776301, -6.152096559282782984 ) ) ;
#6731=VERTEX_POINT ( 'NONE', #17888 ) ;
#6738=ORIENTED_EDGE ( 'NONE', *, *, #5279, .F. ) ;
#6748=ORIENTED_EDGE ( 'NONE', *, *, #12942, .F. ) ;
#6750=DIRECTION ( 'NONE',  ( -1.000000000000000000, 0.000000000000000000, 0.000000000000000000 ) ) ;
#6752=ORIENTED_EDGE ( 'NONE', *, *, #16232, .T. ) ;
#6757=DIRECTION ( 'NONE',  ( 0.000000000000000000, 0.000000000000000000, 1.000000000000000000 ) ) ;
#6761=CARTESIAN_POINT ( 'NONE',  ( 6.357667873252802693, -8.266402141659458636, 2.398098878660925859 ) ) ;
#6769=CARTESIAN_POINT ( 'NONE',  ( 7.249760686538667009, 4.007137495034909236, -6.940565734314555257 ) ) ;
#6776=CARTESIAN_POINT ( 'NONE',  ( -4.950050802731188249, -0.3135853898029607456, 2.983565686104819648 ) ) ;
#6778=CARTESIAN_POINT ( 'NONE',  ( -7.437550801365595099, -1.088641768524163389, -3.675193018007246071 ) ) ;
#6780=FACE_OUTER_BOUND ( 'NONE', #12585, .T. ) ;
#6783=CARTESIAN_POINT ( 'NONE',  ( -2.162942409646512854, 4.884725290497410777E-15, -2.999999999999999556 ) ) ;
#6788=EDGE_CURVE ( 'NONE', #21638, #14302, #28348, .T. ) ;
#6791=EDGE_LOOP ( 'NONE', ( #8027, #26067, #5099, #27609 ) ) ;
#6796=CARTESIAN_POINT ( 'NONE',  ( 4.749760686538667009, -7.530955069117495349, -2.741043480755002371 ) ) ;
#6800=DIRECTION ( 'NONE',  ( 0.000000000000000000, -0.4067366430757887175, -0.9135454576426059736 ) ) ;
#6801=DIRECTION ( 'NONE',  ( -1.000000000000000000, -0.000000000000000000, -0.000000000000000000 ) ) ;
#6805=CARTESIAN_POINT ( 'NONE',  ( -4.550050802731187005, 0.3135853898029611342, -2.983565686104819648 ) ) ;
#6809=CARTESIAN_POINT ( 'NONE',  ( -1.773875666770781789, -0.3178988483021056854, 3.024605502323848949 ) ) ;
#6815=CARTESIAN_POINT ( 'NONE',  ( -7.004531657079158258, -1.883076972206379818, -2.325406398514292761 ) ) ;
#6816=DIRECTION ( 'NONE',  ( 1.000000000000000000, 0.000000000000000000, -0.000000000000000000 ) ) ;
#6823=ADVANCED_FACE ( 'NONE', ( #23673 ), #13457, .T. ) ;
#6839=CARTESIAN_POINT ( 'NONE',  ( -4.687550801365594211, 2.228590825266444142, 2.752080473201636845 ) ) ;
#6843=VERTEX_POINT ( 'NONE', #21174 ) ;
#6854=CARTESIAN_POINT ( 'NONE',  ( -2.337550801365593678, 3.368539882008727115, 1.828967928396026954 ) ) ;
#6855=VERTEX_POINT ( 'NONE', #18826 ) ;
#6867=ORIENTED_EDGE ( 'NONE', *, *, #3895, .F. ) ;
#6872=ORIENTED_EDGE ( 'NONE', *, *, #10127, .T. ) ;
#6873=CARTESIAN_POINT ( 'NONE',  ( 5.612718761614564400, 4.279483796479024882, 7.013540705848194001 ) ) ;
#6876=CARTESIAN_POINT ( 'NONE',  ( 0.000000000000000000, -1.471047635026823786, -6.892461014225975013 ) ) ;
#6880=DIRECTION ( 'NONE',  ( 1.000000000000000000, 0.000000000000000000, -0.000000000000000000 ) ) ;
#6882=FACE_OUTER_BOUND ( 'NONE', #4806, .T. ) ;
#6891=CARTESIAN_POINT ( 'NONE',  ( -2.242109179563498866, -0.3178988483021057410, 3.024605502323848949 ) ) ;
#6900=ORIENTED_EDGE ( 'NONE', *, *, #28690, .T. ) ;
#6908=VECTOR ( 'NONE', #2607, 1000.000000000000000 ) ;
#6910=FACE_OUTER_BOUND ( 'NONE', #2400, .T. ) ;
#6913=ORIENTED_EDGE ( 'NONE', *, *, #10816, .F. ) ;
#6915=CARTESIAN_POINT ( 'NONE',  ( 0.000000000000000000, 0.000000000000000000, 0.000000000000000000 ) ) ;
#6918=CARTESIAN_POINT ( 'NONE',  ( 3.499999999999999556, -2.861184399891040009, 6.440778198864103743 ) ) ;
#6923=EDGE_CURVE ( 'NONE', #6099, #23179, #23545, .T. ) ;
#6927=LINE ( 'NONE', #24167, #17210 ) ;
#6930=EDGE_CURVE ( 'NONE', #25757, #11409, #1211, .T. ) ;
#6931=CARTESIAN_POINT ( 'NONE',  ( -6.100050802731187716, 1.549418761218566143, -2.853674364686379583 ) ) ;
#6933=CARTESIAN_POINT ( 'NONE',  ( -4.100050799999999995, -0.3135853898029607456, 2.983565686104819648 ) ) ;
#6937=ORIENTED_EDGE ( 'NONE', *, *, #7108, .F. ) ;
#6939=DIRECTION ( 'NONE',  ( -1.000000000000000000, 0.000000000000000000, -0.000000000000000000 ) ) ;
#6945=ORIENTED_EDGE ( 'NONE', *, *, #19183, .T. ) ;
#6947=EDGE_CURVE ( 'NONE', #30847, #20064, #17878, .T. ) ;
#6953=ORIENTED_EDGE ( 'NONE', *, *, #235, .T. ) ;
#6954=VECTOR ( 'NONE', #24187, 1000.000000000000000 ) ;
#6961=AXIS2_PLACEMENT_3D ( 'NONE', #10432, #17961, #7262 ) ;
#6963=DIRECTION ( 'NONE',  ( 0.000000000000000000, -0.8191520442889844711, -0.5735764363510564845 ) ) ;
#6965=AXIS2_PLACEMENT_3D ( 'NONE', #6796, #22341, #16983 ) ;
#6967=CARTESIAN_POINT ( 'NONE',  ( 6.037141812302426302, -1.028012177296142582, 8.411869123983613861 ) ) ;
#6973=ORIENTED_EDGE ( 'NONE', *, *, #13108, .T. ) ;
#6974=CARTESIAN_POINT ( 'NONE',  ( -5.654531657079158613, -1.545410377633946286, 2.846291840500174697 ) ) ;
#6975=CARTESIAN_POINT ( 'NONE',  ( 4.749760686538667009, -5.151476664237435443, -6.139290821770307716 ) ) ;
#6990=AXIS2_PLACEMENT_3D ( 'NONE', #28598, #10531, #501 ) ;
#6993=CARTESIAN_POINT ( 'NONE',  ( 7.249760686538667009, 8.385837730238846314E-14, -8.014274990069656823 ) ) ;
#6994=ORIENTED_EDGE ( 'NONE', *, *, #13624, .T. ) ;
#6996=DIRECTION ( 'NONE',  ( -1.000000000000000000, 0.000000000000000000, 0.000000000000000000 ) ) ;
#6999=DIRECTION ( 'NONE',  ( -1.000000000000000000, 0.000000000000000000, -0.000000000000000000 ) ) ;
#7001=CARTESIAN_POINT ( 'NONE',  ( -3.887550801365593500, 2.228590825266444142, 2.752080473201636845 ) ) ;
#7002=FACE_OUTER_BOUND ( 'NONE', #18663, .T. ) ;
#7009=ORIENTED_EDGE ( 'NONE', *, *, #22399, .F. ) ;
#7010=EDGE_CURVE ( 'NONE', #30724, #1352, #6428, .T. ) ;
#7016=CARTESIAN_POINT ( 'NONE',  ( 5.612974044843318744, 8.054452210044761529, 1.622927203279369346 ) ) ;
#7017=AXIS2_PLACEMENT_3D ( 'NONE', #23616, #3091, #5097 ) ;
#7023=DIRECTION ( 'NONE',  ( -1.000000000000000000, -0.000000000000000000, -0.000000000000000000 ) ) ;
#7033=AXIS2_PLACEMENT_3D ( 'NONE', #10483, #10129, #25693 ) ;
#7036=DIRECTION ( 'NONE',  ( 0.000000000000000000, 0.000000000000000000, 1.000000000000000000 ) ) ;
#7043=AXIS2_PLACEMENT_3D ( 'NONE', #7844, #5516, #20565 ) ;
#7045=CIRCLE ( 'NONE', #24157, 8.750000000000000000 ) ;
#7049=DIRECTION ( 'NONE',  ( -0.000000000000000000, -0.2588190451025252359, 0.9659258262890669799 ) ) ;
#7058=CARTESIAN_POINT ( 'NONE',  ( 7.249760686538667009, 6.735557395310442023E-16, -5.500000000000000000 ) ) ;
#7074=AXIS2_PLACEMENT_3D ( 'NONE', #4814, #28211, #5313 ) ;
#7076=CARTESIAN_POINT ( 'NONE',  ( -5.187550801365593323, -3.521866450007987037, -0.3701630799359323931 ) ) ;
#7090=ORIENTED_EDGE ( 'NONE', *, *, #19773, .F. ) ;
#7094=CIRCLE ( 'NONE', #23630, 8.500000000000000000 ) ;
#7097=EDGE_CURVE ( 'NONE', #20949, #33081, #1955, .T. ) ;
#7100=DIRECTION ( 'NONE',  ( -1.000000000000000000, 0.000000000000000000, 0.000000000000000000 ) ) ;
#7105=DIRECTION ( 'NONE',  ( -1.000000000000000000, 0.000000000000000000, -0.000000000000000000 ) ) ;
#7108=EDGE_CURVE ( 'NONE', #16352, #10254, #31380, .T. ) ;
#7114=FACE_OUTER_BOUND ( 'NONE', #23484, .T. ) ;
#7120=CARTESIAN_POINT ( 'NONE',  ( -2.800050802731187005, 3.113457007523260156, -0.9222479816126439855 ) ) ;
#7122=VECTOR ( 'NONE', #5193, 1000.000000000000000 ) ;
#7125=CARTESIAN_POINT ( 'NONE',  ( -3.300050800000000173, -0.3135853898029607456, 2.983565686104819648 ) ) ;
#7127=CARTESIAN_POINT ( 'NONE',  ( -4.500050800000000351, 0.3135853898029611342, -2.983565686104819648 ) ) ;
#7129=ORIENTED_EDGE ( 'NONE', *, *, #26945, .T. ) ;
#7136=CARTESIAN_POINT ( 'NONE',  ( -2.912942406915326909, 4.884725290497410777E-15, -2.999999999999999556 ) ) ;
#7140=CARTESIAN_POINT ( 'NONE',  ( 7.249760686538667009, 6.139290821770327256, -5.151476664237414127 ) ) ;
#7143=CARTESIAN_POINT ( 'NONE',  ( 3.499999999999999556, 1.418488851014406693, 6.085876303339381899 ) ) ;
#7144=PLANE ( 'NONE',  #6965 ) ;
#7145=ORIENTED_EDGE ( 'NONE', *, *, #4088, .F. ) ;
#7153=CARTESIAN_POINT ( 'NONE',  ( 3.499999999999999556, 0.000000000000000000, 0.000000000000000000 ) ) ;
#7155=DIRECTION ( 'NONE',  ( -1.000000000000000000, -0.000000000000000000, -0.000000000000000000 ) ) ;
#7156=FACE_OUTER_BOUND ( 'NONE', #19474, .T. ) ;
#7168=CARTESIAN_POINT ( 'NONE',  ( -7.704531657079157547, 0.3127741368606810068, -2.975847129947406522 ) ) ;
#7174=DIRECTION ( 'NONE',  ( -0.000000000000000000, 0.5735764363510448272, -0.8191520442889927978 ) ) ;
#7175=ORIENTED_EDGE ( 'NONE', *, *, #17737, .F. ) ;
#7180=CARTESIAN_POINT ( 'NONE',  ( 5.887530180601099339, 4.515817126386108882, -7.076866030741268077 ) ) ;
#7181=CARTESIAN_POINT ( 'NONE',  ( 6.356382399260308347, 7.723816458760347281, 3.797266095948507836 ) ) ;
#7182=FACE_OUTER_BOUND ( 'NONE', #15059, .T. ) ;
#7183=ORIENTED_EDGE ( 'NONE', *, *, #29930, .F. ) ;
#7186=CARTESIAN_POINT ( 'NONE',  ( -2.612550801365594033, -3.368539882008727115, -1.828967928396027842 ) ) ;
#7189=CARTESIAN_POINT ( 'NONE',  ( 5.489321486716459475, 8.012877392144810429, -1.307389195612895572 ) ) ;
#7191=AXIS2_PLACEMENT_3D ( 'NONE', #453, #15476, #10633 ) ;
#7192=CARTESIAN_POINT ( 'NONE',  ( -2.587550801365593678, 0.3701630799359330593, -3.521866450007987037 ) ) ;
#7193=DIRECTION ( 'NONE',  ( 0.000000000000000000, 0.000000000000000000, 1.000000000000000000 ) ) ;
#7194=DIRECTION ( 'NONE',  ( -1.000000000000000000, -0.000000000000000000, -0.000000000000000000 ) ) ;
#7200=DIRECTION ( 'NONE',  ( -1.000000000000000000, -0.000000000000000000, -0.000000000000000000 ) ) ;
#7202=EDGE_CURVE ( 'NONE', #23972, #18705, #28891, .T. ) ;
#7206=CARTESIAN_POINT ( 'NONE',  ( 5.612974384376776094, 7.013635602076208286, 4.279837954023495428 ) ) ;
#7212=AXIS2_PLACEMENT_3D ( 'NONE', #9512, #7200, #19728 ) ;
#7215=DIRECTION ( 'NONE',  ( -1.000000000000000000, 0.000000000000000000, -0.000000000000000000 ) ) ;
#7216=EDGE_LOOP ( 'NONE', ( #28250, #1829, #13328, #14731 ) ) ;
#7229=CARTESIAN_POINT ( 'NONE',  ( 7.064423659272771161, 4.973063321325294162, 7.199384779417516533 ) ) ;
#7230=DIRECTION ( 'NONE',  ( 1.000000000000000000, -0.000000000000000000, -0.000000000000000000 ) ) ;
#7232=CARTESIAN_POINT ( 'NONE',  ( 7.249760686538667009, 0.000000000000000000, 0.000000000000000000 ) ) ;
#7234=EDGE_LOOP ( 'NONE', ( #24876, #16215, #10616, #6588 ) ) ;
#7236=CARTESIAN_POINT ( 'NONE',  ( 6.883866557622098092, -2.328663417917384848, -8.415306967752700373 ) ) ;
#7244=CARTESIAN_POINT ( 'NONE',  ( -7.287550801365593856, 2.752080473201636845, -2.228590825266444142 ) ) ;
#7251=EDGE_CURVE ( 'NONE', #16750, #16397, #16833, .T. ) ;
#7252=ORIENTED_EDGE ( 'NONE', *, *, #1132, .T. ) ;
#7255=DIRECTION ( 'NONE',  ( 0.000000000000000000, 0.000000000000000000, 1.000000000000000000 ) ) ;
#7257=VERTEX_POINT ( 'NONE', #6616 ) ;
#7262=DIRECTION ( 'NONE',  ( 0.000000000000000000, 0.9945218953682729568, 0.1045284632676570374 ) ) ;
#7266=DIRECTION ( 'NONE',  ( -1.000000000000000000, 0.000000000000000000, 0.000000000000000000 ) ) ;
#7267=CARTESIAN_POINT ( 'NONE',  ( 5.377543748152548986, 8.014274990069656823, -8.669741416787380218E-17 ) ) ;
#7275=CARTESIAN_POINT ( 'NONE',  ( -2.200050802731187360, -0.9222479816126459840, -3.113457007523259268 ) ) ;
#7276=EDGE_LOOP ( 'NONE', ( #10836, #31248, #17836, #11711 ) ) ;
#7277=CARTESIAN_POINT ( 'NONE',  ( -8.037550801365592079, 3.675193018007247403, -1.088641768524161391 ) ) ;
#7288=EDGE_CURVE ( 'NONE', #13848, #5480, #17124, .T. ) ;
#7290=LINE ( 'NONE', #2111, #24617 ) ;
#7300=DIRECTION ( 'NONE',  ( -1.000000000000000000, -0.000000000000000000, -0.000000000000000000 ) ) ;
#7301=VERTEX_POINT ( 'NONE', #32870 ) ;
#7307=CARTESIAN_POINT ( 'NONE',  ( 6.356381451270081584, 0.5733789922931242788, 8.587653982362816407 ) ) ;
#7314=CARTESIAN_POINT ( 'NONE',  ( -5.662550801365592967, 0.3701630799359330593, -3.521866450007987037 ) ) ;
#7316=CARTESIAN_POINT ( 'NONE',  ( -7.954531657079159324, -3.105402419394638791, 0.9198621039125867149 ) ) ;
#7333=CARTESIAN_POINT ( 'NONE',  ( -8.000050800000000351, -1.817871341476558600, -2.391135792897344903 ) ) ;
#7334=DIRECTION ( 'NONE',  ( -1.000000000000000000, -0.000000000000000000, 0.000000000000000000 ) ) ;
#7339=ORIENTED_EDGE ( 'NONE', *, *, #27309, .T. ) ;
#7340=CARTESIAN_POINT ( 'NONE',  ( -4.037550801365593856, 3.675193018007247403, -1.088641768524161391 ) ) ;
#7350=ADVANCED_FACE ( 'NONE', ( #23316 ), #85, .F. ) ;
#7365=CARTESIAN_POINT ( 'NONE',  ( -2.500050800000000351, -0.3135853898029607456, 2.983565686104819648 ) ) ;
#7370=ORIENTED_EDGE ( 'NONE', *, *, #4060, .T. ) ;
#7371=CARTESIAN_POINT ( 'NONE',  ( -7.262550801365593500, 0.3701630799359330593, -3.521866450007987037 ) ) ;
#7376=CARTESIAN_POINT ( 'NONE',  ( 7.249760686538667009, -2.318425219014174754, -8.437262856154184476 ) ) ;
#7378=CARTESIAN_POINT ( 'NONE',  ( 7.249760686538667009, 4.973063321323876629, 7.199384779417138169 ) ) ;
#7383=ORIENTED_EDGE ( 'NONE', *, *, #15380, .F. ) ;
#7388=DIRECTION ( 'NONE',  ( 0.000000000000000000, 0.000000000000000000, 1.000000000000000000 ) ) ;
#7391=CARTESIAN_POINT ( 'NONE',  ( 6.530491712438077911, -4.859093986587904368, 7.168846788212674070 ) ) ;
#7392=FACE_OUTER_BOUND ( 'NONE', #14086, .T. ) ;
#7393=CARTESIAN_POINT ( 'NONE',  ( -7.987550801365593145, 3.521866450007987037, 0.3701630799359328372 ) ) ;
#7396=CARTESIAN_POINT ( 'NONE',  ( 1.750000000000000000, -5.522688772756352726, -6.461416928141300531 ) ) ;
#7406=FACE_OUTER_BOUND ( 'NONE', #32849, .T. ) ;
#7412=CARTESIAN_POINT ( 'NONE',  ( -5.400050800000000706, -1.887961173149512062, -2.331437884370912261 ) ) ;
#7421=CARTESIAN_POINT ( 'NONE',  ( 5.612718383992090665, 8.123482740191969143, 1.229942497144064451 ) ) ;
#7423=EDGE_CURVE ( 'NONE', #20990, #26613, #18099, .T. ) ;
#7424=CARTESIAN_POINT ( 'NONE',  ( 3.499999999999999556, 2.871924938129968741, -6.435996203144479288 ) ) ;
#7425=CARTESIAN_POINT ( 'NONE',  ( -3.050050802731187449, -1.887961173149512062, -2.331437884370912261 ) ) ;
#7427=CARTESIAN_POINT ( 'NONE',  ( -3.850050799999999995, -2.853674364686378695, -1.549418761218566809 ) ) ;
#7429=DIRECTION ( 'NONE',  ( 0.000000000000000000, 0.000000000000000000, 1.000000000000000000 ) ) ;
#7430=ORIENTED_EDGE ( 'NONE', *, *, #15819, .T. ) ;
#7431=CARTESIAN_POINT ( 'NONE',  ( -2.000050802731187627, 3.113457007523260156, -0.9222479816126439855 ) ) ;
#7445=CARTESIAN_POINT ( 'NONE',  ( 7.249760686538667009, 5.151476664237477188, 6.139290821770273077 ) ) ;
#7446=CARTESIAN_POINT ( 'NONE',  ( 7.249760686538667009, -3.647351267791519636, -7.953573330858250579 ) ) ;
#7447=( BOUNDED_CURVE ( )  B_SPLINE_CURVE ( 2, ( #11960, #27319, #21971 ),
 .UNSPECIFIED., .F., .F. ) 
 B_SPLINE_CURVE_WITH_KNOTS ( ( 3, 3 ),
 ( 0.9353822619934377691, 0.9375000000000000000 ),
 .UNSPECIFIED. ) 
 CURVE ( )  GEOMETRIC_REPRESENTATION_ITEM ( )  RATIONAL_B_SPLINE_CURVE ( ( 0.9821626249036861100, 0.9896829947469995004, 1.000000000000000000 ) ) 
 REPRESENTATION_ITEM ( '' )  );
#7449=DIRECTION ( 'NONE',  ( -1.000000000000000000, -0.000000000000000000, -0.000000000000000000 ) ) ;
#7451=ORIENTED_EDGE ( 'NONE', *, *, #9113, .T. ) ;
#7458=CARTESIAN_POINT ( 'NONE',  ( 5.377543748152548098, -2.789499415801756586E-14, 8.014274990069656823 ) ) ;
#7461=DESIGN_CONTEXT ( 'detailed design', #29135, 'design' ) ;
#7464=CARTESIAN_POINT ( 'NONE',  ( -7.812550801365593323, 3.368539882008727115, 1.828967928396026954 ) ) ;
#7466=CARTESIAN_POINT ( 'NONE',  ( -5.704531657079157547, -0.3127741368606806738, 2.975847129947406522 ) ) ;
#7467=CIRCLE ( 'NONE', #11739, 8.750000000000000000 ) ;
#7473=CARTESIAN_POINT ( 'NONE',  ( 7.249760686538667009, 8.711672189281426171, 0.8180878109962165246 ) ) ;
#7476=CARTESIAN_POINT ( 'NONE',  ( 7.064423669210280643, -5.064320921489739113, 7.135485519863445703 ) ) ;
#7478=CIRCLE ( 'NONE', #14966, 2.999999999999998224 ) ;
#7482=CARTESIAN_POINT ( 'NONE',  ( 4.749760686538667009, 5.151476664237558900, -6.139290821770204687 ) ) ;
#7484=CARTESIAN_POINT ( 'NONE',  ( 7.249760686538667009, 7.906491560603665647, 3.748318449932320107 ) ) ;
#7485=DIRECTION ( 'NONE',  ( -1.000000000000000000, -0.000000000000000000, -0.000000000000000000 ) ) ;
#7489=CARTESIAN_POINT ( 'NONE',  ( -8.000050800000000351, -2.570627647327130116, -1.572659124966501620 ) ) ;
#7496=CARTESIAN_POINT ( 'NONE',  ( -7.512550801365593500, -3.675193018007246071, 1.088641768524163167 ) ) ;
#7498=DIRECTION ( 'NONE',  ( 0.000000000000000000, 0.08715574274765452989, 0.9961946980917458783 ) ) ;
#7503=ORIENTED_EDGE ( 'NONE', *, *, #9493, .T. ) ;
#7508=VECTOR ( 'NONE', #8691, 1000.000000000000000 ) ;
#7509=EDGE_CURVE ( 'NONE', #33081, #16776, #11471, .T. ) ;
#7525=CARTESIAN_POINT ( 'NONE',  ( 7.249760686538667009, -7.135485519861965109, -5.064320921489893657 ) ) ;
#7533=CARTESIAN_POINT ( 'NONE',  ( -6.812550801365595099, -1.828967928396026732, 3.368539882008728004 ) ) ;
#7545=DIRECTION ( 'NONE',  ( 0.000000000000000000, 0.000000000000000000, 1.000000000000000000 ) ) ;
#7549=CARTESIAN_POINT ( 'NONE',  ( 7.249760686538667009, -3.748318449932352081, 7.906491560603652324 ) ) ;
#7552=DIRECTION ( 'NONE',  ( -1.000000000000000000, 0.000000000000000000, -0.000000000000000000 ) ) ;
#7554=DIRECTION ( 'NONE',  ( 0.000000000000000000, 0.000000000000000000, 1.000000000000000000 ) ) ;
#7555=CARTESIAN_POINT ( 'NONE',  ( 5.612717990268488499, 8.213645783354285967, -0.1993707932846307540 ) ) ;
#7557=ORIENTED_EDGE ( 'NONE', *, *, #986, .F. ) ;
#7560=B_SPLINE_CURVE_WITH_KNOTS ( 'NONE', 3,
 ( #8785, #3284, #18989, #11284, #5934, #16132, #21171, #8928, #29175, #31520 ),
 .UNSPECIFIED., .F., .F.,
 ( 4, 2, 2, 2, 4 ),
 ( 1.968338519002106713E-07, 0.0005467930078056959303, 0.001093389181759491522, 0.001639985355713287222, 0.002186581529667083138 ),
 .UNSPECIFIED. ) ;
#7562=CARTESIAN_POINT ( 'NONE',  ( -6.787550801365593856, -3.521866450007987037, -0.3701630799359323931 ) ) ;
#7570=FACE_OUTER_BOUND ( 'NONE', #28000, .T. ) ;
#7571=CARTESIAN_POINT ( 'NONE',  ( 6.037141752603385036, -8.462586328878536790, 0.4483113388088767470 ) ) ;
#7582=ORIENTED_EDGE ( 'NONE', *, *, #25393, .F. ) ;
#7584=CARTESIAN_POINT ( 'NONE',  ( 6.880159396099833735, -4.949130873693328603, -7.192972099401679920 ) ) ;
#7592=EDGE_CURVE ( 'NONE', #24987, #12982, #13953, .T. ) ;
#7597=AXIS2_PLACEMENT_3D ( 'NONE', #19864, #10325, #2817 ) ;
#7608=CARTESIAN_POINT ( 'NONE',  ( -2.450050802731187360, -2.331437884370912705, 1.887961173149512062 ) ) ;
#7609=ORIENTED_EDGE ( 'NONE', *, *, #19997, .F. ) ;
#7610=CARTESIAN_POINT ( 'NONE',  ( -4.237550801365593145, -1.088641768524163389, -3.675193018007246071 ) ) ;
#7611=EDGE_CURVE ( 'NONE', #31571, #32878, #4409, .T. ) ;
#7617=ORIENTED_EDGE ( 'NONE', *, *, #27309, .F. ) ;
#7618=CYLINDRICAL_SURFACE ( 'NONE', #28822, 6.248999999999999666 ) ;
#7619=DIRECTION ( 'NONE',  ( 0.000000000000000000, 0.000000000000000000, 1.000000000000000000 ) ) ;
#7627=ORIENTED_EDGE ( 'NONE', *, *, #12144, .F. ) ;
#7634=CARTESIAN_POINT ( 'NONE',  ( 3.499999999999999556, 0.000000000000000000, 0.000000000000000000 ) ) ;
#7638=EDGE_CURVE ( 'NONE', #21332, #9995, #14391, .T. ) ;
#7658=CARTESIAN_POINT ( 'NONE',  ( -6.262550801365593500, 3.521866450007987037, 0.3701630799359328372 ) ) ;
#7660=CARTESIAN_POINT ( 'NONE',  ( -2.604531657079157903, 1.883076972206379374, 2.325406398514293205 ) ) ;
#7662=CARTESIAN_POINT ( 'NONE',  ( 4.749760686538667009, -8.014274990069656823, 8.669741416787380218E-17 ) ) ;
#7665=ORIENTED_EDGE ( 'NONE', *, *, #15349, .T. ) ;
#7667=( BOUNDED_CURVE ( )  B_SPLINE_CURVE ( 2, ( #11309, #13305, #5800, #15978, #23993, #20852, #13481, #3146, #31729, #8464, #21517 ),
 .UNSPECIFIED., .F., .F. ) 
 B_SPLINE_CURVE_WITH_KNOTS ( ( 3, 2, 2, 2, 2, 3 ),
 ( 0.4978822619934377136, 0.5000000000000000000, 0.5156250000000000000, 0.5312500000000000000, 0.5468750000000000000, 0.5603822619934377691 ),
 .UNSPECIFIED. ) 
 CURVE ( )  GEOMETRIC_REPRESENTATION_ITEM ( )  RATIONAL_B_SPLINE_CURVE ( ( 0.9821626249036857770, 0.9896829947469991673, 1.000000000000000000, 0.9238795325112867385, 1.000000000000000000, 0.9238795325112867385, 1.000000000000000000, 0.9238795325112867385, 1.000000000000000000, 0.9341965377642872381, 0.9821626249036861100 ) ) 
 REPRESENTATION_ITEM ( '' )  );
#7682=CARTESIAN_POINT ( 'NONE',  ( -8.000050800000000351, -0.5569032332065858570, -2.961701699052899261 ) ) ;
#7683=CARTESIAN_POINT ( 'NONE',  ( 0.000000000000000000, 1.459547570502463198, -6.894905428400257996 ) ) ;
#7688=CARTESIAN_POINT ( 'NONE',  ( -5.862550801365593145, -3.521866450007987037, -0.3701630799359323931 ) ) ;
#7691=CARTESIAN_POINT ( 'NONE',  ( 4.749760686538667009, -6.139290821770219786, -5.151476664237539360 ) ) ;
#7692=DIRECTION ( 'NONE',  ( 0.000000000000000000, -0.8191520442889975717, 0.5735764363510378328 ) ) ;
#7709=VERTEX_POINT ( 'NONE', #19613 ) ;
#7711=ADVANCED_FACE ( 'NONE', ( #29811 ), #27289, .T. ) ;
#7716=VECTOR ( 'NONE', #13114, 1000.000000000000000 ) ;
#7718=ORIENTED_EDGE ( 'NONE', *, *, #31689, .T. ) ;
#7724=FACE_OUTER_BOUND ( 'NONE', #12786, .T. ) ;
#7725=DIRECTION ( 'NONE',  ( 0.000000000000000000, 0.9063077870366514910, -0.4226182617406961106 ) ) ;
#7727=DIRECTION ( 'NONE',  ( 0.000000000000000000, 0.000000000000000000, -1.000000000000000000 ) ) ;
#7732=EDGE_CURVE ( 'NONE', #25433, #14402, #6673, .T. ) ;
#7736=DIRECTION ( 'NONE',  ( 0.000000000000000000, 0.8191520442889883569, 0.5735764363510510444 ) ) ;
#7743=DIRECTION ( 'NONE',  ( 0.000000000000000000, 0.000000000000000000, 1.000000000000000000 ) ) ;
#7745=DIRECTION ( 'NONE',  ( 0.000000000000000000, -0.8660254037844432595, 0.4999999999999918954 ) ) ;
#7750=LINE ( 'NONE', #20935, #1229 ) ;
#7751=CARTESIAN_POINT ( 'NONE',  ( -5.037550801365593856, -1.088641768524163611, -3.675193018007245627 ) ) ;
#7754=CARTESIAN_POINT ( 'NONE',  ( 6.038145208238977268, 7.553619661406968611, -3.842870190353619542 ) ) ;
#7755=ADVANCED_FACE ( 'NONE', ( #30970 ), #32987, .T. ) ;
#7766=CARTESIAN_POINT ( 'NONE',  ( 7.064423659272771161, -4.973063321325243535, -7.199384779417551172 ) ) ;
#7767=EDGE_CURVE ( 'NONE', #1536, #9966, #10284, .T. ) ;
#7769=CARTESIAN_POINT ( 'NONE',  ( 6.880159396099833735, -7.192972099401662156, 4.949130873693353472 ) ) ;
#7771=VERTEX_POINT ( 'NONE', #27969 ) ;
#7777=CARTESIAN_POINT ( 'NONE',  ( 5.612973690782940395, 8.213905076232780544, 0.1996300861631225554 ) ) ;
#7783=DIRECTION ( 'NONE',  ( 0.000000000000000000, 0.000000000000000000, -1.000000000000000000 ) ) ;
#7784=LINE ( 'NONE', #92, #14513 ) ;
#7786=CARTESIAN_POINT ( 'NONE',  ( -2.750050802731187627, 2.983565686104819648, 0.3135853898029609677 ) ) ;
#7788=CARTESIAN_POINT ( 'NONE',  ( -6.587550801365593678, 0.3701630799359330593, -3.521866450007987037 ) ) ;
#7792=ORIENTED_EDGE ( 'NONE', *, *, #29662, .T. ) ;
#7795=ADVANCED_FACE ( 'NONE', ( #25608 ), #22627, .T. ) ;
#7797=CARTESIAN_POINT ( 'NONE',  ( 0.000000000000000000, 7.008469740302810891, 2.257469275785292329 ) ) ;
#7802=DIRECTION ( 'NONE',  ( 1.000000000000000000, -0.000000000000000000, -0.000000000000000000 ) ) ;
#7804=CARTESIAN_POINT ( 'NONE',  ( 5.887529311434773760, 0.3723788567094480362, -8.386653846779015709 ) ) ;
#7805=CARTESIAN_POINT ( 'NONE',  ( -2.473317512238808025, -0.04024842339950747416, 3.068583371689424855 ) ) ;
#7813=DIRECTION ( 'NONE',  ( -1.000000000000000000, -0.000000000000000000, -0.000000000000000000 ) ) ;
#7817=CARTESIAN_POINT ( 'NONE',  ( -8.000050800000012785, -0.1176501200716436601, 3.189834295598466873 ) ) ;
#7822=CARTESIAN_POINT ( 'NONE',  ( -5.112550801365594033, -3.675193018007246071, 1.088641768524163167 ) ) ;
#7825=CARTESIAN_POINT ( 'NONE',  ( -4.704531657079158435, -2.975847129947406522, -0.3127741368606805072 ) ) ;
#7838=CARTESIAN_POINT ( 'NONE',  ( 7.249760686538667009, -5.151476664237518044, 6.139290821770238438 ) ) ;
#7841=CARTESIAN_POINT ( 'NONE',  ( -8.000050800000003903, -0.2821670390570966691, -3.000056433408583079 ) ) ;
#7844=CARTESIAN_POINT ( 'NONE',  ( 0.000000000000000000, 0.000000000000000000, 0.000000000000000000 ) ) ;
#7847=CARTESIAN_POINT ( 'NONE',  ( -5.812550801365592434, -3.368539882008727115, -1.828967928396028064 ) ) ;
#7848=CARTESIAN_POINT ( 'NONE',  ( 0.000000000000000000, 0.000000000000000000, 0.000000000000000000 ) ) ;
#7849=CARTESIAN_POINT ( 'NONE',  ( 5.377543748152547209, 1.391664247347333294, -7.892520144992419162 ) ) ;
#7850=CYLINDRICAL_SURFACE ( 'NONE', #1124, 2.999999999999999112 ) ;
#7861=ADVANCED_FACE ( 'NONE', ( #5721 ), #531, .F. ) ;
#7867=ORIENTED_EDGE ( 'NONE', *, *, #826, .T. ) ;
#7873=ORIENTED_EDGE ( 'NONE', *, *, #28557, .F. ) ;
#7875=CARTESIAN_POINT ( 'NONE',  ( -6.212550801365593678, 3.368539882008727115, 1.828967928396027176 ) ) ;
#7876=CARTESIAN_POINT ( 'NONE',  ( 7.249760686538667009, 0.000000000000000000, 0.000000000000000000 ) ) ;
#7894=ORIENTED_EDGE ( 'NONE', *, *, #27846, .T. ) ;
#7896=LINE ( 'NONE', #4897, #28978 ) ;
#7897=CARTESIAN_POINT ( 'NONE',  ( -2.587550801365593678, 0.3701630799359330593, -3.521866450007987037 ) ) ;
#7898=VERTEX_POINT ( 'NONE', #10718 ) ;
#7901=CARTESIAN_POINT ( 'NONE',  ( 7.249760686538667009, 7.199384779417189684, -4.973063321323801134 ) ) ;
#7911=ADVANCED_FACE ( 'NONE', ( #13712 ), #8869, .T. ) ;
#7920=B_SPLINE_CURVE_WITH_KNOTS ( 'NONE', 3,
 ( #4787, #27182, #22695, #14963, #32397, #4288, #14464, #24679, #1805, #11990 ),
 .UNSPECIFIED., .F., .F.,
 ( 4, 2, 2, 2, 4 ),
 ( 1.968338519012299431E-07, 0.0005467928198071724975, 0.001093388805762443789, 0.001639984791717714972, 0.002186580777672986371 ),
 .UNSPECIFIED. ) ;
#7922=DIRECTION ( 'NONE',  ( 0.000000000000000000, 0.000000000000000000, 1.000000000000000000 ) ) ;
#7925=DIRECTION ( 'NONE',  ( 0.000000000000000000, 0.5877852522924689183, 0.8090169943749504489 ) ) ;
#7928=CARTESIAN_POINT ( 'NONE',  ( 7.249760686538667009, -2.741043480754877582, -7.530955069117540646 ) ) ;
#7933=CARTESIAN_POINT ( 'NONE',  ( 7.249760686538667009, -6.147671362329260702, 6.226446564517894799 ) ) ;
#7934=CARTESIAN_POINT ( 'NONE',  ( 6.356381935169121533, -8.556754636093200972, -0.9265622495396655944 ) ) ;
#7939=CARTESIAN_POINT ( 'NONE',  ( -5.137550801365594388, -3.368539882008727115, -1.828967928396028064 ) ) ;
#7942=ORIENTED_EDGE ( 'NONE', *, *, #5491, .F. ) ;
#7944=EDGE_CURVE ( 'NONE', #11273, #27732, #4228, .T. ) ;
#7949=EDGE_LOOP ( 'NONE', ( #6973, #10784, #20905 ) ) ;
#7965=DIRECTION ( 'NONE',  ( 1.000000000000000000, 0.000000000000000000, 0.000000000000000000 ) ) ;
#7971=CARTESIAN_POINT ( 'NONE',  ( 5.377543748152548986, -6.139290821770219786, -5.151476664237539360 ) ) ;
#7972=ORIENTED_EDGE ( 'NONE', *, *, #28359, .F. ) ;
#7973=VERTEX_POINT ( 'NONE', #9871 ) ;
#7974=CARTESIAN_POINT ( 'NONE',  ( -2.804531657079157636, 2.325406398514293205, -1.883076972206379374 ) ) ;
#7991=ORIENTED_EDGE ( 'NONE', *, *, #17433, .T. ) ;
#8000=CARTESIAN_POINT ( 'NONE',  ( -7.212550801365592790, 1.828967928396027176, -3.368539882008727115 ) ) ;
#8005=ORIENTED_EDGE ( 'NONE', *, *, #17075, .T. ) ;
#8026=VERTEX_POINT ( 'NONE', #10182 ) ;
#8027=ORIENTED_EDGE ( 'NONE', *, *, #11934, .F. ) ;
#8029=FACE_OUTER_BOUND ( 'NONE', #32427, .T. ) ;
#8030=CARTESIAN_POINT ( 'NONE',  ( 4.749760686538667009, 7.530955069117513112, 2.741043480754951744 ) ) ;
#8031=EDGE_CURVE ( 'NONE', #4152, #10433, #4114, .T. ) ;
#8045=ORIENTED_EDGE ( 'NONE', *, *, #11358, .F. ) ;
#8046=DIRECTION ( 'NONE',  ( 0.000000000000000000, 0.08715574274765046370, 0.9961946980917462113 ) ) ;
#8051=CARTESIAN_POINT ( 'NONE',  ( 5.377543748152548986, 6.940565734314653845, -4.007137495034738706 ) ) ;
#8052=FACE_OUTER_BOUND ( 'NONE', #13600, .T. ) ;
#8054=CARTESIAN_POINT ( 'NONE',  ( 7.249760686538667009, -6.226446564517873483, -6.147671362329282019 ) ) ;
#8055=DIRECTION ( 'NONE',  ( 0.000000000000000000, 0.8191520442889884679, 0.5735764363510509334 ) ) ;
#8057=DIRECTION ( 'NONE',  ( -1.000000000000000000, -0.000000000000000000, -0.000000000000000000 ) ) ;
#8075=DIRECTION ( 'NONE',  ( -1.000000000000000000, -0.000000000000000000, -0.000000000000000000 ) ) ;
#8077=CARTESIAN_POINT ( 'NONE',  ( 6.524595551582242692, -3.779376390944526598, 7.790581746767720084 ) ) ;
#8078=ORIENTED_EDGE ( 'NONE', *, *, #31484, .F. ) ;
#8083=CARTESIAN_POINT ( 'NONE',  ( 7.249760686538667009, -7.892520144992426268, -1.391664247347309535 ) ) ;
#8086=CARTESIAN_POINT ( 'NONE',  ( -6.650050800000001594, 2.853674364686379583, 1.549418761218565921 ) ) ;
#8092=DIRECTION ( 'NONE',  ( -1.000000000000000000, -0.000000000000000000, -0.000000000000000000 ) ) ;
#8093=ORIENTED_EDGE ( 'NONE', *, *, #22719, .T. ) ;
#8094=CARTESIAN_POINT ( 'NONE',  ( 6.530491751506347420, -6.030130624359216540, 6.216163082443046051 ) ) ;
#8098=DIRECTION ( 'NONE',  ( -1.000000000000000000, 0.000000000000000000, -0.000000000000000000 ) ) ;
#8121=CARTESIAN_POINT ( 'NONE',  ( -2.393873106538427553, 0.6788706457666772165, 3.182475034827832339 ) ) ;
#8128=DIRECTION ( 'NONE',  ( -1.000000000000000000, -0.000000000000000000, 0.000000000000000000 ) ) ;
#8132=CYLINDRICAL_SURFACE ( 'NONE', #27782, 2.999999999999999112 ) ;
#8136=DIRECTION ( 'NONE',  ( 0.000000000000000000, 0.000000000000000000, -1.000000000000000000 ) ) ;
#8137=FACE_OUTER_BOUND ( 'NONE', #4716, .T. ) ;
#8140=CARTESIAN_POINT ( 'NONE',  ( 7.249760686538667009, 0.000000000000000000, 0.000000000000000000 ) ) ;
#8144=CARTESIAN_POINT ( 'NONE',  ( -4.062550801365593323, 0.3701630799359330593, -3.521866450007987037 ) ) ;
#8145=EDGE_LOOP ( 'NONE', ( #25979, #30005, #2409 ) ) ;
#8147=AXIS2_PLACEMENT_3D ( 'NONE', #16421, #4077, #17078 ) ;
#8148=CIRCLE ( 'NONE', #26819, 8.750000000000000000 ) ;
#8149=CARTESIAN_POINT ( 'NONE',  ( -8.100050800000001772, -0.3135853898029607456, 2.983565686104819648 ) ) ;
#8153=CARTESIAN_POINT ( 'NONE',  ( 7.249760686538667009, 0.000000000000000000, 0.000000000000000000 ) ) ;
#8155=AXIS2_PLACEMENT_3D ( 'NONE', #15723, #29089, #23393 ) ;
#8162=EDGE_CURVE ( 'NONE', #10245, #4314, #26845, .T. ) ;
#8172=ADVANCED_FACE ( 'NONE', ( #14440 ), #4457, .F. ) ;
#8179=ORIENTED_EDGE ( 'NONE', *, *, #7010, .F. ) ;
#8180=CARTESIAN_POINT ( 'NONE',  ( -6.112550801365593145, 1.088641768524161613, 3.675193018007247403 ) ) ;
#8183=CIRCLE ( 'NONE', #23123, 2.999999999999999556 ) ;
#8186=EDGE_CURVE ( 'NONE', #15425, #24311, #29849, .T. ) ;
#8194=DIRECTION ( 'NONE',  ( -0.000000000000000000, 0.8191520442889912434, -0.5735764363510468256 ) ) ;
#8196=AXIS2_PLACEMENT_3D ( 'NONE', #2642, #32919, #30579 ) ;
#8209=FACE_OUTER_BOUND ( 'NONE', #18531, .T. ) ;
#8215=EDGE_LOOP ( 'NONE', ( #29318, #1455, #1676, #2419 ) ) ;
#8217=CARTESIAN_POINT ( 'NONE',  ( 7.249760686538667009, -5.151476664237435443, -6.139290821770307716 ) ) ;
#8218=CARTESIAN_POINT ( 'NONE',  ( -5.362550801365593145, 2.228590825266444142, 2.752080473201636845 ) ) ;
#8227=AXIS2_PLACEMENT_3D ( 'NONE', #15257, #25306, #22790 ) ;
#8232=CIRCLE ( 'NONE', #26373, 0.5000000000000004441 ) ;
#8242=DIRECTION ( 'NONE',  ( -1.000000000000000000, 0.000000000000000000, 0.000000000000000000 ) ) ;
#8243=ORIENTED_EDGE ( 'NONE', *, *, #27688, .F. ) ;
#8244=ADVANCED_FACE ( 'NONE', ( #29693 ), #30353, .T. ) ;
#8245=CIRCLE ( 'NONE', #19464, 3.000000000000000000 ) ;
#8263=VERTEX_POINT ( 'NONE', #25153 ) ;
#8271=CARTESIAN_POINT ( 'NONE',  ( -6.750050800000001239, 3.113457007523260156, -0.9222479816126439855 ) ) ;
#8275=CARTESIAN_POINT ( 'NONE',  ( 5.885541838704151374, 5.105720535585501096, -6.662285765435168372 ) ) ;
#8278=CYLINDRICAL_SURFACE ( 'NONE', #5986, 2.999999999999999112 ) ;
#8279=EDGE_CURVE ( 'NONE', #13240, #15674, #15040, .T. ) ;
#8285=CARTESIAN_POINT ( 'NONE',  ( 6.749760686538667009, 0.000000000000000000, 0.000000000000000000 ) ) ;
#8292=ORIENTED_EDGE ( 'NONE', *, *, #25745, .F. ) ;
#8296=CARTESIAN_POINT ( 'NONE',  ( 6.883866357751288412, 0.6899766464188887838, -8.704251636488454125 ) ) ;
#8300=CARTESIAN_POINT ( 'NONE',  ( 3.499999999999999556, -1.471047635026914380, 6.892461014225956362 ) ) ;
#8304=CARTESIAN_POINT ( 'NONE',  ( 4.749760686538667009, -7.892520144992426268, -1.391664247347309535 ) ) ;
#8307=CARTESIAN_POINT ( 'NONE',  ( -6.850050802731187716, 2.331437884370912705, -1.887961173149511618 ) ) ;
#8311=CARTESIAN_POINT ( 'NONE',  ( 7.249760686538667009, -6.139290821770289064, 5.151476664237455871 ) ) ;
#8313=CARTESIAN_POINT ( 'NONE',  ( -3.912550801365593856, 3.675193018007247403, -1.088641768524161391 ) ) ;
#8315=CARTESIAN_POINT ( 'NONE',  ( -3.804531657079157636, -1.883076972206379818, -2.325406398514292761 ) ) ;
#8317=FACE_OUTER_BOUND ( 'NONE', #28674, .T. ) ;
#8329=ORIENTED_EDGE ( 'NONE', *, *, #2436, .T. ) ;
#8335=EDGE_LOOP ( 'NONE', ( #5558, #15328, #5016, #17366 ) ) ;
#8336=CARTESIAN_POINT ( 'NONE',  ( -2.612550801365594477, -3.368539882008727115, -1.828967928396028064 ) ) ;
#8337=ADVANCED_FACE ( 'NONE', ( #2599 ), #15938, .F. ) ;
#8346=EDGE_CURVE ( 'NONE', #10694, #26222, #7784, .T. ) ;
#8347=DIRECTION ( 'NONE',  ( 0.000000000000000000, -0.5735764363510537089, 0.8191520442889864695 ) ) ;
#8353=CARTESIAN_POINT ( 'NONE',  ( 6.037141848526922594, -2.473100090966218190, 8.105561522824304532 ) ) ;
#8357=ORIENTED_EDGE ( 'NONE', *, *, #19047, .F. ) ;
#8363=ORIENTED_EDGE ( 'NONE', *, *, #24697, .F. ) ;
#8365=CARTESIAN_POINT ( 'NONE',  ( -5.762550801365593500, -2.228590825266444586, -2.752080473201636401 ) ) ;
#8368=CARTESIAN_POINT ( 'NONE',  ( 6.037141848526922594, 7.798898458906324827, -3.315649934461640136 ) ) ;
#8370=CARTESIAN_POINT ( 'NONE',  ( -6.037550801365592967, -3.675193018007246071, 1.088641768524163167 ) ) ;
#8376=ADVANCED_FACE ( 'NONE', ( #25492 ), #8278, .T. ) ;
#8378=ORIENTED_EDGE ( 'NONE', *, *, #5183, .T. ) ;
#8379=FACE_OUTER_BOUND ( 'NONE', #21535, .T. ) ;
#8382=EDGE_CURVE ( 'NONE', #6843, #32892, #30525, .T. ) ;
#8383=EDGE_CURVE ( 'NONE', #12214, #19072, #22190, .T. ) ;
#8390=ORIENTED_EDGE ( 'NONE', *, *, #10708, .T. ) ;
#8399=DIRECTION ( 'NONE',  ( 0.000000000000000000, 0.9659258262890668689, 0.2588190451025257910 ) ) ;
#8400=ORIENTED_EDGE ( 'NONE', *, *, #25584, .F. ) ;
#8406=CARTESIAN_POINT ( 'NONE',  ( -5.850050802731187716, 1.887961173149511618, 2.331437884370912705 ) ) ;
#8407=CARTESIAN_POINT ( 'NONE',  ( 7.249760686538667009, -3.748318449932352081, 7.906491560603652324 ) ) ;
#8409=ORIENTED_EDGE ( 'NONE', *, *, #1022, .T. ) ;
#8413=CARTESIAN_POINT ( 'NONE',  ( -2.500050800000000351, -0.3135853898029607456, 2.983565686104819648 ) ) ;
#8415=EDGE_CURVE ( 'NONE', #8879, #29777, #12401, .T. ) ;
#8417=FACE_OUTER_BOUND ( 'NONE', #7949, .T. ) ;
#8419=CARTESIAN_POINT ( 'NONE',  ( 7.249760686538667009, -6.940565734314625423, 4.007137495034787555 ) ) ;
#8424=FACE_OUTER_BOUND ( 'NONE', #24589, .T. ) ;
#8425=CARTESIAN_POINT ( 'NONE',  ( 4.749760686538667009, -6.940565734314570356, -4.007137495034885255 ) ) ;
#8431=CARTESIAN_POINT ( 'NONE',  ( 6.883866621640342132, 7.111352071735089098, -5.066432324612653915 ) ) ;
#8434=ORIENTED_EDGE ( 'NONE', *, *, #22489, .T. ) ;
#8437=EDGE_LOOP ( 'NONE', ( #31344, #6953, #13771 ) ) ;
#8441=CARTESIAN_POINT ( 'NONE',  ( -7.400050800000000706, 1.887961173149511618, 2.331437884370912705 ) ) ;
#8446=ADVANCED_FACE ( 'NONE', ( #21293 ), #21781, .T. ) ;
#8451=ADVANCED_FACE ( 'NONE', ( #8424 ), #6097, .T. ) ;
#8452=CARTESIAN_POINT ( 'NONE',  ( 3.499999999999999556, 6.704570150426983233, 2.172265885002680808 ) ) ;
#8455=CARTESIAN_POINT ( 'NONE',  ( -6.962942409646511344, 7.727249047114547632E-16, -2.999999999999999556 ) ) ;
#8456=DIRECTION ( 'NONE',  ( 1.000000000000000000, -0.000000000000000000, -0.000000000000000000 ) ) ;
#8460=CARTESIAN_POINT ( 'NONE',  ( -4.112550801365593145, -1.088641768524163389, -3.675193018007246071 ) ) ;
#8462=CARTESIAN_POINT ( 'NONE',  ( -5.300050800000001061, 0.3135853898029611342, -2.983565686104819648 ) ) ;
#8464=CARTESIAN_POINT ( 'NONE',  ( -4.957304906975410042, 1.062355717592091686, 3.000000000000001332 ) ) ;
#8481=ORIENTED_EDGE ( 'NONE', *, *, #10579, .F. ) ;
#8482=CARTESIAN_POINT ( 'NONE',  ( -2.762550801365593500, -2.752080473201636845, 2.228590825266444586 ) ) ;
#8493=CARTESIAN_POINT ( 'NONE',  ( -8.000050800000000351, 0.000000000000000000, 0.000000000000000000 ) ) ;
#8497=CARTESIAN_POINT ( 'NONE',  ( -2.249956573341760357, 1.323625320507108460, 3.284597389080124774 ) ) ;
#8501=CARTESIAN_POINT ( 'NONE',  ( 6.880159540721328959, -2.328896285337246130, 8.414807581959454552 ) ) ;
#8515=CARTESIAN_POINT ( 'NONE',  ( 4.749760686538667009, 6.940565734314653845, -4.007137495034738706 ) ) ;
#8516=CARTESIAN_POINT ( 'NONE',  ( -3.612550801365593589, -1.828967928396026732, 3.368539882008728004 ) ) ;
#8519=ORIENTED_EDGE ( 'NONE', *, *, #28359, .T. ) ;
#8520=CARTESIAN_POINT ( 'NONE',  ( -8.187550801365594211, 0.3701630799359330593, -3.521866450007987037 ) ) ;
#8526=EDGE_CURVE ( 'NONE', #16840, #30035, #5433, .T. ) ;
#8536=DIRECTION ( 'NONE',  ( 0.000000000000000000, 0.7071067811865495711, -0.7071067811865454633 ) ) ;
#8537=CARTESIAN_POINT ( 'NONE',  ( -5.437550801365592434, 1.088641768524161613, 3.675193018007247403 ) ) ;
#8546=FACE_OUTER_BOUND ( 'NONE', #26869, .T. ) ;
#8548=CARTESIAN_POINT ( 'NONE',  ( -7.800050800000000173, -1.887961173149512062, -2.331437884370912261 ) ) ;
#8550=EDGE_LOOP ( 'NONE', ( #29636, #16787, #27787, #15146 ) ) ;
#8551=ORIENTED_EDGE ( 'NONE', *, *, #7509, .F. ) ;
#8556=CARTESIAN_POINT ( 'NONE',  ( -5.950050802731187360, 2.983565686104819648, 0.3135853898029609677 ) ) ;
#8557=CARTESIAN_POINT ( 'NONE',  ( 3.499999999999999556, -2.652816298622462376, 5.657964889053574531 ) ) ;
#8559=CARTESIAN_POINT ( 'NONE',  ( 4.749760686538667009, 6.940565734314653845, -4.007137495034738706 ) ) ;
#8566=CARTESIAN_POINT ( 'NONE',  ( -3.050050802731187449, -1.887961173149512062, -2.331437884370912261 ) ) ;
#8571=ADVANCED_FACE ( 'NONE', ( #7392 ), #4578, .F. ) ;
#8573=CYLINDRICAL_SURFACE ( 'NONE', #22002, 6.248999999999999666 ) ;
#8575=CARTESIAN_POINT ( 'NONE',  ( 7.249760686538667009, 3.647351267791679508, -7.953573330858177748 ) ) ;
#8579=FACE_OUTER_BOUND ( 'NONE', #15091, .T. ) ;
#8586=ORIENTED_EDGE ( 'NONE', *, *, #2080, .T. ) ;
#8608=VECTOR ( 'NONE', #25913, 999.9999999999998863 ) ;
#8613=DIRECTION ( 'NONE',  ( 0.000000000000000000, 0.000000000000000000, -1.000000000000000000 ) ) ;
#8616=EDGE_CURVE ( 'NONE', #1245, #28881, #26814, .T. ) ;
#8617=CARTESIAN_POINT ( 'NONE',  ( 7.249760686538667009, 7.953573330858214163, 3.647351267791597795 ) ) ;
#8622=CARTESIAN_POINT ( 'NONE',  ( -4.962550801365593678, -2.228590825266444586, -2.752080473201636401 ) ) ;
#8624=CARTESIAN_POINT ( 'NONE',  ( -6.450050800000000528, -1.549418761218565477, 2.853674364686380471 ) ) ;
#8637=ADVANCED_FACE ( 'NONE', ( #20124 ), #2064, .T. ) ;
#8648=CARTESIAN_POINT ( 'NONE',  ( -8.000050800000000351, 0.000000000000000000, -3.000000000000000444 ) ) ;
#8652=CARTESIAN_POINT ( 'NONE',  ( -3.862550801365593145, 3.521866450007987037, 0.3701630799359328372 ) ) ;
#8653=AXIS2_PLACEMENT_3D ( 'NONE', #7424, #4265, #4944 ) ;
#8660=DIRECTION ( 'NONE',  ( 0.000000000000000000, 0.5877852522924689183, 0.8090169943749503378 ) ) ;
#8662=AXIS2_PLACEMENT_3D ( 'NONE', #17846, #28046, #28358 ) ;
#8667=DIRECTION ( 'NONE',  ( 0.000000000000000000, 0.000000000000000000, -1.000000000000000000 ) ) ;
#8668=ORIENTED_EDGE ( 'NONE', *, *, #29780, .T. ) ;
#8670=CARTESIAN_POINT ( 'NONE',  ( 6.356382228872878848, 2.398350474622056083, -8.265862592379898288 ) ) ;
#8671=DIRECTION ( 'NONE',  ( 0.000000000000000000, 0.000000000000000000, 1.000000000000000000 ) ) ;
#8672=CARTESIAN_POINT ( 'NONE',  ( -4.837550801365592790, 3.675193018007246959, -1.088641768524161391 ) ) ;
#8691=DIRECTION ( 'NONE',  ( 1.000000000000000000, -0.000000000000000000, 0.000000000000000000 ) ) ;
#8692=CARTESIAN_POINT ( 'NONE',  ( -4.812550801365593323, 1.828967928396027398, -3.368539882008727115 ) ) ;
#8694=AXIS2_PLACEMENT_3D ( 'NONE', #14264, #24459, #6757 ) ;
#8698=CARTESIAN_POINT ( 'NONE',  ( -5.587550801365593678, 3.521866450007987037, 0.3701630799359328372 ) ) ;
#8712=CIRCLE ( 'NONE', #9762, 8.750000000000000000 ) ;
#8713=DIRECTION ( 'NONE',  ( 0.000000000000000000, -0.4226182617407076014, 0.9063077870366462729 ) ) ;
#8719=CARTESIAN_POINT ( 'NONE',  ( -4.487550801365593145, -2.752080473201636845, 2.228590825266444586 ) ) ;
#8721=ADVANCED_FACE ( 'NONE', ( #5229 ), #30674, .F. ) ;
#8729=CARTESIAN_POINT ( 'NONE',  ( 3.499999999999999556, 7.008469740302810891, -0.7425307242147067832 ) ) ;
#8731=( BOUNDED_CURVE ( )  B_SPLINE_CURVE ( 2, ( #10391, #15054, #17917, #20599, #2544, #25272, #28443, #13204, #28257, #28108, #5206, #23406, #511, #10041, #20252, #15382, #7371, #20429, #25589, #12561, #22765, #5367, #32973, #12871, #23094, #7533, #17741, #15552, #22915, #10540, #27948, #365, #5055, #15232, #2700, #25435, #30807, #7875, #18067, #13062, #23263, #20751, #16372, #26581, #5843, #20908, #8365, #23567, #21239, #16028, #26256, #8852, #31437, #14026, #8218, #18417, #26734, #21575, #3851, #3682, #24050, #23897, #29250, #13842, #3373, #8692, #6334, #13538, #23749, #16523, #1355, #28608, #16220, #31781, #862, #18716, #6025, #24237, #5702, #21396, #1174, #31131, #11039, #28754, #3195, #31603, #10883, #18561, #15882, #8516, #19059, #3538, #26091, #13357, #28919, #26438, #691, #13695, #1006, #21091, #31292, #11189, #18907, #29100, #6187, #11374, #11529, #9499, #19556, #7186, #19714, #4339, #16710, #24731, #12033, #32286, #17019, #11859, #14518, #29754, #9000 ),
 .UNSPECIFIED., .F., .F. ) 
 B_SPLINE_CURVE_WITH_KNOTS ( ( 3, 2, 2, 2, 2, 2, 2, 2, 2, 2, 2, 2, 2, 2, 2, 2, 2, 2, 2, 2, 2, 2, 2, 2, 2, 2, 2, 2, 2, 2, 2, 2, 2, 2, 2, 2, 2, 2, 2, 2, 2, 2, 2, 2, 2, 2, 2, 2, 2, 2, 2, 2, 2, 2, 2, 2, 2, 2, 2, 2, 3 ),
 ( 0.009695607697749946546, 0.01562500000000000000, 0.03125000000000000000, 0.04687500000000000000, 0.06250000000000000000, 0.07812500000000001388, 0.09375000000000000000, 0.1093750000000000000, 0.1250000000000000000, 0.1406250000000000000, 0.1562500000000000000, 0.1718750000000000000, 0.1875000000000000000, 0.2031250000000000000, 0.2187500000000000000, 0.2343749999999999722, 0.2500000000000000000, 0.2656250000000000000, 0.2812500000000000000, 0.2968750000000000000, 0.3125000000000000000, 0.3281250000000000000, 0.3437500000000000000, 0.3593750000000000000, 0.3750000000000000000, 0.3906250000000000000, 0.4062500000000000000, 0.4218750000000000555, 0.4375000000000000000, 0.4531250000000000000, 0.4687500000000000000, 0.4843750000000000000, 0.4999999999999999445, 0.5156250000000000000, 0.5312500000000000000, 0.5468750000000000000, 0.5625000000000000000, 0.5781250000000000000, 0.5937500000000000000, 0.6093750000000000000, 0.6250000000000000000, 0.6406250000000000000, 0.6562500000000000000, 0.6718750000000000000, 0.6875000000000000000, 0.7031250000000000000, 0.7187500000000000000, 0.7343750000000000000, 0.7500000000000000000, 0.7656250000000000000, 0.7812500000000000000, 0.7968750000000000000, 0.8125000000000000000, 0.8281250000000000000, 0.8437500000000000000, 0.8593750000000000000, 0.8750000000000000000, 0.8906250000000001110, 0.9062500000000000000, 0.9218750000000000000, 0.9278186525000968743 ),
 .UNSPECIFIED. ) 
 CURVE ( )  GEOMETRIC_REPRESENTATION_ITEM ( )  RATIONAL_B_SPLINE_CURVE ( ( 0.9641510359188718571, 0.9711137207058399001, 1.000000000000000000, 0.9238795325112867385, 1.000000000000000000, 0.9238795325112867385, 1.000000000000000000, 0.9238795325112867385, 1.000000000000000000, 0.9238795325112867385, 1.000000000000000000, 0.9238795325112867385, 1.000000000000000000, 0.9238795325112867385, 1.000000000000000000, 0.9238795325112867385, 1.000000000000000000, 0.9238795325112867385, 1.000000000000000000, 0.9238795325112867385, 1.000000000000000000, 0.9238795325112867385, 1.000000000000000000, 0.9238795325112867385, 1.000000000000000000, 0.9238795325112867385, 1.000000000000000000, 0.9238795325112867385, 1.000000000000000000, 0.9238795325112867385, 1.000000000000000000, 0.9238795325112867385, 1.000000000000000000, 0.9238795325112867385, 1.000000000000000000, 0.9238795325112867385, 1.000000000000000000, 0.9238795325112867385, 1.000000000000000000, 0.9238795325112867385, 1.000000000000000000, 0.9238795325112867385, 1.000000000000000000, 0.9238795325112867385, 1.000000000000000000, 0.9238795325112867385, 1.000000000000000000, 0.9238795325112867385, 1.000000000000000000, 0.9238795325112867385, 1.000000000000000000, 0.9238795325112867385, 1.000000000000000000, 0.9238795325112867385, 1.000000000000000000, 0.9238795325112867385, 1.000000000000000000, 0.9238795325112867385, 1.000000000000000000, 0.9238795325112867385, 1.000000000000000000, 0.9238795325112867385, 1.000000000000000000, 0.9238795325112867385, 1.000000000000000000, 0.9238795325112867385, 1.000000000000000000, 0.9238795325112867385, 1.000000000000000000, 0.9238795325112867385, 1.000000000000000000, 0.9238795325112867385, 1.000000000000000000, 0.9238795325112867385, 1.000000000000000000, 0.9238795325112867385, 1.000000000000000000, 0.9238795325112867385, 1.000000000000000000, 0.9238795325112867385, 1.000000000000000000, 0.9238795325112867385, 1.000000000000000000, 0.9238795325112867385, 1.000000000000000000, 0.9238795325112867385, 1.000000000000000000, 0.9238795325112867385, 1.000000000000000000, 0.9238795325112867385, 1.000000000000000000, 0.9238795325112867385, 1.000000000000000000, 0.9238795325112867385, 1.000000000000000000, 0.9238795325112867385, 1.000000000000000000, 0.9238795325112867385, 1.000000000000000000, 0.9238795325112867385, 1.000000000000000000, 0.9238795325112867385, 1.000000000000000000, 0.9238795325112867385, 1.000000000000000000, 0.9238795325112867385, 1.000000000000000000, 0.9238795325112867385, 1.000000000000000000, 0.9238795325112867385, 1.000000000000000000, 0.9238795325112867385, 1.000000000000000000, 0.9238795325112867385, 1.000000000000000000, 0.9238795325112867385, 1.000000000000000000, 0.9238795325112867385, 1.000000000000000000, 0.9710442491585387081, 0.9641176721898496726 ) ) 
 REPRESENTATION_ITEM ( '' )  );
#8737=CARTESIAN_POINT ( 'NONE',  ( -8.000050800000000351, 2.857870525728205990, -2.169999637890065003 ) ) ;
#8739=AXIS2_PLACEMENT_3D ( 'NONE', #8285, #10286, #31022 ) ;
#8740=CARTESIAN_POINT ( 'NONE',  ( -5.762942409646513831, 3.284080845023683730E-15, 3.000000000000000000 ) ) ;
#8743=DIRECTION ( 'NONE',  ( 0.000000000000000000, -0.2588190451025286221, 0.9659258262890662028 ) ) ;
#8745=EDGE_CURVE ( 'NONE', #17772, #26254, #10283, .T. ) ;
#8759=EDGE_CURVE ( 'NONE', #8809, #10694, #20623, .T. ) ;
#8769=ORIENTED_EDGE ( 'NONE', *, *, #20666, .F. ) ;
#8774=ORIENTED_EDGE ( 'NONE', *, *, #3502, .T. ) ;
#8782=CARTESIAN_POINT ( 'NONE',  ( 4.749760686538667009, -5.151476664237518044, 6.139290821770238438 ) ) ;
#8785=CARTESIAN_POINT ( 'NONE',  ( 7.249760686538667009, -0.7071067811865734409, 8.721381771256202953 ) ) ;
#8796=EDGE_CURVE ( 'NONE', #16327, #22347, #7750, .T. ) ;
#8799=CARTESIAN_POINT ( 'NONE',  ( -3.262550801365593056, 0.3701630799359330593, -3.521866450007987037 ) ) ;
#8801=CARTESIAN_POINT ( 'NONE',  ( -5.350050800000001772, -0.9222479816126459840, -3.113457007523259268 ) ) ;
#8802=( BOUNDED_CURVE ( )  B_SPLINE_CURVE ( 2, ( #21762, #31971, #21440, #21612, #3419, #6073, #8556, #19257, #8406, #5887, #8740 ),
 .UNSPECIFIED., .F., .F. ) 
 B_SPLINE_CURVE_WITH_KNOTS ( ( 3, 2, 2, 2, 2, 3 ),
 ( 0.2478822619934377414, 0.2500000000000000000, 0.2656250000000000000, 0.2812500000000000000, 0.2968750000000000000, 0.3103822619934377136 ),
 .UNSPECIFIED. ) 
 CURVE ( )  GEOMETRIC_REPRESENTATION_ITEM ( )  RATIONAL_B_SPLINE_CURVE ( ( 0.9821626249036861100, 0.9896829947469993893, 1.000000000000000000, 0.9238795325112867385, 1.000000000000000000, 0.9238795325112867385, 1.000000000000000000, 0.9238795325112867385, 1.000000000000000000, 0.9341965377642874602, 0.9821626249036857770 ) ) 
 REPRESENTATION_ITEM ( '' )  );
#8803=VECTOR ( 'NONE', #6200, 1000.000000000000000 ) ;
#8808=CARTESIAN_POINT ( 'NONE',  ( 3.499999999999999556, 0.000000000000000000, 0.000000000000000000 ) ) ;
#8809=VERTEX_POINT ( 'NONE', #10413 ) ;
#8813=EDGE_CURVE ( 'NONE', #29082, #23972, #7896, .T. ) ;
#8819=VERTEX_POINT ( 'NONE', #28281 ) ;
#8823=DIRECTION ( 'NONE',  ( 0.000000000000000000, 0.5735764363510378328, 0.8191520442889975717 ) ) ;
#8831=DIRECTION ( 'NONE',  ( 0.000000000000000000, 0.9961946980917454342, 0.08715574274765873486 ) ) ;
#8837=CARTESIAN_POINT ( 'NONE',  ( -2.069657272239051160, 1.153746456547815269, 3.257691561679774139 ) ) ;
#8838=CARTESIAN_POINT ( 'NONE',  ( -2.737550801365594033, -3.368539882008727115, -1.828967928396027842 ) ) ;
#8843=ORIENTED_EDGE ( 'NONE', *, *, #8186, .T. ) ;
#8845=CARTESIAN_POINT ( 'NONE',  ( 7.249760686538667009, 0.000000000000000000, 5.500000000000000000 ) ) ;
#8846=CARTESIAN_POINT ( 'NONE',  ( -3.500050802731187627, 2.853674364686379583, 1.549418761218565921 ) ) ;
#8852=CARTESIAN_POINT ( 'NONE',  ( -5.512550801365594388, 3.675193018007246959, -1.088641768524161391 ) ) ;
#8855=CARTESIAN_POINT ( 'NONE',  ( 0.000000000000000000, 7.008469740302810891, -0.7425307242147067832 ) ) ;
#8857=CARTESIAN_POINT ( 'NONE',  ( -7.537550801365592967, -3.368539882008727115, -1.828967928396028064 ) ) ;
#8863=DIRECTION ( 'NONE',  ( 0.000000000000000000, 0.9961946980917448791, 0.08715574274766618723 ) ) ;
#8866=EDGE_CURVE ( 'NONE', #25021, #21409, #2924, .T. ) ;
#8868=CARTESIAN_POINT ( 'NONE',  ( 6.883866482134012976, -0.8319830743950079599, -8.691827696555167293 ) ) ;
#8869=CYLINDRICAL_SURFACE ( 'NONE', #15015, 6.248999999999999666 ) ;
#8873=CARTESIAN_POINT ( 'NONE',  ( 7.249760686538667009, 8.466096581343512284, -2.210816291636124475 ) ) ;
#8876=CARTESIAN_POINT ( 'NONE',  ( 5.377543748152548986, 7.892520144992453801, -1.391664247347147443 ) ) ;
#8879=VERTEX_POINT ( 'NONE', #26757 ) ;
#8880=CARTESIAN_POINT ( 'NONE',  ( -4.800050800000000173, -2.331437884370912705, 1.887961173149512062 ) ) ;
#8882=DIRECTION ( 'NONE',  ( 0.000000000000000000, 0.9945218953682729568, 0.1045284632676571068 ) ) ;
#8902=DIRECTION ( 'NONE',  ( 0.000000000000000000, -0.5877852522924797984, 0.8090169943749425663 ) ) ;
#8915=CARTESIAN_POINT ( 'NONE',  ( 6.357667873252800028, 3.476490553296956332, -7.873899671211455953 ) ) ;
#8922=EDGE_LOOP ( 'NONE', ( #31980, #5927, #4998 ) ) ;
#8928=CARTESIAN_POINT ( 'NONE',  ( 5.612973690782940395, -0.1996300861631509771, 8.213905076232780544 ) ) ;
#8929=EDGE_CURVE ( 'NONE', #6855, #14402, #23917, .T. ) ;
#8932=CARTESIAN_POINT ( 'NONE',  ( 3.499999999999999556, 0.000000000000000000, 0.000000000000000000 ) ) ;
#8935=FACE_OUTER_BOUND ( 'NONE', #27678, .T. ) ;
#8942=CARTESIAN_POINT ( 'NONE',  ( -4.600050802731187716, -0.9222479816126459840, -3.113457007523259268 ) ) ;
#8945=CARTESIAN_POINT ( 'NONE',  ( -7.200050800000000528, -2.331437884370912705, 1.887961173149512062 ) ) ;
#8961=EDGE_CURVE ( 'NONE', #15643, #136, #3362, .T. ) ;
#8968=CARTESIAN_POINT ( 'NONE',  ( -2.362550801365593589, 2.752080473201636845, -2.228590825266444142 ) ) ;
#8972=DIRECTION ( 'NONE',  ( 0.000000000000000000, 0.9659258262890693114, -0.2588190451025167427 ) ) ;
#8975=CARTESIAN_POINT ( 'NONE',  ( 7.249760686538667009, 8.437262856154164936, 2.318425219014256911 ) ) ;
#8981=EDGE_CURVE ( 'NONE', #18491, #15207, #14052, .T. ) ;
#8982=DIRECTION ( 'NONE',  ( 1.000000000000000000, -0.000000000000000000, -0.000000000000000000 ) ) ;
#8988=DIRECTION ( 'NONE',  ( 0.000000000000000000, 0.000000000000000000, 1.000000000000000000 ) ) ;
#8989=B_SPLINE_CURVE_WITH_KNOTS ( 'NONE', 3,
 ( #16996, #12312, #22038, #12156, #4497, #17172, #22354, #32259, #24868, #27384 ),
 .UNSPECIFIED., .F., .F.,
 ( 4, 2, 2, 2, 4 ),
 ( 1.968338519012285667E-07, 0.0005467926089500455998, 0.001093388384048189993, 0.001639984159146334278, 0.002186579934244478780 ),
 .UNSPECIFIED. ) ;
#8993=EDGE_CURVE ( 'NONE', #19834, #21274, #16697, .T. ) ;
#8995=ORIENTED_EDGE ( 'NONE', *, *, #21617, .F. ) ;
#8996=CARTESIAN_POINT ( 'NONE',  ( 6.357667975083865386, 3.797112024432019339, 7.724391461487803312 ) ) ;
#8997=ORIENTED_EDGE ( 'NONE', *, *, #27733, .F. ) ;
#8998=EDGE_LOOP ( 'NONE', ( #21471, #28554, #26732 ) ) ;
#9000=CARTESIAN_POINT ( 'NONE',  ( -2.124956573341760357, 1.323625320507108460, 3.284597389080124774 ) ) ;
#9005=CARTESIAN_POINT ( 'NONE',  ( -5.187550801365593323, -3.521866450007987037, -0.3701630799359323931 ) ) ;
#9011=ORIENTED_EDGE ( 'NONE', *, *, #3981, .T. ) ;
#9019=CARTESIAN_POINT ( 'NONE',  ( -2.487550801365593589, 2.752080473201636845, -2.228590825266444142 ) ) ;
#9022=AXIS2_PLACEMENT_3D ( 'NONE', #19434, #18880, #16677 ) ;
#9025=CARTESIAN_POINT ( 'NONE',  ( 6.524595126109736576, -2.112519041817556342, -8.397268106035234325 ) ) ;
#9026=CARTESIAN_POINT ( 'NONE',  ( 6.883866601413088482, -7.883091392499345318, 3.754588506078578192 ) ) ;
#9029=EDGE_CURVE ( 'NONE', #25776, #16558, #881, .T. ) ;
#9030=AXIS2_PLACEMENT_3D ( 'NONE', #9043, #7230, #21767 ) ;
#9031=DIRECTION ( 'NONE',  ( 0.000000000000000000, 0.000000000000000000, -1.000000000000000000 ) ) ;
#9039=PLANE ( 'NONE',  #31588 ) ;
#9041=VERTEX_POINT ( 'NONE', #10907 ) ;
#9043=CARTESIAN_POINT ( 'NONE',  ( -8.000050800000000351, 0.000000000000000000, 0.000000000000000000 ) ) ;
#9044=DIRECTION ( 'NONE',  ( 0.000000000000000000, 0.000000000000000000, 1.000000000000000000 ) ) ;
#9047=ORIENTED_EDGE ( 'NONE', *, *, #2273, .T. ) ;
#9048=CARTESIAN_POINT ( 'NONE',  ( 6.524595395369781947, 3.538595500939588856, 7.902859683906627630 ) ) ;
#9049=CIRCLE ( 'NONE', #27748, 6.248999999999999666 ) ;
#9050=VECTOR ( 'NONE', #27991, 1000.000000000000000 ) ;
#9058=CARTESIAN_POINT ( 'NONE',  ( 7.249760686538666121, 7.347880794884119736E-16, -6.000000000000000000 ) ) ;
#9060=ORIENTED_EDGE ( 'NONE', *, *, #1132, .F. ) ;
#9068=EDGE_CURVE ( 'NONE', #9919, #6843, #26313, .T. ) ;
#9077=ORIENTED_EDGE ( 'NONE', *, *, #9029, .T. ) ;
#9082=VERTEX_POINT ( 'NONE', #9368 ) ;
#9086=CARTESIAN_POINT ( 'NONE',  ( 3.499999999999999556, -1.179494851233943598, 6.136676046192483192 ) ) ;
#9092=CARTESIAN_POINT ( 'NONE',  ( 5.887530024394190598, 7.753515897409886115, 3.218326717262283143 ) ) ;
#9099=CARTESIAN_POINT ( 'NONE',  ( -6.400050802731188426, -3.113457007523259268, 0.9222479816126455399 ) ) ;
#9101=CARTESIAN_POINT ( 'NONE',  ( -7.150050800000000706, -3.113457007523259268, 0.9222479816126455399 ) ) ;
#9102=AXIS2_PLACEMENT_3D ( 'NONE', #22415, #26950, #9031 ) ;
#9103=EDGE_CURVE ( 'NONE', #10415, #31571, #9875, .T. ) ;
#9112=CARTESIAN_POINT ( 'NONE',  ( 7.249760686538667009, 6.147671362329219846, 6.226446564517938320 ) ) ;
#9113=EDGE_CURVE ( 'NONE', #24368, #14256, #12697, .T. ) ;
#9114=ORIENTED_EDGE ( 'NONE', *, *, #19701, .T. ) ;
#9118=CARTESIAN_POINT ( 'NONE',  ( 0.000000000000000000, 0.005878491403554959860, -7.047692205288322853 ) ) ;
#9122=LINE ( 'NONE', #14301, #22519 ) ;
#9127=DIRECTION ( 'NONE',  ( -1.000000000000000000, -0.000000000000000000, 0.000000000000000000 ) ) ;
#9129=CYLINDRICAL_SURFACE ( 'NONE', #18702, 8.500000000000000000 ) ;
#9131=LINE ( 'NONE', #24859, #10847 ) ;
#9132=CARTESIAN_POINT ( 'NONE',  ( 5.377543748152548986, -8.014274990069656823, 8.669741416787380218E-17 ) ) ;
#9135=CARTESIAN_POINT ( 'NONE',  ( 5.885541615502094537, -1.090540896198865406, 8.322568858718550899 ) ) ;
#9138=VERTEX_POINT ( 'NONE', #30282 ) ;
#9140=AXIS2_PLACEMENT_3D ( 'NONE', #11055, #15901, #8713 ) ;
#9141=ORIENTED_EDGE ( 'NONE', *, *, #16304, .F. ) ;
#9145=DIRECTION ( 'NONE',  ( 0.000000000000000000, 0.4067366430758010964, -0.9135454576426006446 ) ) ;
#9146=VECTOR ( 'NONE', #13318, 1000.000000000000000 ) ;
#9161=AXIS2_PLACEMENT_3D ( 'NONE', #13720, #6540, #16742 ) ;
#9162=PLANE ( 'NONE',  #15623 ) ;
#9165=VERTEX_POINT ( 'NONE', #5041 ) ;
#9166=CIRCLE ( 'NONE', #26876, 2.999999999999999556 ) ;
#9168=CARTESIAN_POINT ( 'NONE',  ( 5.377543748152549874, -6.940565734314570356, -4.007137495034885255 ) ) ;
#9172=EDGE_CURVE ( 'NONE', #7709, #24619, #15218, .T. ) ;
#9177=CARTESIAN_POINT ( 'NONE',  ( -4.337550801365595454, -3.368539882008727115, -1.828967928396028064 ) ) ;
#9181=CARTESIAN_POINT ( 'NONE',  ( 7.249760686538667009, -3.748318449932238838, -7.906491560603703839 ) ) ;
#9183=ORIENTED_EDGE ( 'NONE', *, *, #32026, .T. ) ;
#9188=CARTESIAN_POINT ( 'NONE',  ( 5.887529755120531227, 8.194579018285292449, 1.823049025159214631 ) ) ;
#9189=EDGE_CURVE ( 'NONE', #27064, #24925, #678, .T. ) ;
#9199=CARTESIAN_POINT ( 'NONE',  ( -2.887550801365593500, -2.752080473201636845, 2.228590825266444586 ) ) ;
#9206=AXIS2_PLACEMENT_3D ( 'NONE', #23737, #28740, #13682 ) ;
#9207=CARTESIAN_POINT ( 'NONE',  ( 5.612718383992090665, -1.622626842546708081, -8.054241895195646705 ) ) ;
#9217=CARTESIAN_POINT ( 'NONE',  ( 6.530491751506348308, 6.030130624359257396, -6.216163082443004306 ) ) ;
#9222=CIRCLE ( 'NONE', #16170, 6.000000000000000000 ) ;
#9230=LINE ( 'NONE', #29806, #3951 ) ;
#9231=VECTOR ( 'NONE', #24838, 1000.000000000000000 ) ;
#9241=CARTESIAN_POINT ( 'NONE',  ( -6.250050800000000351, -2.853674364686378695, -1.549418761218566809 ) ) ;
#9247=AXIS2_PLACEMENT_3D ( 'NONE', #3017, #29066, #13172 ) ;
#9249=CARTESIAN_POINT ( 'NONE',  ( -8.000050800000002127, 0.9238973724631623918, -3.354839762463424524 ) ) ;
#9256=ORIENTED_EDGE ( 'NONE', *, *, #17497, .T. ) ;
#9269=CARTESIAN_POINT ( 'NONE',  ( 7.249760686538667009, -8.437262856154147173, -2.318425219014316419 ) ) ;
#9271=CYLINDRICAL_SURFACE ( 'NONE', #18887, 6.248999999999999666 ) ;
#9273=CIRCLE ( 'NONE', #22023, 8.500000000000000000 ) ;
#9285=CARTESIAN_POINT ( 'NONE',  ( -7.350050802731187716, -0.3135853898029607456, 2.983565686104819648 ) ) ;
#9287=CARTESIAN_POINT ( 'NONE',  ( -7.537550801365592967, -3.368539882008727115, -1.828967928396028064 ) ) ;
#9292=CARTESIAN_POINT ( 'NONE',  ( 0.000000000000000000, 0.000000000000000000, 0.000000000000000000 ) ) ;
#9308=DIRECTION ( 'NONE',  ( -1.000000000000000000, 0.000000000000000000, 0.000000000000000000 ) ) ;
#9312=ORIENTED_EDGE ( 'NONE', *, *, #31294, .T. ) ;
#9313=DIRECTION ( 'NONE',  ( 0.000000000000000000, 0.000000000000000000, 1.000000000000000000 ) ) ;
#9318=CARTESIAN_POINT ( 'NONE',  ( 7.249760686538667009, -0.8180878109962448352, 8.711672189281424394 ) ) ;
#9319=AXIS2_PLACEMENT_3D ( 'NONE', #29147, #4075, #31829 ) ;
#9320=DIRECTION ( 'NONE',  ( 0.000000000000000000, 0.9659258262890668689, 0.2588190451025257355 ) ) ;
#9327=CARTESIAN_POINT ( 'NONE',  ( -7.804531657079157192, -1.883076972206379818, -2.325406398514292761 ) ) ;
#9328=CARTESIAN_POINT ( 'NONE',  ( 3.499999999999999556, 0.000000000000000000, 0.000000000000000000 ) ) ;
#9336=EDGE_LOOP ( 'NONE', ( #30750, #6499, #8243, #11947, #1492, #15163, #20903, #15483, #20131, #7252, #18109, #23789, #24847, #29215, #1259, #8668, #18810, #8434, #22337 ) ) ;
#9341=CARTESIAN_POINT ( 'NONE',  ( -3.700050802731187805, 1.549418761218566143, -2.853674364686379583 ) ) ;
#9344=ORIENTED_EDGE ( 'NONE', *, *, #27894, .F. ) ;
#9350=CARTESIAN_POINT ( 'NONE',  ( 7.064423659272766720, 3.748318449932021679, -7.906491560605039659 ) ) ;
#9352=CARTESIAN_POINT ( 'NONE',  ( -4.187550801365593323, 0.3701630799359330593, -3.521866450007987037 ) ) ;
#9363=EDGE_CURVE ( 'NONE', #25317, #22609, #11353, .T. ) ;
#9367=CARTESIAN_POINT ( 'NONE',  ( 5.887530180601098451, 7.076866030741313374, 4.515817126386032498 ) ) ;
#9368=CARTESIAN_POINT ( 'NONE',  ( 3.499999999999999556, -2.652816298622381996, -5.657964889053610058 ) ) ;
#9369=CARTESIAN_POINT ( 'NONE',  ( -3.787550801365593411, -0.3701630799359326152, 3.521866450007987037 ) ) ;
#9372=ORIENTED_EDGE ( 'NONE', *, *, #7423, .F. ) ;
#9383=VERTEX_POINT ( 'NONE', #28900 ) ;
#9394=DIRECTION ( 'NONE',  ( -1.000000000000000000, -0.000000000000000000, -0.000000000000000000 ) ) ;
#9402=DIRECTION ( 'NONE',  ( -1.000000000000000000, 0.000000000000000000, 0.000000000000000000 ) ) ;
#9404=ORIENTED_EDGE ( 'NONE', *, *, #31164, .F. ) ;
#9406=CARTESIAN_POINT ( 'NONE',  ( 4.749760686538667009, -1.391664247347174754, -7.892520144992448472 ) ) ;
#9408=ORIENTED_EDGE ( 'NONE', *, *, #14129, .T. ) ;
#9409=EDGE_CURVE ( 'NONE', #4399, #12332, #19948, .T. ) ;
#9418=VERTEX_POINT ( 'NONE', #4158 ) ;
#9423=CARTESIAN_POINT ( 'NONE',  ( 4.749760686538667009, -4.007137495034764463, -6.940565734314639634 ) ) ;
#9424=CARTESIAN_POINT ( 'NONE',  ( -2.511343449419940921, 1.323625320507516134, 3.284597389079960461 ) ) ;
#9431=CYLINDRICAL_SURFACE ( 'NONE', #23086, 2.999999999999999112 ) ;
#9437=B_SPLINE_CURVE_WITH_KNOTS ( 'NONE', 3,
 ( #28761, #31613, #1363, #18725, #29257, #26741, #29419, #11048, #21732, #19224 ),
 .UNSPECIFIED., .F., .F.,
 ( 4, 2, 2, 2, 4 ),
 ( 1.968338519012299431E-07, 0.0005467928198071732564, 0.001093388805762445307, 0.001639984791717717357, 0.002186580777672989841 ),
 .UNSPECIFIED. ) ;
#9439=EDGE_CURVE ( 'NONE', #22736, #9882, #29000, .T. ) ;
#9440=CARTESIAN_POINT ( 'NONE',  ( -7.000050802731188071, -0.9222479816126459840, -3.113457007523259268 ) ) ;
#9442=CARTESIAN_POINT ( 'NONE',  ( -3.450050800000000084, 2.853674364686379583, 1.549418761218565921 ) ) ;
#9444=CARTESIAN_POINT ( 'NONE',  ( -4.050050802731187005, -2.331437884370912705, 1.887961173149512062 ) ) ;
#9445=VERTEX_POINT ( 'NONE', #1650 ) ;
#9461=VERTEX_POINT ( 'NONE', #32271 ) ;
#9465=FACE_OUTER_BOUND ( 'NONE', #1926, .T. ) ;
#9471=CYLINDRICAL_SURFACE ( 'NONE', #22482, 2.999999999999999112 ) ;
#9473=CARTESIAN_POINT ( 'NONE',  ( 6.880160201030087741, 0.6895871680713152596, 8.703862158141010497 ) ) ;
#9475=FACE_OUTER_BOUND ( 'NONE', #29311, .T. ) ;
#9478=CARTESIAN_POINT ( 'NONE',  ( 7.064632918400242545, 2.318425219014231597, 8.437262856154173818 ) ) ;
#9480=CARTESIAN_POINT ( 'NONE',  ( -5.854531657079158791, 2.846291840500173365, 1.545410377633946952 ) ) ;
#9481=CARTESIAN_POINT ( 'NONE',  ( 1.750000000000000222, 8.357095590591338663, -1.552080310331533486 ) ) ;
#9483=CYLINDRICAL_SURFACE ( 'NONE', #15127, 3.000000000000000444 ) ;
#9484=DIRECTION ( 'NONE',  ( 0.000000000000000000, 0.9945218953682729568, 0.1045284632676570513 ) ) ;
#9486=ORIENTED_EDGE ( 'NONE', *, *, #1830, .T. ) ;
#9490=SHAPE_DEFINITION_REPRESENTATION ( #25521, #13478 ) ;
#9493=EDGE_CURVE ( 'NONE', #21158, #1567, #15100, .T. ) ;
#9495=CARTESIAN_POINT ( 'NONE',  ( 7.064632940817598517, 3.748318449932297014, 7.906491560603678082 ) ) ;
#9496=CARTESIAN_POINT ( 'NONE',  ( 0.000000000000000000, 0.000000000000000000, 0.000000000000000000 ) ) ;
#9497=ORIENTED_EDGE ( 'NONE', *, *, #1402, .F. ) ;
#9498=DIRECTION ( 'NONE',  ( 0.000000000000000000, 0.9063077870366529343, -0.4226182617406930020 ) ) ;
#9499=CARTESIAN_POINT ( 'NONE',  ( -2.712550801365592790, -3.675193018007245627, 1.088641768524163389 ) ) ;
#9503=ORIENTED_EDGE ( 'NONE', *, *, #12064, .T. ) ;
#9504=CARTESIAN_POINT ( 'NONE',  ( -4.437550801365594211, -3.675193018007246071, 1.088641768524163167 ) ) ;
#9509=PLANE ( 'NONE',  #5381 ) ;
#9512=CARTESIAN_POINT ( 'NONE',  ( 3.499999999999999556, 0.000000000000000000, 0.000000000000000000 ) ) ;
#9514=CARTESIAN_POINT ( 'NONE',  ( -6.207304909706597762, -1.062355717592095017, -2.999999999999999556 ) ) ;
#9516=CARTESIAN_POINT ( 'NONE',  ( 6.038145208238975492, 7.104833038995711725, 4.620191422127150283 ) ) ;
#9517=EDGE_CURVE ( 'NONE', #18225, #26613, #19698, .T. ) ;
#9520=ORIENTED_EDGE ( 'NONE', *, *, #7638, .T. ) ;
#9526=ADVANCED_FACE ( 'NONE', ( #4007 ), #14005, .F. ) ;
#9529=ORIENTED_EDGE ( 'NONE', *, *, #8162, .F. ) ;
#9530=CARTESIAN_POINT ( 'NONE',  ( 3.499999999999999556, 0.000000000000000000, 0.000000000000000000 ) ) ;
#9537=ORIENTED_EDGE ( 'NONE', *, *, #10127, .F. ) ;
#9543=CARTESIAN_POINT ( 'NONE',  ( 0.000000000000000000, 0.000000000000000000, 0.000000000000000000 ) ) ;
#9550=DIRECTION ( 'NONE',  ( 0.000000000000000000, -0.9961946980917461003, 0.08715574274765135188 ) ) ;
#9557=CARTESIAN_POINT ( 'NONE',  ( -7.237550801365593145, 3.675193018007246959, -1.088641768524161391 ) ) ;
#9561=FACE_OUTER_BOUND ( 'NONE', #25660, .T. ) ;
#9570=DIRECTION ( 'NONE',  ( 0.000000000000000000, 0.2079116908177532919, 0.9781476007338070211 ) ) ;
#9581=LINE ( 'NONE', #32863, #20278 ) ;
#9586=VECTOR ( 'NONE', #22158, 1000.000000000000000 ) ;
#9590=DIRECTION ( 'NONE',  ( -0.000000000000000000, 0.9063077870366497146, -0.4226182617406997744 ) ) ;
#9597=CARTESIAN_POINT ( 'NONE',  ( -6.900050802731187538, 1.549418761218566143, -2.853674364686379583 ) ) ;
#9599=CARTESIAN_POINT ( 'NONE',  ( -4.650050799999999818, -2.853674364686378695, -1.549418761218566809 ) ) ;
#9601=CIRCLE ( 'NONE', #4271, 6.248999999999999666 ) ;
#9602=B_SPLINE_CURVE_WITH_KNOTS ( 'NONE', 3,
 ( #27050, #29083, #1153, #26563, #13820, #8670, #28896, #29387, #18886, #6003 ),
 .UNSPECIFIED., .F., .F.,
 ( 4, 2, 2, 2, 4 ),
 ( 2.740849916244211241E-07, 0.0005478761651001725578, 0.001095478245208722241, 0.001643080325317271707, 0.002190682405425821606 ),
 .UNSPECIFIED. ) ;
#9603=CARTESIAN_POINT ( 'NONE',  ( 4.749760686538667009, -4.007137495034861274, 6.940565734314584567 ) ) ;
#9604=EDGE_CURVE ( 'NONE', #16071, #442, #625, .T. ) ;
#9605=CARTESIAN_POINT ( 'NONE',  ( -4.100050802731187716, -1.549418761218565255, 2.853674364686380471 ) ) ;
#9606=VERTEX_POINT ( 'NONE', #23695 ) ;
#9621=ORIENTED_EDGE ( 'NONE', *, *, #26751, .T. ) ;
#9623=CARTESIAN_POINT ( 'NONE',  ( 7.249760686538667009, -7.530955069117533540, 2.741043480754901118 ) ) ;
#9625=AXIS2_PLACEMENT_3D ( 'NONE', #21408, #11050, #29110 ) ;
#9627=ORIENTED_EDGE ( 'NONE', *, *, #24276, .T. ) ;
#9632=CARTESIAN_POINT ( 'NONE',  ( 6.357667975083864498, -3.797112024431965160, -7.724391461487830846 ) ) ;
#9634=CARTESIAN_POINT ( 'NONE',  ( 7.249760686538667009, 6.226446564518003157, -6.147671362329155009 ) ) ;
#9637=CARTESIAN_POINT ( 'NONE',  ( -8.000050799999998574, 3.039769662057022703, 1.609430221797942595 ) ) ;
#9640=CARTESIAN_POINT ( 'NONE',  ( 0.000000000000000000, -3.573533178329543425, -5.126388750707261188 ) ) ;
#9642=DIRECTION ( 'NONE',  ( -1.000000000000000000, 0.000000000000000000, 0.000000000000000000 ) ) ;
#9645=CARTESIAN_POINT ( 'NONE',  ( -6.004531657079157370, 2.325406398514293205, -1.883076972206379374 ) ) ;
#9647=EDGE_CURVE ( 'NONE', #9418, #10650, #7667, .T. ) ;
#9648=AXIS2_PLACEMENT_3D ( 'NONE', #7848, #32942, #15014 ) ;
#9649=CARTESIAN_POINT ( 'NONE',  ( 4.749760686538667009, -2.741043480754877582, -7.530955069117540646 ) ) ;
#9650=DIRECTION ( 'NONE',  ( -1.000000000000000000, -0.000000000000000000, -0.000000000000000000 ) ) ;
#9661=CARTESIAN_POINT ( 'NONE',  ( 7.249760686538667009, 4.973063321323977881, -7.199384779417068891 ) ) ;
#9662=DIRECTION ( 'NONE',  ( 0.000000000000000000, -0.5735764363510352792, -0.8191520442889993481 ) ) ;
#9666=PLANE ( 'NONE',  #156 ) ;
#9667=CARTESIAN_POINT ( 'NONE',  ( 3.499999999999999556, 0.005878491403456947983, 7.047692205288324629 ) ) ;
#9673=CARTESIAN_POINT ( 'NONE',  ( -4.287550801365592967, -2.228590825266444586, -2.752080473201636401 ) ) ;
#9679=CARTESIAN_POINT ( 'NONE',  ( 3.499999999999999556, -5.233522515400055752, -4.720195129223329289 ) ) ;
#9680=ORIENTED_EDGE ( 'NONE', *, *, #32026, .F. ) ;
#9683=FACE_OUTER_BOUND ( 'NONE', #7276, .T. ) ;
#9702=CARTESIAN_POINT ( 'NONE',  ( 3.499999999999999556, 4.561279057474472154, -4.271385531633124621 ) ) ;
#9705=VERTEX_POINT ( 'NONE', #21337 ) ;
#9706=AXIS2_PLACEMENT_3D ( 'NONE', #32700, #6429, #14437 ) ;
#9719=ORIENTED_EDGE ( 'NONE', *, *, #25925, .T. ) ;
#9720=CARTESIAN_POINT ( 'NONE',  ( 6.524595551582240027, 4.857153507487949717, 7.168326838404958323 ) ) ;
#9729=CARTESIAN_POINT ( 'NONE',  ( 5.489321606599602887, -2.678948506461278800, -7.664118171219022280 ) ) ;
#9731=TOROIDAL_SURFACE ( 'NONE', #29502, 5.500000000000000000, 0.5000000000000000000 ) ;
#9740=ADVANCED_FACE ( 'NONE', ( #8317 ), #26201, .T. ) ;
#9743=CARTESIAN_POINT ( 'NONE',  ( -6.687550801365594211, -2.228590825266444586, -2.752080473201636401 ) ) ;
#9750=LINE ( 'NONE', #1565, #21439 ) ;
#9756=ORIENTED_EDGE ( 'NONE', *, *, #17737, .T. ) ;
#9760=AXIS2_PLACEMENT_3D ( 'NONE', #21551, #16351, #26419 ) ;
#9762=AXIS2_PLACEMENT_3D ( 'NONE', #3174, #5683, #13336 ) ;
#9768=EDGE_CURVE ( 'NONE', #12332, #4399, #30097, .T. ) ;
#9772=CYLINDRICAL_SURFACE ( 'NONE', #6583, 2.999999999999999112 ) ;
#9781=CARTESIAN_POINT ( 'NONE',  ( 5.377543748152548986, 7.892520144992435149, 1.391664247347255134 ) ) ;
#9783=VECTOR ( 'NONE', #16592, 1000.000000000000000 ) ;
#9785=CARTESIAN_POINT ( 'NONE',  ( -2.000050802731187627, 3.113457007523260156, -0.9222479816126439855 ) ) ;
#9789=CARTESIAN_POINT ( 'NONE',  ( -2.800050800000000173, 2.331437884370912705, -1.887961173149511618 ) ) ;
#9794=ORIENTED_EDGE ( 'NONE', *, *, #16956, .F. ) ;
#9795=CARTESIAN_POINT ( 'NONE',  ( 3.499999999999999556, -6.700937042937072263, 2.183447440113167826 ) ) ;
#9813=ADVANCED_FACE ( 'NONE', ( #29538 ), #22637, .T. ) ;
#9816=DIRECTION ( 'NONE',  ( 0.000000000000000000, 0.7431448254773954654, -0.6691306063588569053 ) ) ;
#9817=CARTESIAN_POINT ( 'NONE',  ( -3.200050802731187360, -3.113457007523259268, 0.9222479816126455399 ) ) ;
#9830=ORIENTED_EDGE ( 'NONE', *, *, #31243, .T. ) ;
#9831=CARTESIAN_POINT ( 'NONE',  ( -5.312550801365592434, 1.088641768524161613, 3.675193018007247403 ) ) ;
#9833=CARTESIAN_POINT ( 'NONE',  ( -7.054531657079158080, -2.846291840500172921, -1.545410377633947618 ) ) ;
#9840=DIRECTION ( 'NONE',  ( 0.000000000000000000, 0.000000000000000000, 1.000000000000000000 ) ) ;
#9844=CARTESIAN_POINT ( 'NONE',  ( 6.037141879243262288, -5.096219216992895262, 6.770886333893406217 ) ) ;
#9851=CARTESIAN_POINT ( 'NONE',  ( 6.037141752603385925, -0.4483113388087880957, -8.462586328878542119 ) ) ;
#9854=CARTESIAN_POINT ( 'NONE',  ( 0.000000000000000000, 3.673940397442060361E-16, 3.000000000000000444 ) ) ;
#9855=EDGE_CURVE ( 'NONE', #9082, #1245, #32213, .T. ) ;
#9861=CARTESIAN_POINT ( 'NONE',  ( -4.887550801365593500, 2.752080473201636845, -2.228590825266444142 ) ) ;
#9864=DIRECTION ( 'NONE',  ( -1.000000000000000000, -0.000000000000000000, 0.000000000000000000 ) ) ;
#9869=CARTESIAN_POINT ( 'NONE',  ( 7.249760686538667009, 8.466096581343482086, 2.210816291636243047 ) ) ;
#9871=CARTESIAN_POINT ( 'NONE',  ( 0.000000000000000000, 6.745408891279541130, 5.171987904998129437 ) ) ;
#9873=CARTESIAN_POINT ( 'NONE',  ( 7.249760686538667009, -1.391664247347281780, 7.892520144992429820 ) ) ;
#9874=B_SPLINE_CURVE_WITH_KNOTS ( 'NONE', 3,
 ( #9168, #19401, #32436, #29599, #1665, #14695, #22379, #14336, #17206, #17379 ),
 .UNSPECIFIED., .F., .F.,
 ( 4, 2, 2, 2, 4 ),
 ( 2.571685856657688708E-07, 0.0005478592107668807691, 0.001095461252948095677, 0.001643063295129310476, 0.002190665337310524624 ),
 .UNSPECIFIED. ) ;
#9875=LINE ( 'NONE', #12547, #21509 ) ;
#9879=EDGE_CURVE ( 'NONE', #32541, #5413, #22393, .T. ) ;
#9882=VERTEX_POINT ( 'NONE', #1602 ) ;
#9884=EDGE_LOOP ( 'NONE', ( #15229, #11235, #3240, #32947 ) ) ;
#9898=ADVANCED_FACE ( 'NONE', ( #6780 ), #3786, .F. ) ;
#9899=DIRECTION ( 'NONE',  ( -1.000000000000000000, -0.000000000000000000, 0.000000000000000000 ) ) ;
#9910=CARTESIAN_POINT ( 'NONE',  ( 6.883866601413091146, -4.949663153219582945, 7.193114723270793931 ) ) ;
#9911=CARTESIAN_POINT ( 'NONE',  ( -2.007992423166597984, -0.3178988483021057410, 3.024605502323848949 ) ) ;
#9912=CARTESIAN_POINT ( 'NONE',  ( -6.437550801365593323, 3.675193018007246959, -1.088641768524161391 ) ) ;
#9917=EDGE_LOOP ( 'NONE', ( #4731, #26470, #5804 ) ) ;
#9919=VERTEX_POINT ( 'NONE', #2232 ) ;
#9923=CYLINDRICAL_SURFACE ( 'NONE', #1739, 6.248999999999999666 ) ;
#9928=ORIENTED_EDGE ( 'NONE', *, *, #19522, .F. ) ;
#9936=DIRECTION ( 'NONE',  ( -0.000000000000000000, 0.000000000000000000, 1.000000000000000000 ) ) ;
#9941=CARTESIAN_POINT ( 'NONE',  ( 7.249760686538667009, -2.210816291636271025, 8.466096581343474980 ) ) ;
#9944=CARTESIAN_POINT ( 'NONE',  ( -3.000050802731188071, -0.9222479816126459840, -3.113457007523259268 ) ) ;
#9946=CARTESIAN_POINT ( 'NONE',  ( -7.787550801365593856, -0.3701630799359326152, 3.521866450007987037 ) ) ;
#9962=EDGE_CURVE ( 'NONE', #7257, #9966, #538, .T. ) ;
#9963=ORIENTED_EDGE ( 'NONE', *, *, #1222, .T. ) ;
#9965=CARTESIAN_POINT ( 'NONE',  ( -8.000050800000000351, 3.673940397442060361E-16, 3.000000000000000444 ) ) ;
#9966=VERTEX_POINT ( 'NONE', #7901 ) ;
#9975=CARTESIAN_POINT ( 'NONE',  ( -4.250050802731187183, 1.887961173149511618, 2.331437884370912705 ) ) ;
#9979=DIRECTION ( 'NONE',  ( 1.000000000000000000, 0.000000000000000000, 0.000000000000000000 ) ) ;
#9980=CARTESIAN_POINT ( 'NONE',  ( -7.150050802731187538, -2.983565686104819648, -0.3135853898029605791 ) ) ;
#9984=CARTESIAN_POINT ( 'NONE',  ( -5.912550801365592967, -3.675193018007246071, 1.088641768524163167 ) ) ;
#9986=CARTESIAN_POINT ( 'NONE',  ( -6.504531657079157370, -0.3127741368606806738, 2.975847129947406522 ) ) ;
#9995=VERTEX_POINT ( 'NONE', #27979 ) ;
#10010=ORIENTED_EDGE ( 'NONE', *, *, #14179, .F. ) ;
#10011=CARTESIAN_POINT ( 'NONE',  ( -4.662550801365592967, 3.521866450007987037, 0.3701630799359328372 ) ) ;
#10015=ORIENTED_EDGE ( 'NONE', *, *, #8346, .F. ) ;
#10020=CARTESIAN_POINT ( 'NONE',  ( 7.249760686538667009, 0.000000000000000000, 0.000000000000000000 ) ) ;
#10031=ADVANCED_FACE ( 'NONE', ( #10567 ), #20626, .T. ) ;
#10032=CARTESIAN_POINT ( 'NONE',  ( 3.499999999999999556, 0.000000000000000000, 0.000000000000000000 ) ) ;
#10041=CARTESIAN_POINT ( 'NONE',  ( -7.412550801365592967, -3.368539882008727115, -1.828967928396027842 ) ) ;
#10045=ORIENTED_EDGE ( 'NONE', *, *, #22824, .T. ) ;
#10062=DIRECTION ( 'NONE',  ( 0.000000000000000000, 0.08715574274767322327, -0.9961946980917442129 ) ) ;
#10063=CARTESIAN_POINT ( 'NONE',  ( -5.387550801365593500, -0.3701630799359326152, 3.521866450007987037 ) ) ;
#10068=CARTESIAN_POINT ( 'NONE',  ( 5.489321676144491846, 7.082488557107348370, -3.969109389279891431 ) ) ;
#10069=CARTESIAN_POINT ( 'NONE',  ( 5.612717990268488499, -8.213645783354285967, 0.1993707932846307540 ) ) ;
#10070=VERTEX_POINT ( 'NONE', #18587 ) ;
#10072=VERTEX_POINT ( 'NONE', #29442 ) ;
#10073=CARTESIAN_POINT ( 'NONE',  ( 5.377543748152549874, 2.741043480754926875, 7.530955069117522882 ) ) ;
#10083=ORIENTED_EDGE ( 'NONE', *, *, #23501, .F. ) ;
#10087=CARTESIAN_POINT ( 'NONE',  ( 4.749760686538667009, -8.014274990069656823, 8.669741416787380218E-17 ) ) ;
#10094=DIRECTION ( 'NONE',  ( 0.000000000000000000, 0.000000000000000000, 1.000000000000000000 ) ) ;
#10098=CARTESIAN_POINT ( 'NONE',  ( -3.950050802731187360, -2.983565686104819648, -0.3135853898029605791 ) ) ;
#10099=ORIENTED_EDGE ( 'NONE', *, *, #20101, .F. ) ;
#10101=CARTESIAN_POINT ( 'NONE',  ( -6.487550801365593145, 2.752080473201636845, -2.228590825266444142 ) ) ;
#10105=CARTESIAN_POINT ( 'NONE',  ( 5.612974441954673210, -5.126870824538720228, -6.420536856479988508 ) ) ;
#10119=CYLINDRICAL_SURFACE ( 'NONE', #28331, 2.999999999999999112 ) ;
#10121=CARTESIAN_POINT ( 'NONE',  ( -6.562942409646512765, -8.831141768130910875E-16, 2.999999999999999556 ) ) ;
#10123=CARTESIAN_POINT ( 'NONE',  ( 5.612718825656738630, -6.163864706063985288, 5.432357446996388006 ) ) ;
#10127=EDGE_CURVE ( 'NONE', #13648, #20515, #4047, .T. ) ;
#10129=DIRECTION ( 'NONE',  ( 0.000000000000000000, -1.000000000000000000, 0.000000000000000000 ) ) ;
#10134=CARTESIAN_POINT ( 'NONE',  ( -5.762550801365593500, -2.228590825266444586, -2.752080473201636401 ) ) ;
#10136=ADVANCED_FACE ( 'NONE', ( #13564 ), #1378, .T. ) ;
#10137=CARTESIAN_POINT ( 'NONE',  ( -5.054531657079158968, 2.846291840500173365, 1.545410377633946952 ) ) ;
#10138=VECTOR ( 'NONE', #28118, 1000.000000000000000 ) ;
#10148=CARTESIAN_POINT ( 'NONE',  ( 5.612718383992088889, 1.622626842546764259, 8.054241895195636047 ) ) ;
#10155=CIRCLE ( 'NONE', #6961, 2.999999999999999556 ) ;
#10157=CARTESIAN_POINT ( 'NONE',  ( 7.249760686538667009, 7.953573330858264789, -3.647351267791489882 ) ) ;
#10167=CARTESIAN_POINT ( 'NONE',  ( -7.562550801365593323, -2.752080473201636845, 2.228590825266444586 ) ) ;
#10170=LINE ( 'NONE', #25238, #3344 ) ;
#10182=CARTESIAN_POINT ( 'NONE',  ( 7.249760686538667009, -4.973063321323826003, -7.199384779417172808 ) ) ;
#10186=( BOUNDED_CURVE ( )  B_SPLINE_CURVE ( 2, ( #597, #784, #23187, #10790, #18489, #28682, #5286, #10965, #8441, #31365, #5930 ),
 .UNSPECIFIED., .F., .F. ) 
 B_SPLINE_CURVE_WITH_KNOTS ( ( 3, 2, 2, 2, 2, 3 ),
 ( 0.1228822619934377414, 0.1250000000000000000, 0.1406250000000000000, 0.1562500000000000000, 0.1718750000000000000, 0.1853822619934377414 ),
 .UNSPECIFIED. ) 
 CURVE ( )  GEOMETRIC_REPRESENTATION_ITEM ( )  RATIONAL_B_SPLINE_CURVE ( ( 0.9821626249036861100, 0.9896829947469993893, 1.000000000000000000, 0.9238795325112867385, 1.000000000000000000, 0.9238795325112867385, 1.000000000000000000, 0.9238795325112867385, 1.000000000000000000, 0.9341965377642873491, 0.9821626249036861100 ) ) 
 REPRESENTATION_ITEM ( '' )  );
#10190=EDGE_CURVE ( 'NONE', #22736, #29357, #32624, .T. ) ;
#10198=ORIENTED_EDGE ( 'NONE', *, *, #16053, .T. ) ;
#10199=CARTESIAN_POINT ( 'NONE',  ( -5.356376981307136909, 0.1572233378491222633, -3.000000000000000000 ) ) ;
#10204=CARTESIAN_POINT ( 'NONE',  ( -2.253815017383504316, 1.323625320507515690, 3.284597389079958685 ) ) ;
#10207=DIRECTION ( 'NONE',  ( 1.000000000000000000, 0.000000000000000000, -0.000000000000000000 ) ) ;
#10217=CARTESIAN_POINT ( 'NONE',  ( 4.749760686538667009, 1.391664247347228045, 7.892520144992438702 ) ) ;
#10222=VECTOR ( 'NONE', #12333, 1000.000000000000000 ) ;
#10235=CARTESIAN_POINT ( 'NONE',  ( -5.887550801365593500, -2.228590825266444586, -2.752080473201636401 ) ) ;
#10236=ORIENTED_EDGE ( 'NONE', *, *, #17075, .F. ) ;
#10237=AXIS2_PLACEMENT_3D ( 'NONE', #24830, #22167, #21815 ) ;
#10238=VECTOR ( 'NONE', #565, 1000.000000000000000 ) ;
#10241=FACE_BOUND ( 'NONE', #25520, .T. ) ;
#10245=VERTEX_POINT ( 'NONE', #4701 ) ;
#10246=VECTOR ( 'NONE', #2246, 999.9999999999998863 ) ;
#10248=AXIS2_PLACEMENT_3D ( 'NONE', #9496, #12673, #17376 ) ;
#10254=VERTEX_POINT ( 'NONE', #1530 ) ;
#10271=CARTESIAN_POINT ( 'NONE',  ( 7.249760686538667009, 8.721381771256204729, 0.7071067811865429098 ) ) ;
#10279=DIRECTION ( 'NONE',  ( 0.000000000000000000, -0.9063077870366558209, 0.4226182617406868403 ) ) ;
#10280=CARTESIAN_POINT ( 'NONE',  ( -4.150050802731187538, -0.3135853898029607456, 2.983565686104819648 ) ) ;
#10282=CARTESIAN_POINT ( 'NONE',  ( -6.187550801365593323, -0.3701630799359326152, 3.521866450007987037 ) ) ;
#10283=CIRCLE ( 'NONE', #10810, 2.999999999999999556 ) ;
#10284=B_SPLINE_CURVE_WITH_KNOTS ( 'NONE', 3,
 ( #8051, #17761, #18085, #12579, #28467, #2920, #28276, #4893, #5072, #25453 ),
 .UNSPECIFIED., .F., .F.,
 ( 4, 2, 2, 2, 4 ),
 ( 2.571685856657688708E-07, 0.0005478592107668812028, 0.001095461252948096761, 0.001643063295129312210, 0.002190665337310527660 ),
 .UNSPECIFIED. ) ;
#10286=DIRECTION ( 'NONE',  ( -1.000000000000000000, -0.000000000000000000, -0.000000000000000000 ) ) ;
#10287=VECTOR ( 'NONE', #31577, 1000.000000000000000 ) ;
#10296=DIRECTION ( 'NONE',  ( 0.000000000000000000, 0.000000000000000000, 1.000000000000000000 ) ) ;
#10302=VERTEX_POINT ( 'NONE', #32127 ) ;
#10304=CARTESIAN_POINT ( 'NONE',  ( -2.477544768930361130, -0.1796242917493272861, 3.046506040574583185 ) ) ;
#10312=ORIENTED_EDGE ( 'NONE', *, *, #17575, .T. ) ;
#10315=AXIS2_PLACEMENT_3D ( 'NONE', #24221, #6486, #1340 ) ;
#10317=DIRECTION ( 'NONE',  ( 0.000000000000000000, -0.5735764363510565955, 0.8191520442889845821 ) ) ;
#10325=DIRECTION ( 'NONE',  ( -0.000000000000000000, 0.9063077870366511579, -0.4226182617406968323 ) ) ;
#10328=CARTESIAN_POINT ( 'NONE',  ( -6.712550801365593678, -3.675193018007246071, 1.088641768524163167 ) ) ;
#10330=CARTESIAN_POINT ( 'NONE',  ( -3.104531657079157458, -2.975847129947406522, -0.3127741368606805072 ) ) ;
#10344=VECTOR ( 'NONE', #26927, 1000.000000000000000 ) ;
#10345=EDGE_CURVE ( 'NONE', #7709, #16071, #17810, .T. ) ;
#10346=DIRECTION ( 'NONE',  ( -1.000000000000000000, -0.000000000000000000, -0.000000000000000000 ) ) ;
#10349=ORIENTED_EDGE ( 'NONE', *, *, #19060, .T. ) ;
#10354=DIRECTION ( 'NONE',  ( 0.000000000000000000, 0.8191520442889909104, 0.5735764363510474917 ) ) ;
#10357=CARTESIAN_POINT ( 'NONE',  ( -6.662550801365592967, -3.521866450007987037, -0.3701630799359323931 ) ) ;
#10372=ADVANCED_FACE ( 'NONE', ( #13812 ), #31753, .T. ) ;
#10374=DIRECTION ( 'NONE',  ( 0.000000000000000000, 0.000000000000000000, 1.000000000000000000 ) ) ;
#10376=VERTEX_POINT ( 'NONE', #29222 ) ;
#10386=ORIENTED_EDGE ( 'NONE', *, *, #14468, .T. ) ;
#10391=CARTESIAN_POINT ( 'NONE',  ( -8.000050800000018114, 1.979734913925816908, -2.936190332390367086 ) ) ;
#10394=CARTESIAN_POINT ( 'NONE',  ( 0.000000000000000000, 0.000000000000000000, 0.000000000000000000 ) ) ;
#10400=EDGE_CURVE ( 'NONE', #21228, #26019, #6308, .T. ) ;
#10408=CARTESIAN_POINT ( 'NONE',  ( 5.489343555808772201, 8.118190043691528857, -0.1039150536218743925 ) ) ;
#10410=AXIS2_PLACEMENT_3D ( 'NONE', #18922, #4035, #32116 ) ;
#10411=VERTEX_POINT ( 'NONE', #16495 ) ;
#10412=CARTESIAN_POINT ( 'NONE',  ( -2.093800801365593323, -0.3701630799359326152, 3.521866450007987037 ) ) ;
#10413=CARTESIAN_POINT ( 'NONE',  ( 5.377543748152548098, -2.789499415801756586E-14, 8.014274990069656823 ) ) ;
#10414=CARTESIAN_POINT ( 'NONE',  ( -2.437550801365593767, 3.675193018007246959, -1.088641768524161391 ) ) ;
#10415=VERTEX_POINT ( 'NONE', #18688 ) ;
#10430=ORIENTED_EDGE ( 'NONE', *, *, #9363, .F. ) ;
#10431=CARTESIAN_POINT ( 'NONE',  ( -10.00000000000000000, 0.000000000000000000, 0.000000000000000000 ) ) ;
#10432=CARTESIAN_POINT ( 'NONE',  ( 3.499999999999999556, 2.871924938129881699, 6.435996203144517480 ) ) ;
#10433=VERTEX_POINT ( 'NONE', #26414 ) ;
#10435=CARTESIAN_POINT ( 'NONE',  ( -5.706376978575949721, -0.1572233378491221800, 3.000000000000000000 ) ) ;
#10436=CARTESIAN_POINT ( 'NONE',  ( 7.249760686538667009, -8.711672189281431500, 0.8180878109961559064 ) ) ;
#10438=DIRECTION ( 'NONE',  ( 0.000000000000000000, 0.000000000000000000, 1.000000000000000000 ) ) ;
#10453=CARTESIAN_POINT ( 'NONE',  ( -6.887550801365593500, -2.752080473201636845, 2.228590825266444586 ) ) ;
#10461=B_SPLINE_CURVE_WITH_KNOTS ( 'NONE', 3,
 ( #22073, #32289, #21728, #1669, #3855, #19404, #19560, #27228, #9350, #11378 ),
 .UNSPECIFIED., .F., .F.,
 ( 4, 2, 2, 2, 4 ),
 ( 2.571685856669747810E-07, 0.0005478592107668818533, 0.001095461252948096761, 0.001643063295129311560, 0.002190665337310527226 ),
 .UNSPECIFIED. ) ;
#10466=VERTEX_POINT ( 'NONE', #6162 ) ;
#10482=CARTESIAN_POINT ( 'NONE',  ( -8.000050800000003903, -2.165465766649708357, 2.111084521466020103 ) ) ;
#10483=CARTESIAN_POINT ( 'NONE',  ( 7.249760686538666121, 0.000000000000000000, 6.000000000000000000 ) ) ;
#10485=CARTESIAN_POINT ( 'NONE',  ( 6.356382477965130562, -6.947086032709898440, -5.080803740829792581 ) ) ;
#10486=ORIENTED_EDGE ( 'NONE', *, *, #7732, .F. ) ;
#10487=CARTESIAN_POINT ( 'NONE',  ( -7.762550801365593500, 2.228590825266444142, 2.752080473201636845 ) ) ;
#10489=CARTESIAN_POINT ( 'NONE',  ( -4.504531657079157370, 0.3127741368606810068, -2.975847129947406522 ) ) ;
#10494=EDGE_CURVE ( 'NONE', #16352, #1604, #14935, .T. ) ;
#10503=DIRECTION ( 'NONE',  ( -1.000000000000000000, -0.000000000000000000, -0.000000000000000000 ) ) ;
#10506=DIRECTION ( 'NONE',  ( 0.000000000000000000, 0.000000000000000000, 1.000000000000000000 ) ) ;
#10512=CARTESIAN_POINT ( 'NONE',  ( -6.762550801365593500, -2.752080473201636845, 2.228590825266444586 ) ) ;
#10515=MANIFOLD_SOLID_BREP ( 'Chamfer1', #13479 ) ;
#10517=ORIENTED_EDGE ( 'NONE', *, *, #5915, .F. ) ;
#10529=EDGE_CURVE ( 'NONE', #24619, #19255, #15633, .T. ) ;
#10531=DIRECTION ( 'NONE',  ( 0.000000000000000000, -0.2588190451025207950, -0.9659258262890683122 ) ) ;
#10535=CARTESIAN_POINT ( 'NONE',  ( -5.150050802731186650, 2.983565686104819648, 0.3135853898029609677 ) ) ;
#10538=VERTEX_POINT ( 'NONE', #24698 ) ;
#10539=CARTESIAN_POINT ( 'NONE',  ( -2.253815017383503871, -0.3178988483021043532, 3.024605502323848061 ) ) ;
#10540=CARTESIAN_POINT ( 'NONE',  ( -6.612550801365594033, -3.368539882008727115, -1.828967928396027842 ) ) ;
#10556=CARTESIAN_POINT ( 'NONE',  ( -8.000050800000002127, 0.2098993114761400491, -2.993269680925520149 ) ) ;
#10557=CARTESIAN_POINT ( 'NONE',  ( 3.499999999999999556, -4.147285340411747789, -5.698247474649445365 ) ) ;
#10559=EDGE_CURVE ( 'NONE', #8809, #26222, #28110, .T. ) ;
#10564=DIRECTION ( 'NONE',  ( 0.000000000000000000, 0.9945218953682729568, 0.1045284632676570374 ) ) ;
#10565=EDGE_CURVE ( 'NONE', #5075, #21400, #15169, .T. ) ;
#10567=FACE_OUTER_BOUND ( 'NONE', #11958, .T. ) ;
#10568=CARTESIAN_POINT ( 'NONE',  ( 6.524595395369781947, -8.328507089302162214, -2.369138865965912721 ) ) ;
#10570=DIRECTION ( 'NONE',  ( -1.000000000000000000, -0.000000000000000000, 0.000000000000000000 ) ) ;
#10579=EDGE_CURVE ( 'NONE', #11907, #14398, #10940, .T. ) ;
#10581=CARTESIAN_POINT ( 'NONE',  ( 5.489344046532321997, -4.149088721182480732, -6.978601450725530064 ) ) ;
#10588=DIRECTION ( 'NONE',  ( 0.000000000000000000, 0.000000000000000000, 1.000000000000000000 ) ) ;
#10592=EDGE_CURVE ( 'NONE', #481, #11524, #17851, .T. ) ;
#10599=ORIENTED_EDGE ( 'NONE', *, *, #9855, .F. ) ;
#10603=ADVANCED_FACE ( 'NONE', ( #8137 ), #13295, .F. ) ;
#10604=DIRECTION ( 'NONE',  ( 0.000000000000000000, 0.000000000000000000, 1.000000000000000000 ) ) ;
#10609=DIRECTION ( 'NONE',  ( 0.000000000000000000, 0.000000000000000000, 1.000000000000000000 ) ) ;
#10610=( NAMED_UNIT ( * ) PLANE_ANGLE_UNIT ( ) SI_UNIT ( $, .RADIAN. ) );
#10612=ORIENTED_EDGE ( 'NONE', *, *, #14125, .T. ) ;
#10615=DIRECTION ( 'NONE',  ( 0.000000000000000000, -0.7431448254773863615, -0.6691306063588670083 ) ) ;
#10616=ORIENTED_EDGE ( 'NONE', *, *, #14125, .F. ) ;
#10630=CARTESIAN_POINT ( 'NONE',  ( 0.000000000000000000, -4.724769925181146135, -4.089810527897805414 ) ) ;
#10633=DIRECTION ( 'NONE',  ( 0.000000000000000000, 0.000000000000000000, 1.000000000000000000 ) ) ;
#10634=EDGE_CURVE ( 'NONE', #3548, #24916, #1747, .T. ) ;
#10635=CARTESIAN_POINT ( 'NONE',  ( 7.249760686538667009, 5.151476664237558900, -6.139290821770204687 ) ) ;
#10636=CARTESIAN_POINT ( 'NONE',  ( -7.362942409646514363, 1.214281993118000652E-15, 3.000000000000000000 ) ) ;
#10638=CARTESIAN_POINT ( 'NONE',  ( 6.524595623740803596, -7.015943501182358766, -5.074779492939359926 ) ) ;
#10640=CARTESIAN_POINT ( 'NONE',  ( -3.162550801365593856, 2.752080473201636845, -2.228590825266444142 ) ) ;
#10641=EDGE_LOOP ( 'NONE', ( #9963, #13060, #13964 ) ) ;
#10642=CARTESIAN_POINT ( 'NONE',  ( -8.450050800000001416, 1.549418761218566143, -2.853674364686379583 ) ) ;
#10647=DIRECTION ( 'NONE',  ( 0.000000000000000000, 0.000000000000000000, 1.000000000000000000 ) ) ;
#10648=AXIS2_PLACEMENT_3D ( 'NONE', #16803, #19642, #25136 ) ;
#10650=VERTEX_POINT ( 'NONE', #29022 ) ;
#10657=CARTESIAN_POINT ( 'NONE',  ( 7.064423669210277978, 7.135485519863459913, 5.064320921489716909 ) ) ;
#10665=CARTESIAN_POINT ( 'NONE',  ( -6.012550801365594388, -1.828967928396026510, 3.368539882008728004 ) ) ;
#10667=PLANE ( 'NONE',  #23600 ) ;
#10678=CARTESIAN_POINT ( 'NONE',  ( 3.499999999999999556, 4.561279057474412646, 4.271385531633187682 ) ) ;
#10681=CARTESIAN_POINT ( 'NONE',  ( 5.885541736258995904, -2.519172009311986926, 8.006759975090643522 ) ) ;
#10684=ORIENTED_EDGE ( 'NONE', *, *, #17139, .F. ) ;
#10693=ORIENTED_EDGE ( 'NONE', *, *, #17803, .F. ) ;
#10694=VERTEX_POINT ( 'NONE', #16300 ) ;
#10695=DIRECTION ( 'NONE',  ( 1.000000000000000000, -0.000000000000000000, -0.000000000000000000 ) ) ;
#10701=CARTESIAN_POINT ( 'NONE',  ( 7.249760686538667009, -1.391664247347281780, 7.892520144992429820 ) ) ;
#10708=EDGE_CURVE ( 'NONE', #280, #13240, #21313, .T. ) ;
#10718=CARTESIAN_POINT ( 'NONE',  ( -4.512942406915326998, 4.884725290497410777E-15, -2.999999999999999556 ) ) ;
#10724=ADVANCED_BREP_SHAPE_REPRESENTATION ( '', ( #10515, #2865 ), #32200 ) ;
#10726=AXIS2_PLACEMENT_3D ( 'NONE', #30708, #18300, #17971 ) ;
#10733=AXIS2_PLACEMENT_3D ( 'NONE', #26228, #26416, #3343 ) ;
#10734=VECTOR ( 'NONE', #13326, 1000.000000000000114 ) ;
#10737=ORIENTED_EDGE ( 'NONE', *, *, #9189, .F. ) ;
#10740=ORIENTED_EDGE ( 'NONE', *, *, #9189, .T. ) ;
#10761=DIRECTION ( 'NONE',  ( 0.000000000000000000, 0.000000000000000000, 1.000000000000000000 ) ) ;
#10762=ORIENTED_EDGE ( 'NONE', *, *, #12215, .F. ) ;
#10768=ORIENTED_EDGE ( 'NONE', *, *, #22273, .F. ) ;
#10770=VECTOR ( 'NONE', #6710, 999.9999999999998863 ) ;
#10784=ORIENTED_EDGE ( 'NONE', *, *, #9113, .F. ) ;
#10787=CIRCLE ( 'NONE', #8147, 2.999999999999998668 ) ;
#10788=AXIS2_PLACEMENT_3D ( 'NONE', #14672, #21411, #27046 ) ;
#10790=CARTESIAN_POINT ( 'NONE',  ( -7.650050800000001594, 1.549418761218566143, -2.853674364686379583 ) ) ;
#10795=FACE_OUTER_BOUND ( 'NONE', #28974, .T. ) ;
#10797=FACE_OUTER_BOUND ( 'NONE', #6312, .T. ) ;
#10798=EDGE_CURVE ( 'NONE', #4093, #13793, #4426, .T. ) ;
#10801=PLANE ( 'NONE',  #4308 ) ;
#10806=VECTOR ( 'NONE', #10207, 1000.000000000000000 ) ;
#10808=DIRECTION ( 'NONE',  ( 0.000000000000000000, 0.000000000000000000, 1.000000000000000000 ) ) ;
#10810=AXIS2_PLACEMENT_3D ( 'NONE', #3074, #30478, #10564 ) ;
#10812=CARTESIAN_POINT ( 'NONE',  ( -4.662550801365592967, 3.521866450007987037, 0.3701630799359328372 ) ) ;
#10816=EDGE_CURVE ( 'NONE', #12536, #24760, #11884, .T. ) ;
#10817=CARTESIAN_POINT ( 'NONE',  ( -3.004531657079156926, -1.883076972206379818, -2.325406398514292761 ) ) ;
#10824=DIRECTION ( 'NONE',  ( 0.000000000000000000, -0.9945218953682744001, 0.1045284632676437286 ) ) ;
#10832=LINE ( 'NONE', #11000, #6954 ) ;
#10836=ORIENTED_EDGE ( 'NONE', *, *, #24028, .T. ) ;
#10838=CARTESIAN_POINT ( 'NONE',  ( 5.612718383992088889, -8.054241895195639600, 1.622626842546736503 ) ) ;
#10841=VECTOR ( 'NONE', #19380, 1000.000000000000000 ) ;
#10846=CARTESIAN_POINT ( 'NONE',  ( -2.912550801365593411, 1.088641768524161613, 3.675193018007247403 ) ) ;
#10847=VECTOR ( 'NONE', #26881, 1000.000000000000000 ) ;
#10859=CIRCLE ( 'NONE', #6062, 2.999999999999999112 ) ;
#10866=AXIS2_PLACEMENT_3D ( 'NONE', #702, #19069, #4177 ) ;
#10871=PLANE ( 'NONE',  #6990 ) ;
#10872=ORIENTED_EDGE ( 'NONE', *, *, #6291, .F. ) ;
#10883=CARTESIAN_POINT ( 'NONE',  ( -3.762550801365593500, 2.228590825266444142, 2.752080473201636845 ) ) ;
#10894=CIRCLE ( 'NONE', #22113, 6.248999999999999666 ) ;
#10898=CARTESIAN_POINT ( 'NONE',  ( 7.249760686538667009, -6.940565734314570356, -4.007137495034885255 ) ) ;
#10907=CARTESIAN_POINT ( 'NONE',  ( 5.377543748152548986, -6.139290821770219786, -5.151476664237539360 ) ) ;
#10912=CARTESIAN_POINT ( 'NONE',  ( 7.064423539573518873, -8.721381771257245674, 0.7071067811875828557 ) ) ;
#10921=EDGE_CURVE ( 'NONE', #13878, #19582, #27949, .T. ) ;
#10927=CARTESIAN_POINT ( 'NONE',  ( 7.249760686538667009, 7.892520144992435149, 1.391664247347255134 ) ) ;
#10934=CARTESIAN_POINT ( 'NONE',  ( -2.476225935960405966, -0.3178988483021057410, 3.024605502323848949 ) ) ;
#10937=CARTESIAN_POINT ( 'NONE',  ( -8.000050800000000351, -1.836970198721030181E-16, -3.000000000000000444 ) ) ;
#10940=B_SPLINE_CURVE_WITH_KNOTS ( 'NONE', 3,
 ( #1637, #12155, #32258, #22353, #32566, #9637, #14818, #2130, #12311, #32749, #22527, #27694, #4798, #14976, #18158, #615, #12797, #2634, #7817, #23012, #18348, #21025, #30895, #18504, #5791, #33055, #28049, #10482, #454, #20536 ),
 .UNSPECIFIED., .F., .F.,
 ( 4, 2, 2, 2, 2, 2, 2, 2, 2, 2, 2, 2, 2, 2, 4 ),
 ( -0.008140911791333830735, -0.007115276677915103633, -0.006602459121205740515, -0.006089641564496376530, -0.005576824007787013412, -0.005064006451077650295, -0.004038371337658924060, -0.003525553780949560942, -0.003012736224240198692, -0.002499918667530834707, -0.001987101110821470722, -0.001474283554112107604, -0.0009614659974027444864, -0.0004486484406933805014, 6.416911601598088155E-05 ),
 .UNSPECIFIED. ) ;
#10944=CARTESIAN_POINT ( 'NONE',  ( 5.489343958331426521, -2.874233210898315072, -7.593062460271022829 ) ) ;
#10950=EDGE_CURVE ( 'NONE', #8263, #6649, #15055, .T. ) ;
#10953=VERTEX_POINT ( 'NONE', #25436 ) ;
#10965=CARTESIAN_POINT ( 'NONE',  ( -7.450050800000001416, 2.853674364686379583, 1.549418761218565921 ) ) ;
#10966=DIRECTION ( 'NONE',  ( 0.000000000000000000, -0.08715574274765797158, -0.9961946980917455452 ) ) ;
#10967=VERTEX_POINT ( 'NONE', #12714 ) ;
#10972=DIRECTION ( 'NONE',  ( -1.000000000000000000, -0.000000000000000000, -0.000000000000000000 ) ) ;
#10978=FACE_OUTER_BOUND ( 'NONE', #14552, .T. ) ;
#10979=EDGE_CURVE ( 'NONE', #25776, #1551, #569, .T. ) ;
#10983=EDGE_CURVE ( 'NONE', #30369, #26986, #18231, .T. ) ;
#10985=CARTESIAN_POINT ( 'NONE',  ( -4.862550801365594033, 0.3701630799359330593, -3.521866450007987037 ) ) ;
#10987=CARTESIAN_POINT ( 'NONE',  ( -6.150050800000001594, -0.9222479816126459840, -3.113457007523259268 ) ) ;
#10995=VERTEX_POINT ( 'NONE', #863 ) ;
#10999=EDGE_CURVE ( 'NONE', #5581, #19600, #13696, .T. ) ;
#11000=CARTESIAN_POINT ( 'NONE',  ( 3.499999999999999556, -0.1221666339523235223, -6.247805719894684806 ) ) ;
#11003=CARTESIAN_POINT ( 'NONE',  ( 0.000000000000000000, 8.265874651078018331, 1.981241088980808751 ) ) ;
#11004=CYLINDRICAL_SURFACE ( 'NONE', #26771, 6.248999999999999666 ) ;
#11006=EDGE_CURVE ( 'NONE', #16325, #12581, #3051, .T. ) ;
#11009=CARTESIAN_POINT ( 'NONE',  ( -3.362550801365593589, -2.228590825266444586, -2.752080473201636401 ) ) ;
#11010=PLANE ( 'NONE',  #21410 ) ;
#11012=ORIENTED_EDGE ( 'NONE', *, *, #14602, .F. ) ;
#11022=CARTESIAN_POINT ( 'NONE',  ( -3.187550801365593767, 3.521866450007987037, 0.3701630799359328372 ) ) ;
#11029=ORIENTED_EDGE ( 'NONE', *, *, #9068, .T. ) ;
#11034=ORIENTED_EDGE ( 'NONE', *, *, #2772, .F. ) ;
#11039=CARTESIAN_POINT ( 'NONE',  ( -3.962550801365593234, 2.752080473201636845, -2.228590825266444142 ) ) ;
#11046=CARTESIAN_POINT ( 'NONE',  ( -5.087550801365593678, -2.228590825266444586, -2.752080473201636401 ) ) ;
#11048=CARTESIAN_POINT ( 'NONE',  ( 5.612974044843315191, 1.622927203279449282, -8.054452210044747318 ) ) ;
#11050=DIRECTION ( 'NONE',  ( -1.000000000000000000, -0.000000000000000000, 0.000000000000000000 ) ) ;
#11054=CARTESIAN_POINT ( 'NONE',  ( 5.612974044843316079, -1.229732182294847487, -8.123783100924562461 ) ) ;
#11055=CARTESIAN_POINT ( 'NONE',  ( 4.749760686538667009, -7.530955069117533540, 2.741043480754901118 ) ) ;
#11060=CARTESIAN_POINT ( 'NONE',  ( -4.637550801365592612, 1.088641768524161613, 3.675193018007247403 ) ) ;
#11069=ORIENTED_EDGE ( 'NONE', *, *, #19550, .F. ) ;
#11073=ORIENTED_EDGE ( 'NONE', *, *, #10592, .F. ) ;
#11095=DIRECTION ( 'NONE',  ( -1.000000000000000000, 0.000000000000000000, 0.000000000000000000 ) ) ;
#11099=FACE_OUTER_BOUND ( 'NONE', #206, .T. ) ;
#11102=CARTESIAN_POINT ( 'NONE',  ( 5.377543748152550762, 6.139290821770327256, -5.151476664237414127 ) ) ;
#11105=VERTEX_POINT ( 'NONE', #25907 ) ;
#11108=FACE_OUTER_BOUND ( 'NONE', #4838, .T. ) ;
#11109=VERTEX_POINT ( 'NONE', #18677 ) ;
#11121=CARTESIAN_POINT ( 'NONE',  ( -3.900050800000000706, -2.983565686104819648, -0.3135853898029605791 ) ) ;
#11125=EDGE_CURVE ( 'NONE', #12969, #13197, #9222, .T. ) ;
#11130=DIRECTION ( 'NONE',  ( 1.000000000000000000, -0.000000000000000000, -0.000000000000000000 ) ) ;
#11132=CARTESIAN_POINT ( 'NONE',  ( -2.212550801365593234, 3.368539882008727115, 1.828967928396026954 ) ) ;
#11134=CARTESIAN_POINT ( 'NONE',  ( -7.750050800000000351, -0.9222479816126459840, -3.113457007523259268 ) ) ;
#11139=LINE ( 'NONE', #26389, #23634 ) ;
#11148=ORIENTED_EDGE ( 'NONE', *, *, #12575, .F. ) ;
#11152=EDGE_CURVE ( 'NONE', #22574, #9919, #23133, .T. ) ;
#11154=ORIENTED_EDGE ( 'NONE', *, *, #10921, .F. ) ;
#11155=CARTESIAN_POINT ( 'NONE',  ( -3.612550801365593589, -1.828967928396026510, 3.368539882008728004 ) ) ;
#11158=ORIENTED_EDGE ( 'NONE', *, *, #5307, .T. ) ;
#11163=PLANE ( 'NONE',  #25288 ) ;
#11168=CARTESIAN_POINT ( 'NONE',  ( -8.454531657079160212, 1.545410377633947174, -2.846291840500173365 ) ) ;
#11171=EDGE_CURVE ( 'NONE', #16287, #27971, #1321, .T. ) ;
#11172=CARTESIAN_POINT ( 'NONE',  ( -4.487550801365593145, -2.752080473201636845, 2.228590825266444586 ) ) ;
#11175=VERTEX_POINT ( 'NONE', #24009 ) ;
#11176=CYLINDRICAL_SURFACE ( 'NONE', #9206, 2.999999999999999112 ) ;
#11182=AXIS2_PLACEMENT_3D ( 'NONE', #29012, #1078, #31508 ) ;
#11189=CARTESIAN_POINT ( 'NONE',  ( -3.012550801365593500, 3.368539882008727115, 1.828967928396027176 ) ) ;
#11195=CARTESIAN_POINT ( 'NONE',  ( -7.287550801365593856, 2.752080473201636845, -2.228590825266444142 ) ) ;
#11202=EDGE_CURVE ( 'NONE', #11273, #20542, #1135, .T. ) ;
#11207=CIRCLE ( 'NONE', #6402, 2.999999999999999556 ) ;
#11210=CARTESIAN_POINT ( 'NONE',  ( 3.499999999999999556, 4.561279057474412646, 4.271385531633187682 ) ) ;
#11212=B_SPLINE_CURVE_WITH_KNOTS ( 'NONE', 3,
 ( #11926, #29970, #7236, #19609, #32650, #27776, #14389, #4888, #9729, #17073 ),
 .UNSPECIFIED., .F., .F.,
 ( 4, 2, 2, 2, 4 ),
 ( 1.968338519013083730E-07, 0.0005467927057105487470, 0.001093388577569196071, 0.001639984449427843395, 0.002186580321286489634 ),
 .UNSPECIFIED. ) ;
#11214=CARTESIAN_POINT ( 'NONE',  ( -4.837550801365592790, 3.675193018007247403, -1.088641768524161391 ) ) ;
#11215=ORIENTED_EDGE ( 'NONE', *, *, #5221, .T. ) ;
#11217=AXIS2_PLACEMENT_3D ( 'NONE', #1939, #20489, #12605 ) ;
#11219=CARTESIAN_POINT ( 'NONE',  ( 5.885541615502094537, 8.193643496140877502, -1.821712961073262527 ) ) ;
#11221=CARTESIAN_POINT ( 'NONE',  ( 4.749760686538667009, 6.940565734314597002, 4.007137495034836405 ) ) ;
#11222=ORIENTED_EDGE ( 'NONE', *, *, #5279, .T. ) ;
#11228=ORIENTED_EDGE ( 'NONE', *, *, #2151, .T. ) ;
#11231=EDGE_CURVE ( 'NONE', #1551, #6094, #26041, .T. ) ;
#11232=AXIS2_PLACEMENT_3D ( 'NONE', #9679, #12535, #32606 ) ;
#11235=ORIENTED_EDGE ( 'NONE', *, *, #20631, .F. ) ;
#11239=CARTESIAN_POINT ( 'NONE',  ( 3.499999999999999556, 4.058600654062849422, 7.468451026206211374 ) ) ;
#11249=CARTESIAN_POINT ( 'NONE',  ( -3.300050800000000173, -0.3135853898029607456, 2.983565686104819648 ) ) ;
#11263=DIRECTION ( 'NONE',  ( 1.000000000000000000, -0.000000000000000000, -0.000000000000000000 ) ) ;
#11266=CARTESIAN_POINT ( 'NONE',  ( 7.064632951172269415, 7.135485519862065473, -5.064320921489749772 ) ) ;
#11269=VERTEX_POINT ( 'NONE', #30228 ) ;
#11270=CARTESIAN_POINT ( 'NONE',  ( 6.038145077921539539, 3.316258947000968238, -7.799182446117161049 ) ) ;
#11273=VERTEX_POINT ( 'NONE', #10121 ) ;
#11276=EDGE_CURVE ( 'NONE', #29777, #12969, #25182, .T. ) ;
#11278=ORIENTED_EDGE ( 'NONE', *, *, #24510, .F. ) ;
#11284=CARTESIAN_POINT ( 'NONE',  ( 6.530491241813343173, -0.6236753264481147419, 8.637950316517743587 ) ) ;
#11290=VECTOR ( 'NONE', #838, 1000.000000000000114 ) ;
#11297=AXIS2_PLACEMENT_3D ( 'NONE', #28647, #8075, #15272 ) ;
#11304=CARTESIAN_POINT ( 'NONE',  ( -2.162550801365593856, 2.228590825266444142, 2.752080473201636845 ) ) ;
#11305=ORIENTED_EDGE ( 'NONE', *, *, #22001, .F. ) ;
#11306=CARTESIAN_POINT ( 'NONE',  ( -5.600050800000000883, -2.331437884370912705, 1.887961173149512062 ) ) ;
#11309=CARTESIAN_POINT ( 'NONE',  ( -5.312942406915326821, -3.366872799099910998E-15, -3.000000000000000000 ) ) ;
#11312=CARTESIAN_POINT ( 'NONE',  ( -7.306376978575949366, -0.1572233378491242062, 2.999999999999999556 ) ) ;
#11326=EDGE_LOOP ( 'NONE', ( #25422, #17794, #24667, #555 ) ) ;
#11329=CARTESIAN_POINT ( 'NONE',  ( 6.524595395369783724, -7.902859683906637400, 3.538595500939559990 ) ) ;
#11330=DIRECTION ( 'NONE',  ( 0.000000000000000000, -0.9659258262890674240, 0.2588190451025241257 ) ) ;
#11331=ORIENTED_EDGE ( 'NONE', *, *, #20079, .F. ) ;
#11332=VECTOR ( 'NONE', #16248, 1000.000000000000000 ) ;
#11333=CARTESIAN_POINT ( 'NONE',  ( -3.462550801365593678, -3.521866450007987037, -0.3701630799359323931 ) ) ;
#11336=CIRCLE ( 'NONE', #6532, 8.750000000000000000 ) ;
#11352=CARTESIAN_POINT ( 'NONE',  ( -3.987550801365593145, 3.521866450007987037, 0.3701630799359328372 ) ) ;
#11353=LINE ( 'NONE', #10678, #6040 ) ;
#11357=VECTOR ( 'NONE', #14188, 1000.000000000000000 ) ;
#11358=EDGE_CURVE ( 'NONE', #2704, #27064, #20984, .T. ) ;
#11374=CARTESIAN_POINT ( 'NONE',  ( -2.812550801365592879, -1.828967928396026732, 3.368539882008728004 ) ) ;
#11377=CARTESIAN_POINT ( 'NONE',  ( 4.749760686538667009, 7.530955069117551304, -2.741043480754851380 ) ) ;
#11378=CARTESIAN_POINT ( 'NONE',  ( 7.249760686538667009, 3.748318449932404484, -7.906491560603625679 ) ) ;
#11380=CARTESIAN_POINT ( 'NONE',  ( -6.387550801365593500, 3.521866450007987037, 0.3701630799359328372 ) ) ;
#11389=CIRCLE ( 'NONE', #8196, 8.500000000000000000 ) ;
#11391=CARTESIAN_POINT ( 'NONE',  ( 6.530491482054475050, -0.8857639883442328665, -8.615020591497811964 ) ) ;
#11398=CARTESIAN_POINT ( 'NONE',  ( -8.000050800000000351, 0.000000000000000000, -3.000000000000000444 ) ) ;
#11404=CARTESIAN_POINT ( 'NONE',  ( 6.357667975083865386, -7.724391461487817523, 3.797112024431991362 ) ) ;
#11408=CYLINDRICAL_SURFACE ( 'NONE', #12859, 2.999999999999999112 ) ;
#11409=VERTEX_POINT ( 'NONE', #14968 ) ;
#11413=CARTESIAN_POINT ( 'NONE',  ( -8.000050800000002127, 3.543061387910618976, -0.5685797888652569521 ) ) ;
#11418=CARTESIAN_POINT ( 'NONE',  ( 5.489344046532322885, -3.969101778623974397, 7.082516960462303501 ) ) ;
#11426=DIRECTION ( 'NONE',  ( 0.000000000000000000, 0.000000000000000000, 1.000000000000000000 ) ) ;
#11431=DIRECTION ( 'NONE',  ( 0.000000000000000000, 0.000000000000000000, -1.000000000000000000 ) ) ;
#11445=ORIENTED_EDGE ( 'NONE', *, *, #26053, .F. ) ;
#11448=CARTESIAN_POINT ( 'NONE',  ( 5.489321486716459475, -8.012877392144806876, 1.307389195612950639 ) ) ;
#11454=CARTESIAN_POINT ( 'NONE',  ( 6.357667873252800028, -7.873899671211468387, -3.476490553296930131 ) ) ;
#11461=DIRECTION ( 'NONE',  ( 0.000000000000000000, -0.8191520442889866915, -0.5735764363510533759 ) ) ;
#11465=CARTESIAN_POINT ( 'NONE',  ( 3.499999999999999556, -6.106419733534973027, -3.518755179752868223 ) ) ;
#11469=CARTESIAN_POINT ( 'NONE',  ( -2.912942406915326909, 4.884725290497410777E-15, -2.999999999999999556 ) ) ;
#11471=B_SPLINE_CURVE_WITH_KNOTS ( 'NONE', 3,
 ( #14091, #3253, #757, #31831, #31490, #21456, #31674, #18961, #29148, #13900 ),
 .UNSPECIFIED., .F., .F.,
 ( 4, 2, 2, 2, 4 ),
 ( 2.740849916244211241E-07, 0.0005478761651001751599, 0.001095478245208724409, 0.001643080325317273658, 0.002190682405425823341 ),
 .UNSPECIFIED. ) ;
#11473=CARTESIAN_POINT ( 'NONE',  ( -6.650050802731187538, 1.887961173149511618, 2.331437884370912705 ) ) ;
#11475=EDGE_CURVE ( 'NONE', #10376, #5304, #3287, .T. ) ;
#11476=CARTESIAN_POINT ( 'NONE',  ( -7.950050800000001416, -3.113457007523259268, 0.9222479816126455399 ) ) ;
#11491=CARTESIAN_POINT ( 'NONE',  ( 7.249760686538667009, 8.014274990069656823, -8.669741416787380218E-17 ) ) ;
#11498=CARTESIAN_POINT ( 'NONE',  ( -3.212550801365593678, 1.828967928396027176, -3.368539882008727115 ) ) ;
#11508=EDGE_CURVE ( 'NONE', #13878, #24971, #21530, .T. ) ;
#11509=CARTESIAN_POINT ( 'NONE',  ( -2.607304909706597229, 1.062355717592091686, 3.000000000000001332 ) ) ;
#11510=ORIENTED_EDGE ( 'NONE', *, *, #10950, .F. ) ;
#11515=CARTESIAN_POINT ( 'NONE',  ( -2.269454921107341594, 1.816023192640135786, 3.086171154715485088 ) ) ;
#11517=CARTESIAN_POINT ( 'NONE',  ( 7.249760686538667009, 0.000000000000000000, 0.000000000000000000 ) ) ;
#11518=ORIENTED_EDGE ( 'NONE', *, *, #8981, .F. ) ;
#11524=VERTEX_POINT ( 'NONE', #605 ) ;
#11526=ORIENTED_EDGE ( 'NONE', *, *, #32492, .T. ) ;
#11527=ORIENTED_EDGE ( 'NONE', *, *, #16769, .T. ) ;
#11529=CARTESIAN_POINT ( 'NONE',  ( -2.762550801365593500, -2.752080473201636845, 2.228590825266444586 ) ) ;
#11533=CARTESIAN_POINT ( 'NONE',  ( 7.249760686538667009, -6.139290821770219786, -5.151476664237539360 ) ) ;
#11535=CARTESIAN_POINT ( 'NONE',  ( -5.287550801365593856, -2.752080473201636845, 2.228590825266444586 ) ) ;
#11537=DIRECTION ( 'NONE',  ( -1.000000000000000000, -0.000000000000000000, -0.000000000000000000 ) ) ;
#11540=CARTESIAN_POINT ( 'NONE',  ( 7.064632940817594076, -7.199384779417085767, -4.973063321323950348 ) ) ;
#11541=ORIENTED_EDGE ( 'NONE', *, *, #15380, .T. ) ;
#11550=DIRECTION ( 'NONE',  ( -1.000000000000000000, 0.000000000000000000, 0.000000000000000000 ) ) ;
#11551=CARTESIAN_POINT ( 'NONE',  ( -3.187550801365593767, 3.521866450007987037, 0.3701630799359328372 ) ) ;
#11557=DIRECTION ( 'NONE',  ( -1.000000000000000000, -0.000000000000000000, -0.000000000000000000 ) ) ;
#11558=ORIENTED_EDGE ( 'NONE', *, *, #13035, .T. ) ;
#11559=CARTESIAN_POINT ( 'NONE',  ( 7.249760686538667009, 6.139290821770327256, -5.151476664237414127 ) ) ;
#11563=ORIENTED_EDGE ( 'NONE', *, *, #7288, .T. ) ;
#11573=EDGE_LOOP ( 'NONE', ( #22756, #8378, #22758, #7129, #19933, #549, #17086, #26857, #24366, #24582, #2018, #16109, #24775, #29673, #6704, #27259, #21832, #13621, #2383, #9408, #17579, #14038, #1692, #2530, #14900, #25243, #12706, #16205, #30851, #817, #28248, #11228, #2282, #26335, #14534, #5131, #26084, #16501, #15865, #30327, #6301, #25916, #12238, #18893, #27274, #5920, #14803, #9312, #109, #2320, #31818, #29259, #13819, #1988, #18090, #30230, #18 ) ) ;
#11584=ADVANCED_FACE ( 'NONE', ( #15471 ), #15818, .F. ) ;
#11609=CARTESIAN_POINT ( 'NONE',  ( 6.037141812302424526, 1.028012177296197871, -8.411869123983606755 ) ) ;
#11615=CYLINDRICAL_SURFACE ( 'NONE', #31046, 8.500000000000000000 ) ;
#11624=CARTESIAN_POINT ( 'NONE',  ( -7.450050802731187360, 1.887961173149511618, 2.331437884370912705 ) ) ;
#11626=CARTESIAN_POINT ( 'NONE',  ( -6.100050799999999995, 0.3135853898029611342, -2.983565686104819648 ) ) ;
#11628=DIRECTION ( 'NONE',  ( -1.000000000000000000, 0.000000000000000000, 0.000000000000000000 ) ) ;
#11642=DIRECTION ( 'NONE',  ( -0.000000000000000000, -0.7071067811865507924, -0.7071067811865441310 ) ) ;
#11643=ORIENTED_EDGE ( 'NONE', *, *, #23466, .F. ) ;
#11645=EDGE_CURVE ( 'NONE', #29851, #4862, #16054, .T. ) ;
#11647=CARTESIAN_POINT ( 'NONE',  ( 6.880159540721329847, -7.943102264535277790, 3.624895993596839894 ) ) ;
#11655=ADVANCED_FACE ( 'NONE', ( #31708 ), #9271, .T. ) ;
#11656=CARTESIAN_POINT ( 'NONE',  ( 6.749760686538667009, 0.000000000000000000, 0.000000000000000000 ) ) ;
#11660=CARTESIAN_POINT ( 'NONE',  ( 5.887530024394193262, 2.518482652462555649, 8.008238305624853837 ) ) ;
#11661=ORIENTED_EDGE ( 'NONE', *, *, #6044, .F. ) ;
#11662=FACE_OUTER_BOUND ( 'NONE', #9336, .T. ) ;
#11663=EDGE_CURVE ( 'NONE', #516, #19070, #26515, .T. ) ;
#11670=EDGE_CURVE ( 'NONE', #1567, #22104, #1435, .T. ) ;
#11677=CARTESIAN_POINT ( 'NONE',  ( 5.612718825656739519, 6.163864706064027033, -5.432357446996346262 ) ) ;
#11681=CARTESIAN_POINT ( 'NONE',  ( 4.749760686538667009, -6.940565734314625423, 4.007137495034787555 ) ) ;
#11687=CARTESIAN_POINT ( 'NONE',  ( -3.187550801365593767, 3.521866450007987037, 0.3701630799359328372 ) ) ;
#11689=EDGE_CURVE ( 'NONE', #14000, #31571, #18825, .T. ) ;
#11695=CARTESIAN_POINT ( 'NONE',  ( -6.800050800000000173, 2.331437884370912705, -1.887961173149511618 ) ) ;
#11702=CARTESIAN_POINT ( 'NONE',  ( -2.637550801365593500, -1.088641768524163389, -3.675193018007246071 ) ) ;
#11706=CIRCLE ( 'NONE', #22407, 2.999999999999998668 ) ;
#11707=DIRECTION ( 'NONE',  ( -1.000000000000000000, 0.000000000000000000, -0.000000000000000000 ) ) ;
#11709=FACE_OUTER_BOUND ( 'NONE', #10641, .T. ) ;
#11711=ORIENTED_EDGE ( 'NONE', *, *, #11940, .F. ) ;
#11727=DIRECTION ( 'NONE',  ( -1.000000000000000000, -0.000000000000000000, -0.000000000000000000 ) ) ;
#11734=CIRCLE ( 'NONE', #31504, 8.500000000000000000 ) ;
#11739=AXIS2_PLACEMENT_3D ( 'NONE', #7232, #27619, #7545 ) ;
#11742=DIRECTION ( 'NONE',  ( 0.000000000000000000, 0.8191520442889889120, 0.5735764363510503783 ) ) ;
#11752=AXIS2_PLACEMENT_3D ( 'NONE', #3651, #11330, #6460 ) ;
#11754=AXIS2_PLACEMENT_3D ( 'NONE', #29917, #19220, #14339 ) ;
#11758=CARTESIAN_POINT ( 'NONE',  ( 5.377543748152549874, -7.892520144992443143, 1.391664247347202288 ) ) ;
#11760=EDGE_LOOP ( 'NONE', ( #1868, #7503, #24957, #25296 ) ) ;
#11764=VECTOR ( 'NONE', #30231, 1000.000000000000000 ) ;
#11772=AXIS2_PLACEMENT_3D ( 'NONE', #4175, #29760, #1510 ) ;
#11781=PLANE ( 'NONE',  #13445 ) ;
#11782=AXIS2_PLACEMENT_3D ( 'NONE', #11681, #21880, #32096 ) ;
#11785=CARTESIAN_POINT ( 'NONE',  ( -7.150050802731187538, -2.983565686104819648, -0.3135853898029605791 ) ) ;
#11787=CARTESIAN_POINT ( 'NONE',  ( -7.637550801365593500, -3.675193018007246071, 1.088641768524163167 ) ) ;
#11789=ADVANCED_FACE ( 'NONE', ( #13775 ), #24156, .F. ) ;
#11791=CARTESIAN_POINT ( 'NONE',  ( -5.407304909706597051, -1.062355717592097015, -2.999999999999998668 ) ) ;
#11793=VERTEX_POINT ( 'NONE', #27502 ) ;
#11795=CARTESIAN_POINT ( 'NONE',  ( -7.200050800000000528, -2.331437884370912705, 1.887961173149512062 ) ) ;
#11799=VECTOR ( 'NONE', #8456, 1000.000000000000000 ) ;
#11802=ADVANCED_FACE ( 'NONE', ( #27152 ), #9772, .T. ) ;
#11807=CARTESIAN_POINT ( 'NONE',  ( -5.757304906975409864, 1.062355717592095683, 2.999999999999999112 ) ) ;
#11815=DIRECTION ( 'NONE',  ( 1.000000000000000000, -0.000000000000000000, -0.000000000000000000 ) ) ;
#11824=ADVANCED_FACE ( 'NONE', ( #11963 ), #32865, .F. ) ;
#11826=LINE ( 'NONE', #19862, #13416 ) ;
#11829=VERTEX_POINT ( 'NONE', #12607 ) ;
#11831=CARTESIAN_POINT ( 'NONE',  ( 7.249760686538667009, 2.318425219014230265, 8.437262856154170265 ) ) ;
#11837=LINE ( 'NONE', #17006, #14043 ) ;
#11840=VECTOR ( 'NONE', #18563, 1000.000000000000000 ) ;
#11845=CIRCLE ( 'NONE', #10248, 8.500000000000000000 ) ;
#11848=ADVANCED_FACE ( 'NONE', ( #30193 ), #32690, .T. ) ;
#11859=CARTESIAN_POINT ( 'NONE',  ( -2.212550801365593234, 3.368539882008727115, 1.828967928396027176 ) ) ;
#11860=AXIS2_PLACEMENT_3D ( 'NONE', #12615, #30711, #20311 ) ;
#11866=CARTESIAN_POINT ( 'NONE',  ( -4.587550801365592790, -0.3701630799359326152, 3.521866450007987037 ) ) ;
#11867=VECTOR ( 'NONE', #22031, 1000.000000000000000 ) ;
#11872=ORIENTED_EDGE ( 'NONE', *, *, #32033, .T. ) ;
#11878=CARTESIAN_POINT ( 'NONE',  ( 0.000000000000000000, 5.241389472434724084, -4.711457988287002685 ) ) ;
#11882=CARTESIAN_POINT ( 'NONE',  ( -6.300050802731188782, -2.853674364686378695, -1.549418761218566809 ) ) ;
#11884=CIRCLE ( 'NONE', #32708, 8.750000000000000000 ) ;
#11889=CARTESIAN_POINT ( 'NONE',  ( -2.937550801365593323, -1.828967928396026510, 3.368539882008728004 ) ) ;
#11899=CARTESIAN_POINT ( 'NONE',  ( 6.749760686538667009, 6.429395695523604153E-16, -5.000000000000000000 ) ) ;
#11907=VERTEX_POINT ( 'NONE', #4255 ) ;
#11908=VERTEX_POINT ( 'NONE', #17455 ) ;
#11913=EDGE_LOOP ( 'NONE', ( #5093, #19259, #26812 ) ) ;
#11917=CARTESIAN_POINT ( 'NONE',  ( 5.489321606599603776, -2.874206582856462688, 7.593050043411102124 ) ) ;
#11923=DIRECTION ( 'NONE',  ( 0.000000000000000000, 0.4226182617406930020, 0.9063077870366529343 ) ) ;
#11924=CIRCLE ( 'NONE', #29008, 8.750000000000000000 ) ;
#11926=CARTESIAN_POINT ( 'NONE',  ( 7.249760686538667009, -2.318425219014174754, -8.437262856154184476 ) ) ;
#11932=CARTESIAN_POINT ( 'NONE',  ( -6.506376978575948655, -0.1572233378491221800, 3.000000000000000000 ) ) ;
#11934=EDGE_CURVE ( 'NONE', #12106, #10302, #2439, .T. ) ;
#11938=( BOUNDED_CURVE ( )  B_SPLINE_CURVE ( 2, ( #2101, #20013, #7127, #24990, #19826, #22496, #27518, #27168, #30208, #4273, #19662 ),
 .UNSPECIFIED., .F., .F. ) 
 B_SPLINE_CURVE_WITH_KNOTS ( ( 3, 2, 2, 2, 2, 3 ),
 ( 0.6228822619934377691, 0.6250000000000000000, 0.6406250000000000000, 0.6562500000000000000, 0.6718750000000000000, 0.6853822619934377691 ),
 .UNSPECIFIED. ) 
 CURVE ( )  GEOMETRIC_REPRESENTATION_ITEM ( )  RATIONAL_B_SPLINE_CURVE ( ( 0.9821626249036861100, 0.9896829947469995004, 1.000000000000000000, 0.9238795325112867385, 1.000000000000000000, 0.9238795325112867385, 1.000000000000000000, 0.9238795325112867385, 1.000000000000000000, 0.9341965377642872381, 0.9821626249036861100 ) ) 
 REPRESENTATION_ITEM ( '' )  );
#11940=EDGE_CURVE ( 'NONE', #15458, #13197, #17306, .T. ) ;
#11947=ORIENTED_EDGE ( 'NONE', *, *, #10579, .T. ) ;
#11951=VERTEX_POINT ( 'NONE', #5422 ) ;
#11954=ORIENTED_EDGE ( 'NONE', *, *, #29748, .T. ) ;
#11958=EDGE_LOOP ( 'NONE', ( #1342, #13504, #2291, #27387 ) ) ;
#11960=CARTESIAN_POINT ( 'NONE',  ( -1.762942409646513164, -5.022711880624455567E-15, 2.999999999999999556 ) ) ;
#11963=FACE_OUTER_BOUND ( 'NONE', #16790, .T. ) ;
#11964=VECTOR ( 'NONE', #32064, 1000.000000000000114 ) ;
#11966=PLANE ( 'NONE',  #2230 ) ;
#11968=EDGE_CURVE ( 'NONE', #19129, #31349, #4478, .T. ) ;
#11974=CARTESIAN_POINT ( 'NONE',  ( -6.200050802731188249, -0.9222479816126459840, -3.113457007523259268 ) ) ;
#11977=CARTESIAN_POINT ( 'NONE',  ( -3.950050800000000084, -3.113457007523259268, 0.9222479816126455399 ) ) ;
#11984=CARTESIAN_POINT ( 'NONE',  ( 0.000000000000000000, 0.000000000000000000, 0.000000000000000000 ) ) ;
#11990=CARTESIAN_POINT ( 'NONE',  ( 5.377543748152550762, -1.391664247347281780, 7.892520144992429820 ) ) ;
#12009=CARTESIAN_POINT ( 'NONE',  ( -2.506376978575949099, -0.1572233378491262878, 2.999999999999999556 ) ) ;
#12011=EDGE_LOOP ( 'NONE', ( #10517, #10740, #5444, #10872 ) ) ;
#12015=ORIENTED_EDGE ( 'NONE', *, *, #21807, .T. ) ;
#12016=CARTESIAN_POINT ( 'NONE',  ( -8.354531657079157014, 3.105402419394639235, -0.9198621039125850496 ) ) ;
#12018=FACE_OUTER_BOUND ( 'NONE', #4697, .T. ) ;
#12026=EDGE_CURVE ( 'NONE', #21233, #28961, #10859, .T. ) ;
#12028=CARTESIAN_POINT ( 'NONE',  ( 6.530491712438077023, 3.778856441136722477, 7.792522225867655195 ) ) ;
#12029=PLANE ( 'NONE',  #2805 ) ;
#12030=ORIENTED_EDGE ( 'NONE', *, *, #1911, .T. ) ;
#12033=CARTESIAN_POINT ( 'NONE',  ( -2.362550801365593589, 2.752080473201636845, -2.228590825266444142 ) ) ;
#12038=CARTESIAN_POINT ( 'NONE',  ( -3.337550801365593678, 1.828967928396027176, -3.368539882008727115 ) ) ;
#12052=LINE ( 'NONE', #9873, #5514 ) ;
#12054=CARTESIAN_POINT ( 'NONE',  ( -3.687550801365593323, -2.752080473201636845, 2.228590825266444586 ) ) ;
#12062=CYLINDRICAL_SURFACE ( 'NONE', #24071, 6.248999999999999666 ) ;
#12063=ORIENTED_EDGE ( 'NONE', *, *, #1444, .F. ) ;
#12064=EDGE_CURVE ( 'NONE', #3656, #24705, #4073, .T. ) ;
#12069=EDGE_LOOP ( 'NONE', ( #7792, #9794, #31882, #20924 ) ) ;
#12083=DIRECTION ( 'NONE',  ( 0.000000000000000000, 0.9510565162951544194, -0.3090169943749449533 ) ) ;
#12086=CARTESIAN_POINT ( 'NONE',  ( 3.499999999999999556, -6.200809695932780308, 0.7745709230444962623 ) ) ;
#12091=CARTESIAN_POINT ( 'NONE',  ( -6.887550801365593500, -2.752080473201636845, 2.228590825266444586 ) ) ;
#12101=CARTESIAN_POINT ( 'NONE',  ( 4.749760686538667009, 6.139290821770327256, -5.151476664237414127 ) ) ;
#12106=VERTEX_POINT ( 'NONE', #24434 ) ;
#12109=ORIENTED_EDGE ( 'NONE', *, *, #24301, .F. ) ;
#12116=EDGE_CURVE ( 'NONE', #15020, #18257, #29550, .T. ) ;
#12124=CARTESIAN_POINT ( 'NONE',  ( -4.900050802731187538, -1.549418761218565477, 2.853674364686380471 ) ) ;
#12126=CARTESIAN_POINT ( 'NONE',  ( -2.900050800000000706, 0.3135853898029611342, -2.983565686104819648 ) ) ;
#12129=VERTEX_POINT ( 'NONE', #31826 ) ;
#12136=ORIENTED_EDGE ( 'NONE', *, *, #32790, .F. ) ;
#12138=DIRECTION ( 'NONE',  ( 1.000000000000000000, -0.000000000000000000, 0.000000000000000000 ) ) ;
#12143=VERTEX_POINT ( 'NONE', #13589 ) ;
#12144=EDGE_CURVE ( 'NONE', #10538, #26682, #14466, .T. ) ;
#12148=CARTESIAN_POINT ( 'NONE',  ( -10.00000000000000000, 0.000000000000000000, 0.000000000000000000 ) ) ;
#12155=CARTESIAN_POINT ( 'NONE',  ( -8.000050800000003903, 3.519328457705152235, 0.3516833816935649448 ) ) ;
#12156=CARTESIAN_POINT ( 'NONE',  ( 6.530491751506347420, -6.216163082443024734, -6.030130624359239633 ) ) ;
#12158=CARTESIAN_POINT ( 'NONE',  ( 4.749760686538667009, 8.385837730238846314E-14, -8.014274990069656823 ) ) ;
#12159=ORIENTED_EDGE ( 'NONE', *, *, #31043, .F. ) ;
#12162=CARTESIAN_POINT ( 'NONE',  ( -5.304531657079158080, 0.3127741368606810068, -2.975847129947406522 ) ) ;
#12169=EDGE_CURVE ( 'NONE', #9705, #19878, #24286, .T. ) ;
#12182=CARTESIAN_POINT ( 'NONE',  ( 6.530491482054475050, 8.615020591497813740, -0.8857639883442027795 ) ) ;
#12183=ORIENTED_EDGE ( 'NONE', *, *, #1183, .T. ) ;
#12184=CARTESIAN_POINT ( 'NONE',  ( -4.787550801365593856, 3.521866450007987037, 0.3701630799359328372 ) ) ;
#12186=EDGE_CURVE ( 'NONE', #5075, #1352, #26363, .T. ) ;
#12188=CARTESIAN_POINT ( 'NONE',  ( 3.499999999999999556, 4.561279057474472154, -4.271385531633124621 ) ) ;
#12190=CARTESIAN_POINT ( 'NONE',  ( 6.357667975083868050, -7.150591204917362553, -4.790963222208079131 ) ) ;
#12192=DIRECTION ( 'NONE',  ( -1.000000000000000000, -0.000000000000000000, -0.000000000000000000 ) ) ;
#12196=CARTESIAN_POINT ( 'NONE',  ( -6.400050802731188426, -3.113457007523259268, 0.9222479816126455399 ) ) ;
#12202=ORIENTED_EDGE ( 'NONE', *, *, #27448, .T. ) ;
#12203=CARTESIAN_POINT ( 'NONE',  ( 7.249760686538667009, 7.530955069117513112, 2.741043480754951744 ) ) ;
#12214=VERTEX_POINT ( 'NONE', #25286 ) ;
#12215=EDGE_CURVE ( 'NONE', #5480, #29891, #27773, .T. ) ;
#12219=DIRECTION ( 'NONE',  ( 0.000000000000000000, -0.7431448254773862505, -0.6691306063588670083 ) ) ;
#12220=ORIENTED_EDGE ( 'NONE', *, *, #22277, .T. ) ;
#12221=CARTESIAN_POINT ( 'NONE',  ( 5.377543748152548986, 4.007137495034812424, 6.940565734314612101 ) ) ;
#12237=CARTESIAN_POINT ( 'NONE',  ( -5.337550801365593678, -1.828967928396026732, 3.368539882008728004 ) ) ;
#12238=ORIENTED_EDGE ( 'NONE', *, *, #24697, .T. ) ;
#12241=LINE ( 'NONE', #25113, #2366 ) ;
#12254=EDGE_CURVE ( 'NONE', #12214, #1670, #9230, .T. ) ;
#12256=DIRECTION ( 'NONE',  ( 0.000000000000000000, -0.9063077870366482713, 0.4226182617407029940 ) ) ;
#12260=CARTESIAN_POINT ( 'NONE',  ( 0.000000000000000000, 0.000000000000000000, 0.000000000000000000 ) ) ;
#12274=DIRECTION ( 'NONE',  ( -1.000000000000000000, -0.000000000000000000, -0.000000000000000000 ) ) ;
#12276=CARTESIAN_POINT ( 'NONE',  ( -3.900050802731187982, -2.853674364686378695, -1.549418761218566809 ) ) ;
#12278=CARTESIAN_POINT ( 'NONE',  ( -3.650050800000000706, 1.549418761218566143, -2.853674364686379583 ) ) ;
#12282=CARTESIAN_POINT ( 'NONE',  ( -3.900050802731187982, -2.853674364686378695, -1.549418761218566809 ) ) ;
#12284=CARTESIAN_POINT ( 'NONE',  ( -1.850050802731187716, 1.887961173149511618, 2.331437884370912705 ) ) ;
#12286=EDGE_CURVE ( 'NONE', #28961, #16345, #31733, .T. ) ;
#12287=AXIS2_PLACEMENT_3D ( 'NONE', #10217, #30659, #7736 ) ;
#12303=CARTESIAN_POINT ( 'NONE',  ( -3.250050802731187183, -2.331437884370912705, 1.887961173149512062 ) ) ;
#12310=AXIS2_PLACEMENT_3D ( 'NONE', #23779, #29128, #31646 ) ;
#12311=CARTESIAN_POINT ( 'NONE',  ( -8.000050800000002127, 2.629983047553211328, 2.147054542866906779 ) ) ;
#12312=CARTESIAN_POINT ( 'NONE',  ( 7.064632951172269415, -6.226446564517874371, -6.147671362329281131 ) ) ;
#12316=CARTESIAN_POINT ( 'NONE',  ( -6.312550801365593323, 3.675193018007247403, -1.088641768524161391 ) ) ;
#12318=CARTESIAN_POINT ( 'NONE',  ( -7.454531657079158435, 2.846291840500173365, 1.545410377633946952 ) ) ;
#12332=VERTEX_POINT ( 'NONE', #7058 ) ;
#12333=DIRECTION ( 'NONE',  ( 1.000000000000000000, -0.000000000000000000, -0.000000000000000000 ) ) ;
#12337=VECTOR ( 'NONE', #6674, 1000.000000000000114 ) ;
#12339=CARTESIAN_POINT ( 'NONE',  ( 6.880159396099833735, 7.882559112973164694, 3.754731129947811219 ) ) ;
#12348=CARTESIAN_POINT ( 'NONE',  ( -4.837550801365592790, 3.675193018007247403, -1.088641768524161391 ) ) ;
#12355=VERTEX_POINT ( 'NONE', #20116 ) ;
#12357=AXIS2_PLACEMENT_3D ( 'NONE', #11465, #6124, #1098 ) ;
#12361=CARTESIAN_POINT ( 'NONE',  ( 5.377543748152548986, 7.892520144992435149, 1.391664247347255134 ) ) ;
#12367=CIRCLE ( 'NONE', #3323, 8.750000000000000000 ) ;
#12380=AXIS2_PLACEMENT_3D ( 'NONE', #6876, #9899, #32483 ) ;
#12381=ORIENTED_EDGE ( 'NONE', *, *, #11358, .T. ) ;
#12382=CARTESIAN_POINT ( 'NONE',  ( 3.499999999999999556, -8.497168642645963388, -0.2193742428685781509 ) ) ;
#12395=CARTESIAN_POINT ( 'NONE',  ( 3.499999999999999556, 0.000000000000000000, 0.000000000000000000 ) ) ;
#12401=CIRCLE ( 'NONE', #18807, 2.750000000000000444 ) ;
#12416=CARTESIAN_POINT ( 'NONE',  ( -7.387550801365593500, 0.3701630799359330593, -3.521866450007987037 ) ) ;
#12418=AXIS2_PLACEMENT_3D ( 'NONE', #20062, #15344, #15193 ) ;
#12420=CYLINDRICAL_SURFACE ( 'NONE', #15159, 8.500000000000000000 ) ;
#12430=DIRECTION ( 'NONE',  ( 1.000000000000000000, -0.000000000000000000, 0.000000000000000000 ) ) ;
#12435=ORIENTED_EDGE ( 'NONE', *, *, #10634, .F. ) ;
#12441=VERTEX_POINT ( 'NONE', #26104 ) ;
#12449=CARTESIAN_POINT ( 'NONE',  ( -3.362942409646513031, -5.022711880624455567E-15, 2.999999999999999556 ) ) ;
#12451=CARTESIAN_POINT ( 'NONE',  ( 7.249760686538667009, 0.000000000000000000, 0.000000000000000000 ) ) ;
#12458=DIRECTION ( 'NONE',  ( 0.000000000000000000, 0.2588190451025185190, -0.9659258262890689783 ) ) ;
#12460=CARTESIAN_POINT ( 'NONE',  ( -3.250050802731187183, -2.331437884370912705, 1.887961173149512062 ) ) ;
#12464=CARTESIAN_POINT ( 'NONE',  ( -4.450050800000000528, 1.549418761218566143, -2.853674364686379583 ) ) ;
#12482=VECTOR ( 'NONE', #28621, 1000.000000000000000 ) ;
#12486=CARTESIAN_POINT ( 'NONE',  ( -5.712942406915326288, 3.284080845023683730E-15, 3.000000000000000000 ) ) ;
#12496=B_SPLINE_CURVE_WITH_KNOTS ( 'NONE', 3,
 ( #19296, #16791, #29496, #26348, #8915, #11270, #928, #31694, #6594, #16289 ),
 .UNSPECIFIED., .F., .F.,
 ( 4, 2, 2, 2, 4 ),
 ( 1.968338519012340724E-07, 0.0005467927057105484217, 0.001093388577569195637, 0.001639984449427842744, 0.002186580321286490068 ),
 .UNSPECIFIED. ) ;
#12498=EDGE_CURVE ( 'NONE', #10411, #18566, #5380, .T. ) ;
#12505=CARTESIAN_POINT ( 'NONE',  ( -6.362550801365593145, 2.752080473201636845, -2.228590825266444142 ) ) ;
#12507=CARTESIAN_POINT ( 'NONE',  ( -5.954531657079157547, 3.105402419394639235, -0.9198621039125850496 ) ) ;
#12508=CIRCLE ( 'NONE', #16247, 5.000000000000000000 ) ;
#12509=CARTESIAN_POINT ( 'NONE',  ( 5.377543748152548098, 6.940565734314597002, 4.007137495034836405 ) ) ;
#12510=DIRECTION ( 'NONE',  ( 0.000000000000000000, 0.000000000000000000, 1.000000000000000000 ) ) ;
#12512=FACE_OUTER_BOUND ( 'NONE', #11573, .T. ) ;
#12515=ORIENTED_EDGE ( 'NONE', *, *, #2113, .T. ) ;
#12516=CARTESIAN_POINT ( 'NONE',  ( -3.650050800000000262, 1.549418761218566143, -2.853674364686379583 ) ) ;
#12522=DIRECTION ( 'NONE',  ( 0.000000000000000000, 0.000000000000000000, 1.000000000000000000 ) ) ;
#12530=CARTESIAN_POINT ( 'NONE',  ( -5.312550801365592434, 1.088641768524161613, 3.675193018007247403 ) ) ;
#12535=DIRECTION ( 'NONE',  ( -1.000000000000000000, 0.000000000000000000, 0.000000000000000000 ) ) ;
#12536=VERTEX_POINT ( 'NONE', #13076 ) ;
#12540=B_SPLINE_CURVE_WITH_KNOTS ( 'NONE', 3,
 ( #17884, #32939, #15352, #12182, #17528, #20070, #25557, #30266, #7189, #15011 ),
 .UNSPECIFIED., .F., .F.,
 ( 4, 2, 2, 2, 4 ),
 ( 1.968338519002063038E-07, 0.0005467928198071719554, 0.001093388805762443572, 0.001639984791717715188, 0.002186580777672987239 ),
 .UNSPECIFIED. ) ;
#12541=EDGE_CURVE ( 'NONE', #11793, #26254, #22778, .T. ) ;
#12546=( BOUNDED_CURVE ( )  B_SPLINE_CURVE ( 2, ( #13797, #14151, #6294, #19167, #1614, #3982, #14461, #22186, #26863, #11807, #22015 ),
 .UNSPECIFIED., .F., .F. ) 
 B_SPLINE_CURVE_WITH_KNOTS ( ( 3, 2, 2, 2, 2, 3 ),
 ( 0.3728822619934377136, 0.3750000000000000000, 0.3906250000000000000, 0.4062500000000000000, 0.4218750000000000000, 0.4353822619934377136 ),
 .UNSPECIFIED. ) 
 CURVE ( )  GEOMETRIC_REPRESENTATION_ITEM ( )  RATIONAL_B_SPLINE_CURVE ( ( 0.9821626249036857770, 0.9896829947469991673, 1.000000000000000000, 0.9238795325112867385, 1.000000000000000000, 0.9238795325112867385, 1.000000000000000000, 0.9238795325112867385, 1.000000000000000000, 0.9341965377642874602, 0.9821626249036857770 ) ) 
 REPRESENTATION_ITEM ( '' )  );
#12547=CARTESIAN_POINT ( 'NONE',  ( 7.249760686538667009, 7.892520144992435149, 1.391664247347255134 ) ) ;
#12553=ORIENTED_EDGE ( 'NONE', *, *, #5165, .F. ) ;
#12561=CARTESIAN_POINT ( 'NONE',  ( -7.112550801365592257, 3.675193018007246959, -1.088641768524161391 ) ) ;
#12564=CARTESIAN_POINT ( 'NONE',  ( 0.000000000000000000, 8.357095590591338663, -1.552080310331533486 ) ) ;
#12575=EDGE_CURVE ( 'NONE', #9383, #13763, #30964, .T. ) ;
#12576=CARTESIAN_POINT ( 'NONE',  ( 7.249760686538667009, -0.7071067811865734409, 8.721381771256202953 ) ) ;
#12579=CARTESIAN_POINT ( 'NONE',  ( 5.885541806331895387, 7.076443837534019288, -4.514241479885472863 ) ) ;
#12581=VERTEX_POINT ( 'NONE', #7549 ) ;
#12584=CARTESIAN_POINT ( 'NONE',  ( -5.937550801365592434, -3.368539882008727115, -1.828967928396027842 ) ) ;
#12585=EDGE_LOOP ( 'NONE', ( #28407, #15550, #16401 ) ) ;
#12586=CARTESIAN_POINT ( 'NONE',  ( -5.362942409646513475, -3.366872799099910998E-15, -3.000000000000000000 ) ) ;
#12587=CARTESIAN_POINT ( 'NONE',  ( 5.612974384376776982, 7.213266193303311979, -3.934067627273127865 ) ) ;
#12593=ORIENTED_EDGE ( 'NONE', *, *, #15919, .F. ) ;
#12595=CARTESIAN_POINT ( 'NONE',  ( 3.499999999999999556, 8.265874651078044977, -1.981241088980699061 ) ) ;
#12598=CARTESIAN_POINT ( 'NONE',  ( 6.356382399260309235, -4.790388219480510301, -7.150437133400980194 ) ) ;
#12605=DIRECTION ( 'NONE',  ( 0.000000000000000000, -0.9961946980917446570, -0.08715574274766962892 ) ) ;
#12607=CARTESIAN_POINT ( 'NONE',  ( 7.249760686538667009, -5.151476664237435443, -6.139290821770307716 ) ) ;
#12608=( BOUNDED_CURVE ( )  B_SPLINE_CURVE ( 2, ( #14450, #11312, #1606, #6286, #11795, #16470, #26677, #3789, #13958, #24179, #28025 ),
 .UNSPECIFIED., .F., .F. ) 
 B_SPLINE_CURVE_WITH_KNOTS ( ( 3, 2, 2, 2, 2, 3 ),
 ( 0.1853822619934377414, 0.1875000000000000000, 0.2031250000000000000, 0.2187500000000000000, 0.2343750000000000000, 0.2478822619934377414 ),
 .UNSPECIFIED. ) 
 CURVE ( )  GEOMETRIC_REPRESENTATION_ITEM ( )  RATIONAL_B_SPLINE_CURVE ( ( 0.9821626249036861100, 0.9896829947469993893, 1.000000000000000000, 0.9238795325112867385, 1.000000000000000000, 0.9238795325112867385, 1.000000000000000000, 0.9238795325112867385, 1.000000000000000000, 0.9341965377642873491, 0.9821626249036861100 ) ) 
 REPRESENTATION_ITEM ( '' )  );
#12610=EDGE_CURVE ( 'NONE', #16442, #6099, #16493, .T. ) ;
#12611=FACE_BOUND ( 'NONE', #29202, .T. ) ;
#12615=CARTESIAN_POINT ( 'NONE',  ( 3.499999999999999556, 0.000000000000000000, 0.000000000000000000 ) ) ;
#12619=CARTESIAN_POINT ( 'NONE',  ( -3.650050802731187094, 2.331437884370912705, -1.887961173149511618 ) ) ;
#12621=CARTESIAN_POINT ( 'NONE',  ( -6.787550801365593856, -3.521866450007987037, -0.3701630799359323931 ) ) ;
#12624=CARTESIAN_POINT ( 'NONE',  ( 7.064632951172269415, -5.064320921489772864, -7.135485519862048598 ) ) ;
#12625=CARTESIAN_POINT ( 'NONE',  ( 6.356382477965130562, -5.959271875177110545, -6.209963745178070482 ) ) ;
#12628=EDGE_CURVE ( 'NONE', #26246, #9383, #22202, .T. ) ;
#12645=CARTESIAN_POINT ( 'NONE',  ( 6.037141879243262288, -6.194548269014922504, 5.783072176360625427 ) ) ;
#12654=ORIENTED_EDGE ( 'NONE', *, *, #16956, .T. ) ;
#12655=CARTESIAN_POINT ( 'NONE',  ( -6.162550801365593856, 2.228590825266444142, 2.752080473201636845 ) ) ;
#12657=EDGE_CURVE ( 'NONE', #6174, #31510, #6467, .T. ) ;
#12658=CARTESIAN_POINT ( 'NONE',  ( -6.304531657079157192, -2.975847129947406522, -0.3127741368606805072 ) ) ;
#12662=CARTESIAN_POINT ( 'NONE',  ( -10.00000000000000000, 0.000000000000000000, 0.000000000000000000 ) ) ;
#12667=CARTESIAN_POINT ( 'NONE',  ( 5.377543748152548986, 1.391664247347228045, 7.892520144992438702 ) ) ;
#12671=CARTESIAN_POINT ( 'NONE',  ( 6.883866601413089370, 4.949663153219632683, -7.193114723270757516 ) ) ;
#12673=DIRECTION ( 'NONE',  ( -1.000000000000000000, -0.000000000000000000, -0.000000000000000000 ) ) ;
#12675=ADVANCED_FACE ( 'NONE', ( #8379 ), #3208, .F. ) ;
#12676=CARTESIAN_POINT ( 'NONE',  ( -8.000050800000002127, -2.680285808942373560, 1.376672160408170198 ) ) ;
#12682=CARTESIAN_POINT ( 'NONE',  ( -6.262550801365593500, 3.521866450007987037, 0.3701630799359328372 ) ) ;
#12684=CARTESIAN_POINT ( 'NONE',  ( 3.499999999999999556, 5.241389472434724084, -4.711457988287002685 ) ) ;
#12696=CARTESIAN_POINT ( 'NONE',  ( 1.750000000000000222, 4.058600654062850310, 7.468451026206211374 ) ) ;
#12697=LINE ( 'NONE', #18212, #30595 ) ;
#12700=DIRECTION ( 'NONE',  ( 0.000000000000000000, 0.9063077870366514910, -0.4226182617406961106 ) ) ;
#12706=ORIENTED_EDGE ( 'NONE', *, *, #21871, .T. ) ;
#12714=CARTESIAN_POINT ( 'NONE',  ( 5.377543748152549874, -2.741043480754877582, -7.530955069117540646 ) ) ;
#12723=ORIENTED_EDGE ( 'NONE', *, *, #18670, .F. ) ;
#12730=ORIENTED_EDGE ( 'NONE', *, *, #837, .F. ) ;
#12733=CARTESIAN_POINT ( 'NONE',  ( -6.237550801365593145, 1.088641768524161613, 3.675193018007246959 ) ) ;
#12736=CARTESIAN_POINT ( 'NONE',  ( 5.377543748152548986, 6.940565734314653845, -4.007137495034738706 ) ) ;
#12742=CARTESIAN_POINT ( 'NONE',  ( 5.377543748152551650, 6.139290821770257089, 5.151476664237498504 ) ) ;
#12743=ORIENTED_EDGE ( 'NONE', *, *, #12981, .F. ) ;
#12762=CARTESIAN_POINT ( 'NONE',  ( 6.524595126109738352, 8.613374939462827840, 0.8869162863044809386 ) ) ;
#12763=CARTESIAN_POINT ( 'NONE',  ( 0.000000000000000000, 1.459547570502368385, 6.894905428400277536 ) ) ;
#12767=CARTESIAN_POINT ( 'NONE',  ( -6.337550801365593678, 3.368539882008727115, 1.828967928396026954 ) ) ;
#12786=EDGE_LOOP ( 'NONE', ( #8292, #26170, #8769, #30947 ) ) ;
#12788=DIRECTION ( 'NONE',  ( -1.000000000000000000, 0.000000000000000000, 0.000000000000000000 ) ) ;
#12789=LINE ( 'NONE', #9623, #1282 ) ;
#12792=CARTESIAN_POINT ( 'NONE',  ( 6.880159329304571081, -6.224287131858844191, 6.122988934091259772 ) ) ;
#12795=PLANE ( 'NONE',  #20368 ) ;
#12797=CARTESIAN_POINT ( 'NONE',  ( -8.000050800000009232, 0.3876333558353860509, 3.203076781024368547 ) ) ;
#12804=CARTESIAN_POINT ( 'NONE',  ( -6.512550801365594388, -1.088641768524163389, -3.675193018007246071 ) ) ;
#12806=CARTESIAN_POINT ( 'NONE',  ( -8.050050799999999285, -1.549418761218565477, 2.853674364686380471 ) ) ;
#12812=VERTEX_POINT ( 'NONE', #9634 ) ;
#12824=CARTESIAN_POINT ( 'NONE',  ( 5.612974259723590542, 7.786824029658800939, -2.621729824970306044 ) ) ;
#12827=CARTESIAN_POINT ( 'NONE',  ( -7.500050802731187183, 2.853674364686379583, 1.549418761218565921 ) ) ;
#12835=CARTESIAN_POINT ( 'NONE',  ( -5.362550801365593145, 2.228590825266444142, 2.752080473201636845 ) ) ;
#12837=CARTESIAN_POINT ( 'NONE',  ( 6.883866621640342132, -7.111352071735057123, 5.066432324612699212 ) ) ;
#12841=B_SPLINE_CURVE_WITH_KNOTS ( 'NONE', 3,
 ( #5633, #30732, #8296, #5779, #18636, #5459, #7804, #440, #28834, #26174 ),
 .UNSPECIFIED., .F., .F.,
 ( 4, 2, 2, 2, 4 ),
 ( 1.968338519010642687E-07, 0.0005467930078056964724, 0.001093389181759491739, 0.001639985355713287222, 0.002186581529667082704 ),
 .UNSPECIFIED. ) ;
#12852=CIRCLE ( 'NONE', #18732, 3.000000000000000000 ) ;
#12854=DIRECTION ( 'NONE',  ( -1.000000000000000000, 0.000000000000000000, 0.000000000000000000 ) ) ;
#12859=AXIS2_PLACEMENT_3D ( 'NONE', #21604, #1890, #6713 ) ;
#12862=ORIENTED_EDGE ( 'NONE', *, *, #28673, .F. ) ;
#12865=CARTESIAN_POINT ( 'NONE',  ( -5.200050802731187360, 3.113457007523260156, -0.9222479816126439855 ) ) ;
#12871=CARTESIAN_POINT ( 'NONE',  ( -6.912550801365593856, 1.088641768524161613, 3.675193018007246959 ) ) ;
#12874=VECTOR ( 'NONE', #7692, 1000.000000000000000 ) ;
#12879=VERTEX_POINT ( 'NONE', #24864 ) ;
#12892=B_SPLINE_CURVE_WITH_KNOTS ( 'NONE', 3,
 ( #12667, #4816, #10148, #20372, #14833, #14996, #6544, #32131, #21911, #30587 ),
 .UNSPECIFIED., .F., .F.,
 ( 4, 2, 2, 2, 4 ),
 ( 3.032460776719120378E-07, 0.0005479053915603968516, 0.001095507537043121900, 0.001643109682525846840, 0.002190711828008571564 ),
 .UNSPECIFIED. ) ;
#12894=CARTESIAN_POINT ( 'NONE',  ( 6.749760686538667009, 0.000000000000000000, 0.000000000000000000 ) ) ;
#12903=VECTOR ( 'NONE', #9320, 1000.000000000000227 ) ;
#12905=CIRCLE ( 'NONE', #12380, 2.999999999999999556 ) ;
#12907=CARTESIAN_POINT ( 'NONE',  ( 7.064632940817592299, 7.906491560603718050, -3.748318449932210417 ) ) ;
#12909=CIRCLE ( 'NONE', #25209, 2.999999999999999112 ) ;
#12910=CARTESIAN_POINT ( 'NONE',  ( 7.249760686538667009, 2.210816291636326092, -8.466096581343458993 ) ) ;
#12914=DIRECTION ( 'NONE',  ( 0.000000000000000000, -0.7071067811865442421, 0.7071067811865509034 ) ) ;
#12931=AXIS2_PLACEMENT_3D ( 'NONE', #31872, #24946, #27288 ) ;
#12932=CARTESIAN_POINT ( 'NONE',  ( 3.499999999999999556, 3.771202944355708020, 4.982773259188384429 ) ) ;
#12942=EDGE_CURVE ( 'NONE', #516, #11273, #22613, .T. ) ;
#12943=EDGE_CURVE ( 'NONE', #16345, #31994, #5643, .T. ) ;
#12948=CARTESIAN_POINT ( 'NONE',  ( 7.064632951172269415, -6.147671362329258926, 6.226446564517893911 ) ) ;
#12950=CARTESIAN_POINT ( 'NONE',  ( 4.749760686538667009, 2.741043480755029016, -7.530955069117485579 ) ) ;
#12953=CARTESIAN_POINT ( 'NONE',  ( -4.987550801365594033, 0.3701630799359330593, -3.521866450007987037 ) ) ;
#12955=VECTOR ( 'NONE', #8242, 1000.000000000000000 ) ;
#12956=CARTESIAN_POINT ( 'NONE',  ( 7.249760686538667009, 4.973063321323876629, 7.199384779417138169 ) ) ;
#12959=ORIENTED_EDGE ( 'NONE', *, *, #26555, .T. ) ;
#12963=ORIENTED_EDGE ( 'NONE', *, *, #2190, .T. ) ;
#12967=DIRECTION ( 'NONE',  ( 0.000000000000000000, 0.000000000000000000, -1.000000000000000000 ) ) ;
#12969=VERTEX_POINT ( 'NONE', #16141 ) ;
#12975=DIRECTION ( 'NONE',  ( -1.000000000000000000, -0.000000000000000000, -0.000000000000000000 ) ) ;
#12979=DIRECTION ( 'NONE',  ( -1.000000000000000000, 0.000000000000000000, 0.000000000000000000 ) ) ;
#12981=EDGE_CURVE ( 'NONE', #13763, #22300, #17327, .T. ) ;
#12982=VERTEX_POINT ( 'NONE', #800 ) ;
#12988=CARTESIAN_POINT ( 'NONE',  ( -6.900050802731187538, 1.549418761218566143, -2.853674364686379583 ) ) ;
#12990=EDGE_CURVE ( 'NONE', #12106, #13240, #22663, .T. ) ;
#12991=AXIS2_PLACEMENT_3D ( 'NONE', #21824, #26675, #32036 ) ;
#12993=ADVANCED_FACE ( 'NONE', ( #10978 ), #28196, .F. ) ;
#13000=CARTESIAN_POINT ( 'NONE',  ( -5.012550801365594388, -3.368539882008727115, -1.828967928396028064 ) ) ;
#13001=ORIENTED_EDGE ( 'NONE', *, *, #5401, .T. ) ;
#13002=CARTESIAN_POINT ( 'NONE',  ( -3.704531657079157103, 0.3127741368606810068, -2.975847129947406522 ) ) ;
#13003=CARTESIAN_POINT ( 'NONE',  ( 3.499999999999999556, 1.106368468154430129, 8.427689411260576691 ) ) ;
#13006=ORIENTED_EDGE ( 'NONE', *, *, #29854, .F. ) ;
#13018=LINE ( 'NONE', #18184, #31077 ) ;
#13019=EDGE_CURVE ( 'NONE', #4058, #24916, #31052, .T. ) ;
#13020=ORIENTED_EDGE ( 'NONE', *, *, #423, .T. ) ;
#13022=DIRECTION ( 'NONE',  ( -1.000000000000000000, -0.000000000000000000, -0.000000000000000000 ) ) ;
#13029=CARTESIAN_POINT ( 'NONE',  ( -7.662550801365593856, -0.3701630799359326152, 3.521866450007987037 ) ) ;
#13030=DIRECTION ( 'NONE',  ( 0.000000000000000000, 0.9961946980917458783, -0.08715574274765383600 ) ) ;
#13035=EDGE_CURVE ( 'NONE', #3548, #280, #8245, .T. ) ;
#13037=AXIS2_PLACEMENT_3D ( 'NONE', #17573, #27622, #29652 ) ;
#13043=CARTESIAN_POINT ( 'NONE',  ( 5.377543748152549874, 2.741043480755029016, -7.530955069117485579 ) ) ;
#13049=ADVANCED_FACE ( 'NONE', ( #5473 ), #3137, .F. ) ;
#13051=CARTESIAN_POINT ( 'NONE',  ( 7.249760686538667009, -7.199384779417155045, 4.973063321323851760 ) ) ;
#13060=ORIENTED_EDGE ( 'NONE', *, *, #30324, .F. ) ;
#13062=CARTESIAN_POINT ( 'NONE',  ( -6.112550801365593145, 1.088641768524161613, 3.675193018007246959 ) ) ;
#13076=CARTESIAN_POINT ( 'NONE',  ( 7.249760686538667009, 3.748318449932404484, -7.906491560603625679 ) ) ;
#13079=EDGE_CURVE ( 'NONE', #5270, #13793, #30168, .T. ) ;
#13085=CARTESIAN_POINT ( 'NONE',  ( 4.749760686538667009, -2.741043480754977946, 7.530955069117504230 ) ) ;
#13088=EDGE_CURVE ( 'NONE', #24063, #19677, #12508, .T. ) ;
#13101=DIRECTION ( 'NONE',  ( 0.000000000000000000, 0.7071067811865495711, -0.7071067811865455743 ) ) ;
#13102=CARTESIAN_POINT ( 'NONE',  ( 0.000000000000000000, -5.349675154362299345, -3.229702268444987645 ) ) ;
#13107=CYLINDRICAL_SURFACE ( 'NONE', #633, 6.248999999999999666 ) ;
#13108=EDGE_CURVE ( 'NONE', #7301, #14256, #29333, .T. ) ;
#13112=DIRECTION ( 'NONE',  ( 0.000000000000000000, 0.4226182617406976094, -0.9063077870366508249 ) ) ;
#13114=DIRECTION ( 'NONE',  ( 0.000000000000000000, -0.9063077870366448296, -0.4226182617407103770 ) ) ;
#13124=ORIENTED_EDGE ( 'NONE', *, *, #27981, .F. ) ;
#13125=CARTESIAN_POINT ( 'NONE',  ( 6.530491751506347420, -5.074604403564623389, -7.017944781892005324 ) ) ;
#13126=ORIENTED_EDGE ( 'NONE', *, *, #27321, .F. ) ;
#13139=DIRECTION ( 'NONE',  ( -1.000000000000000000, 0.000000000000000000, -0.000000000000000000 ) ) ;
#13149=CARTESIAN_POINT ( 'NONE',  ( 0.000000000000000000, 0.005878491403456947983, 7.047692205288324629 ) ) ;
#13153=CARTESIAN_POINT ( 'NONE',  ( -3.212550801365593678, 1.828967928396027176, -3.368539882008727115 ) ) ;
#13155=CARTESIAN_POINT ( 'NONE',  ( -3.204531657079157547, -2.325406398514293205, 1.883076972206379818 ) ) ;
#13170=CARTESIAN_POINT ( 'NONE',  ( 3.499999999999999556, 1.459547570502368385, 6.894905428400277536 ) ) ;
#13172=DIRECTION ( 'NONE',  ( 0.000000000000000000, 0.8660254037844361541, 0.5000000000000041078 ) ) ;
#13177=CARTESIAN_POINT ( 'NONE',  ( -6.612550801365593145, -3.368539882008727115, -1.828967928396028064 ) ) ;
#13188=DIRECTION ( 'NONE',  ( -0.000000000000000000, -0.5735764363510502672, 0.8191520442889888010 ) ) ;
#13197=VERTEX_POINT ( 'NONE', #26838 ) ;
#13201=EDGE_CURVE ( 'NONE', #24044, #508, #16310, .T. ) ;
#13204=CARTESIAN_POINT ( 'NONE',  ( -7.712550801365593678, 1.088641768524161613, 3.675193018007246959 ) ) ;
#13208=ORIENTED_EDGE ( 'NONE', *, *, #16494, .F. ) ;
#13225=CYLINDRICAL_SURFACE ( 'NONE', #16154, 3.000000000000000444 ) ;
#13230=ORIENTED_EDGE ( 'NONE', *, *, #28690, .F. ) ;
#13232=DIRECTION ( 'NONE',  ( 0.000000000000000000, 0.7431448254773954654, -0.6691306063588569053 ) ) ;
#13240=VERTEX_POINT ( 'NONE', #2594 ) ;
#13252=DIRECTION ( 'NONE',  ( -1.000000000000000000, -0.000000000000000000, -0.000000000000000000 ) ) ;
#13265=CARTESIAN_POINT ( 'NONE',  ( 7.249760686538667009, -8.014274990069656823, 8.669741416787380218E-17 ) ) ;
#13278=ORIENTED_EDGE ( 'NONE', *, *, #26605, .F. ) ;
#13286=CYLINDRICAL_SURFACE ( 'NONE', #17837, 2.999999999999999112 ) ;
#13291=CARTESIAN_POINT ( 'NONE',  ( -4.106376978575948300, -0.1572233378491262878, 2.999999999999999556 ) ) ;
#13294=CARTESIAN_POINT ( 'NONE',  ( 0.000000000000000000, 2.871924938129968741, -6.435996203144479288 ) ) ;
#13295=PLANE ( 'NONE',  #28425 ) ;
#13296=CARTESIAN_POINT ( 'NONE',  ( 0.000000000000000000, 7.008469740302802897, 0.7425307242148009301 ) ) ;
#13299=CARTESIAN_POINT ( 'NONE',  ( -7.550050802731187893, 2.983565686104819648, 0.3135853898029609677 ) ) ;
#13300=ORIENTED_EDGE ( 'NONE', *, *, #10921, .T. ) ;
#13302=CARTESIAN_POINT ( 'NONE',  ( -3.154531657079157281, -3.105402419394638791, 0.9198621039125867149 ) ) ;
#13303=CIRCLE ( 'NONE', #32010, 6.000000000000000000 ) ;
#13305=CARTESIAN_POINT ( 'NONE',  ( -5.306376978575950254, 0.1572233378491222633, -3.000000000000000000 ) ) ;
#13308=CARTESIAN_POINT ( 'NONE',  ( 3.499999999999999556, 7.008469740302810891, -0.7425307242147067832 ) ) ;
#13314=LINE ( 'NONE', #18522, #23522 ) ;
#13318=DIRECTION ( 'NONE',  ( -1.000000000000000000, 0.000000000000000000, -0.000000000000000000 ) ) ;
#13322=EDGE_LOOP ( 'NONE', ( #19120, #26347 ) ) ;
#13323=CARTESIAN_POINT ( 'NONE',  ( -4.062550801365593323, 0.3701630799359330593, -3.521866450007987037 ) ) ;
#13326=DIRECTION ( 'NONE',  ( -0.000000000000000000, -0.9063077870366526012, 0.4226182617406936126 ) ) ;
#13328=ORIENTED_EDGE ( 'NONE', *, *, #22489, .F. ) ;
#13329=AXIS2_PLACEMENT_3D ( 'NONE', #29964, #22428, #32981 ) ;
#13330=DIRECTION ( 'NONE',  ( -0.000000000000000000, 0.7071067811865466846, -0.7071067811865483499 ) ) ;
#13332=EDGE_CURVE ( 'NONE', #26019, #5620, #20974, .T. ) ;
#13333=LINE ( 'NONE', #18393, #10287 ) ;
#13336=DIRECTION ( 'NONE',  ( 0.000000000000000000, 0.000000000000000000, 1.000000000000000000 ) ) ;
#13338=VECTOR ( 'NONE', #1659, 1000.000000000000000 ) ;
#13342=FACE_OUTER_BOUND ( 'NONE', #14021, .T. ) ;
#13345=ORIENTED_EDGE ( 'NONE', *, *, #12169, .T. ) ;
#13347=DIRECTION ( 'NONE',  ( 0.000000000000000000, 0.000000000000000000, -1.000000000000000000 ) ) ;
#13349=AXIS2_PLACEMENT_3D ( 'NONE', #26184, #21322, #2991 ) ;
#13351=ORIENTED_EDGE ( 'NONE', *, *, #18557, .F. ) ;
#13356=DIRECTION ( 'NONE',  ( 0.000000000000000000, -0.9961946980917445460, -0.08715574274766962892 ) ) ;
#13357=CARTESIAN_POINT ( 'NONE',  ( -3.412550801365592967, -3.368539882008727115, -1.828967928396027842 ) ) ;
#13359=CARTESIAN_POINT ( 'NONE',  ( 0.000000000000000000, 7.003298780661427969, 4.817032923780590892 ) ) ;
#13388=AXIS2_PLACEMENT_3D ( 'NONE', #11878, #14708, #4356 ) ;
#13401=CARTESIAN_POINT ( 'NONE',  ( 6.356382399260309235, -3.797266095948536258, 7.723816458760333958 ) ) ;
#13402=VERTEX_POINT ( 'NONE', #8419 ) ;
#13407=CARTESIAN_POINT ( 'NONE',  ( 0.000000000000000000, 0.000000000000000000, 0.000000000000000000 ) ) ;
#13416=VECTOR ( 'NONE', #14819, 1000.000000000000000 ) ;
#13419=CARTESIAN_POINT ( 'NONE',  ( 6.524595623740805372, 5.074779492939383019, -7.015943501182343667 ) ) ;
#13427=VECTOR ( 'NONE', #11642, 1000.000000000000114 ) ;
#13430=VERTEX_POINT ( 'NONE', #24111 ) ;
#13437=B_SPLINE_SURFACE_WITH_KNOTS ( 'NONE', 1, 3, ( 
 ( #9424, #10204, #2388, #15231 ),
 ( #20, #10539, #18228, #22914 ) ),
 .UNSPECIFIED., .F., .F., .F.,
 ( 2, 2 ),
 ( 4, 4 ),
 ( 0.000000000000000000, 1.000000000000000000 ),
 ( 0.0001138015799683909565, 0.0008863868760781655996 ),
 .UNSPECIFIED. ) ;
#13440=ORIENTED_EDGE ( 'NONE', *, *, #29044, .F. ) ;
#13441=ORIENTED_EDGE ( 'NONE', *, *, #29807, .F. ) ;
#13445=AXIS2_PLACEMENT_3D ( 'NONE', #14438, #29336, #29848 ) ;
#13447=DIRECTION ( 'NONE',  ( -1.000000000000000000, -0.000000000000000000, 0.000000000000000000 ) ) ;
#13453=B_SPLINE_CURVE_WITH_KNOTS ( 'NONE', 3,
 ( #23280, #382, #10556, #30968, #20930, #15074 ),
 .UNSPECIFIED., .F., .F.,
 ( 4, 2, 4 ),
 ( 0.4834212463832757156, 0.4917106231916378856, 0.5000000000000000000 ),
 .UNSPECIFIED. ) ;
#13454=AXIS2_PLACEMENT_3D ( 'NONE', #20055, #22366, #32582 ) ;
#13457=CYLINDRICAL_SURFACE ( 'NONE', #13904, 8.500000000000000000 ) ;
#13460=LINE ( 'NONE', #31228, #24666 ) ;
#13462=CARTESIAN_POINT ( 'NONE',  ( -6.650050802731187538, 1.887961173149511618, 2.331437884370912705 ) ) ;
#13473=CARTESIAN_POINT ( 'NONE',  ( -2.362550801365593589, 2.752080473201636845, -2.228590825266444142 ) ) ;
#13477=CARTESIAN_POINT ( 'NONE',  ( -6.050050800000001061, 1.549418761218566143, -2.853674364686379583 ) ) ;
#13478=SHAPE_REPRESENTATION ( 'Part4_Gear', ( #2865 ), #32200 ) ;
#13479=CLOSED_SHELL ( 'NONE', ( #19164, #24832, #16483, #3568, #1131, #11848, #3909, #17850, #31379, #18029, #6535, #30831, #6281, #8244, #28349, #4579, #27194, #1794, #27588, #27747, #7755, #700, #5113, #23433, #20133, #28197, #6823, #18956, #15748, #21820, #820, #28638, #3117, #23275, #31627, #10031, #8446, #28951, #28475, #22032, #21858, #16087, #30352, #32902, #16764, #29113, #7795, #22684, #7711, #8376, #15497, #31119, #27380, #9740, #14782, #5748, #26333, #4224, #27772, #2509, #32649, #23301, #32475, #10136, #8637, #3923, #15900, #14177, #32860, #14606, #16756, #14958, #19141, #11802, #22975, #11655, #5611, #17391, #17291, #29712, #5715, #7911, #17216, #27280, #17685, #8451, #21898, #28625, #18865, #10372, #3671, #4789, #23728, #31845, #11789, #5151, #15631, #11584, #16365, #24369, #23845, #25819, #29773, #8721, #81, #18746, #10603, #8337, #13049, #31021, #13576, #24023, #8571, #23157, #31762, #28021, #3740, #7350, #15389, #26162, #19988, #2871, #21850, #27485, #24104, #5645, #3590, #21788, #27831, #11824, #19004, #23052, #25058, #1950, #4307, #28122, #20701, #31896, #26325, #22412, #23064, #14233, #14998, #7861, #32046, #12993, #6643, #26726, #27599, #3296, #16261, #31498, #8172, #3861, #9898, #9526, #22406, #18419, #21840, #12675, #31433, #14105, #26871, #9813, #25163, #362, #18503, #27329, #1701 ) ) ;
#13481=CARTESIAN_POINT ( 'NONE',  ( -5.100050799999999995, 2.983565686104819648, 0.3135853898029609677 ) ) ;
#13485=DIRECTION ( 'NONE',  ( -1.000000000000000000, 0.000000000000000000, 0.000000000000000000 ) ) ;
#13488=ORIENTED_EDGE ( 'NONE', *, *, #13201, .F. ) ;
#13489=DIRECTION ( 'NONE',  ( 0.000000000000000000, -0.9961946980917465444, 0.08715574274764703588 ) ) ;
#13494=CARTESIAN_POINT ( 'NONE',  ( 5.377543748152551650, 6.139290821770257089, 5.151476664237498504 ) ) ;
#13497=VECTOR ( 'NONE', #18126, 1000.000000000000114 ) ;
#13499=DIRECTION ( 'NONE',  ( 0.000000000000000000, -0.2588190451025066396, -0.9659258262890719759 ) ) ;
#13500=VECTOR ( 'NONE', #13188, 1000.000000000000114 ) ;
#13502=CIRCLE ( 'NONE', #17790, 2.999999999999999112 ) ;
#13504=ORIENTED_EDGE ( 'NONE', *, *, #9068, .F. ) ;
#13505=CARTESIAN_POINT ( 'NONE',  ( -3.962550801365593234, 2.752080473201636845, -2.228590825266444142 ) ) ;
#13520=CARTESIAN_POINT ( 'NONE',  ( -3.637550801365593944, -3.675193018007245627, 1.088641768524163389 ) ) ;
#13527=EDGE_CURVE ( 'NONE', #6094, #30847, #29093, .T. ) ;
#13538=CARTESIAN_POINT ( 'NONE',  ( -4.712550801365592790, 3.675193018007246959, -1.088641768524161391 ) ) ;
#13543=ORIENTED_EDGE ( 'NONE', *, *, #11006, .F. ) ;
#13545=CARTESIAN_POINT ( 'NONE',  ( -5.537550801365594744, 3.368539882008727115, 1.828967928396026954 ) ) ;
#13550=AXIS2_PLACEMENT_3D ( 'NONE', #23472, #11263, #31683 ) ;
#13553=B_SPLINE_CURVE_WITH_KNOTS ( 'NONE', 3,
 ( #30691, #10581, #25319, #20787, #30990, #12598, #22802, #7584, #7766, #17957 ),
 .UNSPECIFIED., .F., .F.,
 ( 4, 2, 2, 2, 4 ),
 ( 2.571685856645629606E-07, 0.0005478592107668799017, 0.001095461252948095243, 0.001643063295129310476, 0.002190665337310525925 ),
 .UNSPECIFIED. ) ;
#13562=CARTESIAN_POINT ( 'NONE',  ( -4.687550801365594211, 2.228590825266444142, 2.752080473201636845 ) ) ;
#13563=ORIENTED_EDGE ( 'NONE', *, *, #21502, .F. ) ;
#13564=FACE_OUTER_BOUND ( 'NONE', #26227, .T. ) ;
#13567=LINE ( 'NONE', #26120, #25718 ) ;
#13574=ORIENTED_EDGE ( 'NONE', *, *, #22535, .T. ) ;
#13576=ADVANCED_FACE ( 'NONE', ( #21774 ), #31983, .F. ) ;
#13586=DIRECTION ( 'NONE',  ( 0.000000000000000000, 0.9063077870366492705, 0.4226182617407007180 ) ) ;
#13589=CARTESIAN_POINT ( 'NONE',  ( 0.000000000000000000, -2.652816298622461932, 5.657964889053573643 ) ) ;
#13590=CIRCLE ( 'NONE', #10410, 6.248999999999999666 ) ;
#13597=CARTESIAN_POINT ( 'NONE',  ( 6.037141848526921706, -3.315649934461669002, -7.798898458906313280 ) ) ;
#13599=PLANE ( 'NONE',  #711 ) ;
#13600=EDGE_LOOP ( 'NONE', ( #8586, #23442, #29004, #21969, #3492, #17146 ) ) ;
#13621=ORIENTED_EDGE ( 'NONE', *, *, #26518, .T. ) ;
#13624=EDGE_CURVE ( 'NONE', #24971, #14880, #5074, .T. ) ;
#13637=EDGE_CURVE ( 'NONE', #10538, #10650, #21252, .T. ) ;
#13639=CARTESIAN_POINT ( 'NONE',  ( -2.412550801365592967, 1.828967928396027176, -3.368539882008727115 ) ) ;
#13641=CARTESIAN_POINT ( 'NONE',  ( -6.350050800000000883, -3.113457007523259268, 0.9222479816126455399 ) ) ;
#13642=EDGE_CURVE ( 'NONE', #15020, #19834, #13590, .T. ) ;
#13648=VERTEX_POINT ( 'NONE', #1520 ) ;
#13663=ORIENTED_EDGE ( 'NONE', *, *, #22773, .F. ) ;
#13664=CARTESIAN_POINT ( 'NONE',  ( -2.212550801365593234, 3.368539882008727115, 1.828967928396026954 ) ) ;
#13673=CARTESIAN_POINT ( 'NONE',  ( 5.377543748152549874, -5.151476664237518044, 6.139290821770238438 ) ) ;
#13678=CARTESIAN_POINT ( 'NONE',  ( -4.787550801365593856, 3.521866450007987037, 0.3701630799359328372 ) ) ;
#13682=DIRECTION ( 'NONE',  ( 0.000000000000000000, 0.000000000000000000, 1.000000000000000000 ) ) ;
#13683=EDGE_CURVE ( 'NONE', #10415, #14000, #25884, .T. ) ;
#13695=CARTESIAN_POINT ( 'NONE',  ( -3.212550801365593678, 1.828967928396027398, -3.368539882008727115 ) ) ;
#13696=LINE ( 'NONE', #15883, #25786 ) ;
#13700=ORIENTED_EDGE ( 'NONE', *, *, #15105, .F. ) ;
#13701=CARTESIAN_POINT ( 'NONE',  ( -8.087550801365594566, 2.752080473201636845, -2.228590825266444142 ) ) ;
#13707=EDGE_LOOP ( 'NONE', ( #31704, #15601, #12159 ) ) ;
#13712=FACE_OUTER_BOUND ( 'NONE', #2849, .T. ) ;
#13716=CARTESIAN_POINT ( 'NONE',  ( 3.499999999999999556, -6.700937042937042065, -2.183447440113257976 ) ) ;
#13717=CARTESIAN_POINT ( 'NONE',  ( -6.637550801365594388, -1.088641768524163389, -3.675193018007246071 ) ) ;
#13720=CARTESIAN_POINT ( 'NONE',  ( 3.499999999999999556, 0.000000000000000000, 0.000000000000000000 ) ) ;
#13721=EDGE_CURVE ( 'NONE', #23931, #24941, #2970, .T. ) ;
#13735=ORIENTED_EDGE ( 'NONE', *, *, #25283, .F. ) ;
#13741=DIRECTION ( 'NONE',  ( 0.000000000000000000, 0.000000000000000000, 1.000000000000000000 ) ) ;
#13752=EDGE_CURVE ( 'NONE', #24941, #32892, #26431, .T. ) ;
#13763=VERTEX_POINT ( 'NONE', #24558 ) ;
#13764=ORIENTED_EDGE ( 'NONE', *, *, #3502, .F. ) ;
#13769=CARTESIAN_POINT ( 'NONE',  ( 7.249760686538667009, -0.8180878109962448352, 8.711672189281424394 ) ) ;
#13770=FACE_OUTER_BOUND ( 'NONE', #3878, .T. ) ;
#13771=ORIENTED_EDGE ( 'NONE', *, *, #10494, .F. ) ;
#13775=FACE_OUTER_BOUND ( 'NONE', #2016, .T. ) ;
#13784=DIRECTION ( 'NONE',  ( -1.000000000000000000, 0.000000000000000000, -0.000000000000000000 ) ) ;
#13785=CARTESIAN_POINT ( 'NONE',  ( -2.262550801365593056, 3.521866450007987037, 0.3701630799359328372 ) ) ;
#13787=CARTESIAN_POINT ( 'NONE',  ( -6.200050800000000528, -1.887961173149512062, -2.331437884370912261 ) ) ;
#13793=VERTEX_POINT ( 'NONE', #3499 ) ;
#13797=CARTESIAN_POINT ( 'NONE',  ( -6.112942406915326643, -3.366872799099910998E-15, -3.000000000000000000 ) ) ;
#13801=ORIENTED_EDGE ( 'NONE', *, *, #5956, .T. ) ;
#13803=CARTESIAN_POINT ( 'NONE',  ( 6.524595126109737464, -8.397268106035227220, 2.112519041817586984 ) ) ;
#13806=FACE_OUTER_BOUND ( 'NONE', #20595, .T. ) ;
#13808=CARTESIAN_POINT ( 'NONE',  ( -2.812550801365592879, -1.828967928396026510, 3.368539882008728004 ) ) ;
#13812=FACE_OUTER_BOUND ( 'NONE', #24075, .T. ) ;
#13813=CARTESIAN_POINT ( 'NONE',  ( 3.499999999999999556, 4.137773741518377513, 5.705158055754806945 ) ) ;
#13819=ORIENTED_EDGE ( 'NONE', *, *, #10494, .T. ) ;
#13820=CARTESIAN_POINT ( 'NONE',  ( 6.037141848526922594, 2.473100090966272813, -8.105561522824284992 ) ) ;
#13824=CARTESIAN_POINT ( 'NONE',  ( -4.587550801365592790, -0.3701630799359326152, 3.521866450007987037 ) ) ;
#13827=ORIENTED_EDGE ( 'NONE', *, *, #26053, .T. ) ;
#13829=EDGE_CURVE ( 'NONE', #8819, #19834, #21835, .T. ) ;
#13842=CARTESIAN_POINT ( 'NONE',  ( -4.912550801365593856, -1.088641768524163611, -3.675193018007245627 ) ) ;
#13848=VERTEX_POINT ( 'NONE', #32552 ) ;
#13849=CARTESIAN_POINT ( 'NONE',  ( -5.887550801365593500, -2.228590825266444586, -2.752080473201636401 ) ) ;
#13859=CARTESIAN_POINT ( 'NONE',  ( 5.377543748152548986, -1.391664247347174754, -7.892520144992448472 ) ) ;
#13861=DIRECTION ( 'NONE',  ( -1.000000000000000000, 0.000000000000000000, 0.000000000000000000 ) ) ;
#13871=CARTESIAN_POINT ( 'NONE',  ( 0.000000000000000000, 1.418488851014406693, 6.085876303339381899 ) ) ;
#13877=FACE_OUTER_BOUND ( 'NONE', #6374, .T. ) ;
#13878=VERTEX_POINT ( 'NONE', #7143 ) ;
#13888=DIRECTION ( 'NONE',  ( 0.000000000000000000, -0.9659258262890662028, -0.2588190451025286221 ) ) ;
#13895=CARTESIAN_POINT ( 'NONE',  ( -4.800050802731187005, -3.113457007523259268, 0.9222479816126455399 ) ) ;
#13900=CARTESIAN_POINT ( 'NONE',  ( 7.249760686538667009, 8.437262856154164936, 2.318425219014256911 ) ) ;
#13901=DIRECTION ( 'NONE',  ( 1.000000000000000000, -0.000000000000000000, -0.000000000000000000 ) ) ;
#13904=AXIS2_PLACEMENT_3D ( 'NONE', #793, #10972, #7193 ) ;
#13907=CARTESIAN_POINT ( 'NONE',  ( -8.000050800000002127, 3.541248556864417196, 0.01107501445590582979 ) ) ;
#13908=ORIENTED_EDGE ( 'NONE', *, *, #6293, .F. ) ;
#13909=CIRCLE ( 'NONE', #26747, 2.999999999999999556 ) ;
#13915=EDGE_LOOP ( 'NONE', ( #22447, #20848, #1168, #18005, #14603, #16023, #407, #3862, #3271, #28649, #25508, #23343, #2792, #17921, #24037, #15309, #23463, #19089, #3804, #22951, #7383, #10015, #13208, #599, #29745, #28517, #9344, #10762, #16875, #17600, #13543, #28289, #12743, #11148, #20710, #18592, #14770, #5820, #7145, #31367, #8400, #4097, #29320, #25904, #31851, #1694, #22301, #26169, #1116, #32580, #17383, #25975, #11305, #24227, #23274, #14505, #32125, #30583, #26296, #17950, #13006, #17956, #26669, #32646, #21063, #31696, #28292, #20561, #13700, #26464, #27852, #14943, #30029, #12723, #31144, #2747, #20641, #23850, #4239, #5883, #22869, #18818, #28966, #6913, #18518, #19112, #32855, #11073, #5910, #5600, #29976, #16642, #31938, #27047, #20289, #14267, #25258, #13663, #24577, #22676, #5547, #20273, #23535, #7942, #32940, #25728, #24353, #16822 ) ) ;
#13916=AXIS2_PLACEMENT_3D ( 'NONE', #22838, #7802, #5129 ) ;
#13935=AXIS2_PLACEMENT_3D ( 'NONE', #754, #5752, #15930 ) ;
#13941=DIRECTION ( 'NONE',  ( 0.000000000000000000, 0.000000000000000000, -1.000000000000000000 ) ) ;
#13948=CARTESIAN_POINT ( 'NONE',  ( 7.249760686538667009, 7.135485519862069914, -5.064320921489747995 ) ) ;
#13950=CARTESIAN_POINT ( 'NONE',  ( -4.850050802731186828, -2.331437884370912705, 1.887961173149512062 ) ) ;
#13952=CARTESIAN_POINT ( 'NONE',  ( -5.050050800000001061, 2.853674364686379583, 1.549418761218565921 ) ) ;
#13953=CIRCLE ( 'NONE', #21972, 2.999999999999999112 ) ;
#13958=CARTESIAN_POINT ( 'NONE',  ( -7.000050800000001239, -1.887961173149512062, -2.331437884370912261 ) ) ;
#13959=VECTOR ( 'NONE', #21852, 1000.000000000000000 ) ;
#13964=ORIENTED_EDGE ( 'NONE', *, *, #29281, .F. ) ;
#13966=VECTOR ( 'NONE', #12700, 1000.000000000000114 ) ;
#13968=CYLINDRICAL_SURFACE ( 'NONE', #1100, 2.999999999999999112 ) ;
#13980=PLANE ( 'NONE',  #30467 ) ;
#13982=AXIS2_PLACEMENT_3D ( 'NONE', #1764, #25590, #25273 ) ;
#13983=CARTESIAN_POINT ( 'NONE',  ( -4.462550801365592790, -0.3701630799359326152, 3.521866450007987037 ) ) ;
#13985=AXIS2_PLACEMENT_3D ( 'NONE', #30171, #26977, #1559 ) ;
#13987=DIRECTION ( 'NONE',  ( 0.000000000000000000, 0.000000000000000000, 1.000000000000000000 ) ) ;
#13997=ORIENTED_EDGE ( 'NONE', *, *, #5186, .F. ) ;
#13998=CIRCLE ( 'NONE', #7074, 2.999999999999999112 ) ;
#14000=VERTEX_POINT ( 'NONE', #33044 ) ;
#14003=CARTESIAN_POINT ( 'NONE',  ( -1.981386825810575125, 0.8521285013611177295, 3.209918541081830945 ) ) ;
#14004=CARTESIAN_POINT ( 'NONE',  ( -4.137550801365593500, 1.828967928396027398, -3.368539882008727115 ) ) ;
#14005=PLANE ( 'NONE',  #10315 ) ;
#14011=VERTEX_POINT ( 'NONE', #7445 ) ;
#14020=CARTESIAN_POINT ( 'NONE',  ( -10.00000000000000000, 0.000000000000000000, 0.000000000000000000 ) ) ;
#14021=EDGE_LOOP ( 'NONE', ( #33089, #17599, #31036, #12183 ) ) ;
#14026=CARTESIAN_POINT ( 'NONE',  ( -5.412550801365593856, 3.368539882008727115, 1.828967928396027176 ) ) ;
#14031=CARTESIAN_POINT ( 'NONE',  ( -5.737550801365594033, 1.828967928396027176, -3.368539882008727115 ) ) ;
#14033=EDGE_CURVE ( 'NONE', #24488, #16352, #7920, .T. ) ;
#14038=ORIENTED_EDGE ( 'NONE', *, *, #1584, .T. ) ;
#14043=VECTOR ( 'NONE', #27207, 1000.000000000000000 ) ;
#14052=LINE ( 'NONE', #18930, #12955 ) ;
#14053=CARTESIAN_POINT ( 'NONE',  ( -3.037550801365593411, 1.088641768524161613, 3.675193018007247403 ) ) ;
#14060=LINE ( 'NONE', #18936, #28907 ) ;
#14064=VECTOR ( 'NONE', #20650, 1000.000000000000000 ) ;
#14065=CARTESIAN_POINT ( 'NONE',  ( 3.499999999999999556, -1.179494851233859887, -6.136676046192499179 ) ) ;
#14069=ORIENTED_EDGE ( 'NONE', *, *, #20596, .T. ) ;
#14074=AXIS2_PLACEMENT_3D ( 'NONE', #20130, #22451, #17590 ) ;
#14080=FACE_OUTER_BOUND ( 'NONE', #22507, .T. ) ;
#14086=EDGE_LOOP ( 'NONE', ( #5656, #23539, #18329 ) ) ;
#14091=CARTESIAN_POINT ( 'NONE',  ( 5.377543748152548098, 7.530955069117513112, 2.741043480754951744 ) ) ;
#14096=DIRECTION ( 'NONE',  ( 0.000000000000000000, 0.000000000000000000, 1.000000000000000000 ) ) ;
#14099=ORIENTED_EDGE ( 'NONE', *, *, #8993, .F. ) ;
#14105=ADVANCED_FACE ( 'NONE', ( #2389 ), #4872, .F. ) ;
#14109=FACE_OUTER_BOUND ( 'NONE', #28666, .T. ) ;
#14119=VERTEX_POINT ( 'NONE', #2897 ) ;
#14120=CARTESIAN_POINT ( 'NONE',  ( 1.750000000000000000, 0.6700234925293840904, -8.473551116235670477 ) ) ;
#14121=CARTESIAN_POINT ( 'NONE',  ( 5.377543748152547209, 1.391664247347333294, -7.892520144992419162 ) ) ;
#14125=EDGE_CURVE ( 'NONE', #19712, #16397, #8731, .T. ) ;
#14127=FACE_OUTER_BOUND ( 'NONE', #21085, .T. ) ;
#14128=CARTESIAN_POINT ( 'NONE',  ( 6.749760686538667009, 0.000000000000000000, 0.000000000000000000 ) ) ;
#14129=EDGE_CURVE ( 'NONE', #4959, #31510, #9874, .T. ) ;
#14135=CARTESIAN_POINT ( 'NONE',  ( -5.450050802731187360, -1.887961173149512062, -2.331437884370912261 ) ) ;
#14137=CARTESIAN_POINT ( 'NONE',  ( -6.950050800000000528, -0.9222479816126459840, -3.113457007523259268 ) ) ;
#14139=DIRECTION ( 'NONE',  ( 0.000000000000000000, 0.1045284632676536235, -0.9945218953682734009 ) ) ;
#14141=ORIENTED_EDGE ( 'NONE', *, *, #2772, .T. ) ;
#14148=CARTESIAN_POINT ( 'NONE',  ( 0.000000000000000000, 4.561279057474412646, 4.271385531633187682 ) ) ;
#14151=CARTESIAN_POINT ( 'NONE',  ( -6.106376978575948300, 0.1572233378491222633, -3.000000000000000000 ) ) ;
#14157=LINE ( 'NONE', #27369, #16622 ) ;
#14160=ORIENTED_EDGE ( 'NONE', *, *, #31653, .T. ) ;
#14165=CARTESIAN_POINT ( 'NONE',  ( 5.377543748152550762, -1.391664247347281780, 7.892520144992429820 ) ) ;
#14174=CARTESIAN_POINT ( 'NONE',  ( 7.249760686538667009, 0.000000000000000000, 0.000000000000000000 ) ) ;
#14177=ADVANCED_FACE ( 'NONE', ( #22228 ), #32595, .T. ) ;
#14179=EDGE_CURVE ( 'NONE', #11951, #29082, #26917, .T. ) ;
#14188=DIRECTION ( 'NONE',  ( -1.000000000000000000, 0.000000000000000000, 0.000000000000000000 ) ) ;
#14195=CARTESIAN_POINT ( 'NONE',  ( -6.987550801365594033, -0.3701630799359326152, 3.521866450007987037 ) ) ;
#14201=EDGE_LOOP ( 'NONE', ( #4488, #19293, #28530, #16978 ) ) ;
#14202=CARTESIAN_POINT ( 'NONE',  ( -6.900050800000000706, 0.3135853898029611342, -2.983565686104819648 ) ) ;
#14216=CARTESIAN_POINT ( 'NONE',  ( 7.249760686538667009, 0.000000000000000000, 0.000000000000000000 ) ) ;
#14217=CARTESIAN_POINT ( 'NONE',  ( 7.064423600674403225, -2.210816291637359932, -8.466096581344345395 ) ) ;
#14220=LINE ( 'NONE', #16557, #14445 ) ;
#14221=VERTEX_POINT ( 'NONE', #4671 ) ;
#14226=ORIENTED_EDGE ( 'NONE', *, *, #31005, .T. ) ;
#14233=ADVANCED_FACE ( 'NONE', ( #4022 ), #1504, .F. ) ;
#14234=DIRECTION ( 'NONE',  ( 0.000000000000000000, 0.4226182617407007736, -0.9063077870366493816 ) ) ;
#14238=DIRECTION ( 'NONE',  ( 1.000000000000000000, 0.000000000000000000, 0.000000000000000000 ) ) ;
#14243=FACE_OUTER_BOUND ( 'NONE', #7216, .T. ) ;
#14248=EDGE_CURVE ( 'NONE', #31994, #24044, #12852, .T. ) ;
#14256=VERTEX_POINT ( 'NONE', #25399 ) ;
#14258=CARTESIAN_POINT ( 'NONE',  ( 7.064632879756603145, -8.711672189281433276, 0.8180878109961572386 ) ) ;
#14264=CARTESIAN_POINT ( 'NONE',  ( 7.249760686538667009, 0.000000000000000000, 0.000000000000000000 ) ) ;
#14265=CARTESIAN_POINT ( 'NONE',  ( 6.883866557622100757, -7.943335131954982309, -3.625395379390166983 ) ) ;
#14267=ORIENTED_EDGE ( 'NONE', *, *, #26751, .F. ) ;
#14270=CARTESIAN_POINT ( 'NONE',  ( 6.357667697713667465, 0.9262207444595902395, 8.557242355892487495 ) ) ;
#14271=CARTESIAN_POINT ( 'NONE',  ( 4.749760686538667009, 7.892520144992435149, 1.391664247347255134 ) ) ;
#14277=CARTESIAN_POINT ( 'NONE',  ( -2.249956573341760357, 1.323625320507108460, 3.284597389080124774 ) ) ;
#14278=DIRECTION ( 'NONE',  ( -1.000000000000000000, 0.000000000000000000, 0.000000000000000000 ) ) ;
#14279=CARTESIAN_POINT ( 'NONE',  ( 3.499999999999999556, -2.652816298622381996, -5.657964889053610058 ) ) ;
#14283=CARTESIAN_POINT ( 'NONE',  ( -5.400050802731186650, -0.9222479816126459840, -3.113457007523259268 ) ) ;
#14285=CARTESIAN_POINT ( 'NONE',  ( -3.350050800000000439, 0.9222479816126443186, 3.113457007523260156 ) ) ;
#14287=CARTESIAN_POINT ( 'NONE',  ( -5.500050802731188071, -2.853674364686378695, -1.549418761218566809 ) ) ;
#14289=ORIENTED_EDGE ( 'NONE', *, *, #30070, .T. ) ;
#14293=CARTESIAN_POINT ( 'NONE',  ( 5.377543748152549874, 5.151476664237477188, 6.139290821770273077 ) ) ;
#14301=CARTESIAN_POINT ( 'NONE',  ( 7.249760686538667009, 1.391664247347333294, -7.892520144992419162 ) ) ;
#14302=VERTEX_POINT ( 'NONE', #9854 ) ;
#14305=CARTESIAN_POINT ( 'NONE',  ( 7.249760686538667009, -7.953573330858239920, 3.647351267791542284 ) ) ;
#14322=DIRECTION ( 'NONE',  ( 0.000000000000000000, -0.08715574274764384399, -0.9961946980917467664 ) ) ;
#14324=DIRECTION ( 'NONE',  ( -1.000000000000000000, -0.000000000000000000, 0.000000000000000000 ) ) ;
#14331=CARTESIAN_POINT ( 'NONE',  ( -8.000050800000000351, 0.000000000000000000, -3.000000000000000444 ) ) ;
#14332=CARTESIAN_POINT ( 'NONE',  ( 7.064423669210280643, 6.226446564518129279, -6.147671362330616063 ) ) ;
#14336=CARTESIAN_POINT ( 'NONE',  ( 6.880159396099835512, -7.882559112973138937, -3.754731129947869395 ) ) ;
#14339=DIRECTION ( 'NONE',  ( 0.000000000000000000, 0.2079116908177532919, 0.9781476007338070211 ) ) ;
#14341=CARTESIAN_POINT ( 'NONE',  ( -2.187550801365593767, -0.3701630799359326152, 3.521866450007987037 ) ) ;
#14358=CARTESIAN_POINT ( 'NONE',  ( -3.387550801365593056, 0.3701630799359330593, -3.521866450007987037 ) ) ;
#14364=CARTESIAN_POINT ( 'NONE',  ( 3.499999999999999556, -5.349675154362298457, -3.229702268444986757 ) ) ;
#14376=EDGE_CURVE ( 'NONE', #10953, #11269, #23550, .T. ) ;
#14389=CARTESIAN_POINT ( 'NONE',  ( 5.887530024394195038, -2.518482652462503690, -8.008238305624875153 ) ) ;
#14391=LINE ( 'NONE', #12086, #31600 ) ;
#14395=CARTESIAN_POINT ( 'NONE',  ( -6.350050800000000883, -3.113457007523259268, 0.9222479816126455399 ) ) ;
#14398=VERTEX_POINT ( 'NONE', #4827 ) ;
#14399=CARTESIAN_POINT ( 'NONE',  ( -2.162942409646512854, 4.884725290497410777E-15, -2.999999999999999556 ) ) ;
#14402=VERTEX_POINT ( 'NONE', #334 ) ;
#14405=CIRCLE ( 'NONE', #35, 8.750000000000000000 ) ;
#14413=ORIENTED_EDGE ( 'NONE', *, *, #28588, .T. ) ;
#14417=CARTESIAN_POINT ( 'NONE',  ( -8.000050800000000351, 0.000000000000000000, 0.000000000000000000 ) ) ;
#14424=CARTESIAN_POINT ( 'NONE',  ( 7.249760686538667009, -7.953573330858239920, 3.647351267791542284 ) ) ;
#14428=DIRECTION ( 'NONE',  ( 0.000000000000000000, -0.7071067811865495711, 0.7071067811865455743 ) ) ;
#14431=DIRECTION ( 'NONE',  ( -1.000000000000000000, -0.000000000000000000, -0.000000000000000000 ) ) ;
#14437=DIRECTION ( 'NONE',  ( 0.000000000000000000, 0.000000000000000000, 1.000000000000000000 ) ) ;
#14438=CARTESIAN_POINT ( 'NONE',  ( 4.749760686538667009, 4.007137495034909236, -6.940565734314555257 ) ) ;
#14440=FACE_OUTER_BOUND ( 'NONE', #13707, .T. ) ;
#14441=CARTESIAN_POINT ( 'NONE',  ( -5.150050802731186650, 2.983565686104819648, 0.3135853898029609677 ) ) ;
#14444=CARTESIAN_POINT ( 'NONE',  ( -3.700050800000000084, 0.3135853898029611342, -2.983565686104819648 ) ) ;
#14445=VECTOR ( 'NONE', #24418, 1000.000000000000114 ) ;
#14450=CARTESIAN_POINT ( 'NONE',  ( -7.312942406915325044, -8.831141768130910875E-16, 2.999999999999999556 ) ) ;
#14455=AXIS2_PLACEMENT_3D ( 'NONE', #12451, #19653, #4262 ) ;
#14456=CARTESIAN_POINT ( 'NONE',  ( -2.850050799999999995, 1.549418761218566143, -2.853674364686379583 ) ) ;
#14461=CARTESIAN_POINT ( 'NONE',  ( -5.900050800000000706, 2.983565686104819648, 0.3135853898029609677 ) ) ;
#14464=CARTESIAN_POINT ( 'NONE',  ( 5.887529755120530339, -1.823049025159242831, 8.194579018285287120 ) ) ;
#14466=( BOUNDED_CURVE ( )  B_SPLINE_CURVE ( 2, ( #18955, #6232, #3910, #29471, #1052, #13895, #28984, #4071, #6381, #1552, #29145 ),
 .UNSPECIFIED., .F., .F. ) 
 B_SPLINE_CURVE_WITH_KNOTS ( ( 3, 2, 2, 2, 2, 3 ),
 ( 0.4353822619934377136, 0.4375000000000000000, 0.4531250000000000000, 0.4687500000000000000, 0.4843750000000000000, 0.4978822619934377136 ),
 .UNSPECIFIED. ) 
 CURVE ( )  GEOMETRIC_REPRESENTATION_ITEM ( )  RATIONAL_B_SPLINE_CURVE ( ( 0.9821626249036857770, 0.9896829947469991673, 1.000000000000000000, 0.9238795325112867385, 1.000000000000000000, 0.9238795325112867385, 1.000000000000000000, 0.9238795325112867385, 1.000000000000000000, 0.9341965377642874602, 0.9821626249036857770 ) ) 
 REPRESENTATION_ITEM ( '' )  );
#14467=ORIENTED_EDGE ( 'NONE', *, *, #15411, .T. ) ;
#14468=EDGE_CURVE ( 'NONE', #14256, #12536, #18526, .T. ) ;
#14472=DIRECTION ( 'NONE',  ( -0.000000000000000000, -0.8191520442889951292, 0.5735764363510413855 ) ) ;
#14478=CARTESIAN_POINT ( 'NONE',  ( 6.357667408475528248, -8.588075071450651521, -0.5738000813809884804 ) ) ;
#14480=CYLINDRICAL_SURFACE ( 'NONE', #28352, 8.500000000000000000 ) ;
#14494=CARTESIAN_POINT ( 'NONE',  ( -6.454531657079158435, -1.545410377633946286, 2.846291840500174697 ) ) ;
#14498=DIRECTION ( 'NONE',  ( 1.000000000000000000, 0.000000000000000000, -0.000000000000000000 ) ) ;
#14501=AXIS2_PLACEMENT_3D ( 'NONE', #22734, #23047, #10354 ) ;
#14505=ORIENTED_EDGE ( 'NONE', *, *, #3941, .F. ) ;
#14508=CARTESIAN_POINT ( 'NONE',  ( -3.550050802731187005, 2.983565686104819648, 0.3135853898029609677 ) ) ;
#14509=VECTOR ( 'NONE', #21547, 1000.000000000000000 ) ;
#14511=DIRECTION ( 'NONE',  ( -1.000000000000000000, 0.000000000000000000, 0.000000000000000000 ) ) ;
#14513=VECTOR ( 'NONE', #23467, 999.9999999999998863 ) ;
#14518=CARTESIAN_POINT ( 'NONE',  ( -2.162550801365593856, 2.228590825266444142, 2.752080473201636845 ) ) ;
#14524=EDGE_LOOP ( 'NONE', ( #30134, #31987, #4510, #10430 ) ) ;
#14525=CARTESIAN_POINT ( 'NONE',  ( -2.487550801365593589, 2.752080473201636845, -2.228590825266444142 ) ) ;
#14528=VECTOR ( 'NONE', #23150, 1000.000000000000000 ) ;
#14534=ORIENTED_EDGE ( 'NONE', *, *, #11231, .T. ) ;
#14535=CIRCLE ( 'NONE', #4419, 8.750000000000000000 ) ;
#14543=VECTOR ( 'NONE', #15322, 1000.000000000000114 ) ;
#14549=CARTESIAN_POINT ( 'NONE',  ( -3.337550801365593678, 1.828967928396027176, -3.368539882008727115 ) ) ;
#14550=ORIENTED_EDGE ( 'NONE', *, *, #19634, .T. ) ;
#14552=EDGE_LOOP ( 'NONE', ( #21905, #19283, #31393 ) ) ;
#14554=CIRCLE ( 'NONE', #19369, 2.999999999999999112 ) ;
#14560=FACE_OUTER_BOUND ( 'NONE', #31128, .T. ) ;
#14563=VECTOR ( 'NONE', #25222, 1000.000000000000000 ) ;
#14567=EDGE_CURVE ( 'NONE', #18257, #24987, #5667, .T. ) ;
#14578=VECTOR ( 'NONE', #29899, 1000.000000000000000 ) ;
#14579=CARTESIAN_POINT ( 'NONE',  ( 7.064632918400240769, -3.647351267791623552, 7.953573330858202617 ) ) ;
#14580=AXIS2_PLACEMENT_3D ( 'NONE', #5799, #6624, #6435 ) ;
#14585=CIRCLE ( 'NONE', #199, 6.248999999999998778 ) ;
#14587=PLANE ( 'NONE',  #2763 ) ;
#14594=CARTESIAN_POINT ( 'NONE',  ( 7.064632940817594076, -4.973063321323921926, 7.199384779417104419 ) ) ;
#14602=EDGE_CURVE ( 'NONE', #23931, #22574, #21538, .T. ) ;
#14603=ORIENTED_EDGE ( 'NONE', *, *, #29343, .F. ) ;
#14606=ADVANCED_FACE ( 'NONE', ( #3329 ), #11004, .T. ) ;
#14611=ORIENTED_EDGE ( 'NONE', *, *, #16946, .F. ) ;
#14630=FACE_OUTER_BOUND ( 'NONE', #8215, .T. ) ;
#14634=CARTESIAN_POINT ( 'NONE',  ( -6.250050802731187183, -1.887961173149512062, -2.331437884370912261 ) ) ;
#14636=CARTESIAN_POINT ( 'NONE',  ( -2.950050800000000528, -0.9222479816126459840, -3.113457007523259268 ) ) ;
#14644=B_SPLINE_CURVE_WITH_KNOTS ( 'NONE', 3,
 ( #11831, #9478, #1484, #19693, #14675, #30082, #11660, #21856, #17177, #32071 ),
 .UNSPECIFIED., .F., .F.,
 ( 4, 2, 2, 2, 4 ),
 ( 1.968338519010298316E-07, 0.0005467927057105484217, 0.001093388577569195854, 0.001639984449427843395, 0.002186580321286489201 ),
 .UNSPECIFIED. ) ;
#14648=CARTESIAN_POINT ( 'NONE',  ( 6.356382477965130562, 5.959271875177152289, 6.209963745178032291 ) ) ;
#14661=FACE_OUTER_BOUND ( 'NONE', #30042, .T. ) ;
#14665=CARTESIAN_POINT ( 'NONE',  ( 4.749760686538667009, -1.391664247347174754, -7.892520144992448472 ) ) ;
#14669=CARTESIAN_POINT ( 'NONE',  ( 7.249760686538667009, 0.7071067811865129338, 8.721381771256208282 ) ) ;
#14671=CARTESIAN_POINT ( 'NONE',  ( 7.249760686538667009, 0.000000000000000000, 0.000000000000000000 ) ) ;
#14672=CARTESIAN_POINT ( 'NONE',  ( 4.499760686538666121, 0.000000000000000000, 0.000000000000000000 ) ) ;
#14673=ORIENTED_EDGE ( 'NONE', *, *, #20235, .T. ) ;
#14674=EDGE_CURVE ( 'NONE', #29424, #24311, #14157, .T. ) ;
#14675=CARTESIAN_POINT ( 'NONE',  ( 6.357667873252798252, 2.398098878660953392, 8.266402141659449754 ) ) ;
#14677=CARTESIAN_POINT ( 'NONE',  ( -6.404531657079157725, -2.325406398514293205, 1.883076972206379818 ) ) ;
#14681=DIRECTION ( 'NONE',  ( -1.000000000000000000, 0.000000000000000000, 0.000000000000000000 ) ) ;
#14690=FACE_OUTER_BOUND ( 'NONE', #15454, .T. ) ;
#14691=CARTESIAN_POINT ( 'NONE',  ( 5.377543748152548098, 6.940565734314597002, 4.007137495034836405 ) ) ;
#14692=CARTESIAN_POINT ( 'NONE',  ( 7.064423539573519761, -0.7071067811874917064, -8.721381771257252780 ) ) ;
#14694=CARTESIAN_POINT ( 'NONE',  ( 6.038145268433182444, 6.194606843114086381, 5.783741681378098853 ) ) ;
#14695=CARTESIAN_POINT ( 'NONE',  ( 6.356382399260311900, -7.723816458760322412, -3.797266095948563347 ) ) ;
#14701=CARTESIAN_POINT ( 'NONE',  ( -2.287550801365593856, 2.228590825266444142, 2.752080473201636845 ) ) ;
#14708=DIRECTION ( 'NONE',  ( 1.000000000000000000, 0.000000000000000000, 0.000000000000000000 ) ) ;
#14709=B_SPLINE_CURVE_WITH_KNOTS ( 'NONE', 3,
 ( #5585, #25970, #10069, #30486, #7571, #27982, #5083, #23603, #10912, #1208 ),
 .UNSPECIFIED., .F., .F.,
 ( 4, 2, 2, 2, 4 ),
 ( 3.512955445812634541E-07, 0.0005479535487286800108, 0.001095555801912778812, 0.001643158055096877613, 0.002190760308280976631 ),
 .UNSPECIFIED. ) ;
#14714=CARTESIAN_POINT ( 'NONE',  ( 6.357667975083867162, 7.150591204917396304, 4.790963222208030281 ) ) ;
#14718=ORIENTED_EDGE ( 'NONE', *, *, #22277, .F. ) ;
#14719=DIRECTION ( 'NONE',  ( -1.000000000000000000, 0.000000000000000000, 0.000000000000000000 ) ) ;
#14723=SHAPE_REPRESENTATION_RELATIONSHIP ( 'NONE' , 'NONE' ,  #13478, #10724 ) ;
#14725=ORIENTED_EDGE ( 'NONE', *, *, #10345, .T. ) ;
#14727=ORIENTED_EDGE ( 'NONE', *, *, #12064, .F. ) ;
#14731=ORIENTED_EDGE ( 'NONE', *, *, #9517, .F. ) ;
#14756=CARTESIAN_POINT ( 'NONE',  ( -6.837550801365592790, -3.675193018007245627, 1.088641768524163389 ) ) ;
#14770=ORIENTED_EDGE ( 'NONE', *, *, #16566, .F. ) ;
#14773=ORIENTED_EDGE ( 'NONE', *, *, #9604, .T. ) ;
#14775=CARTESIAN_POINT ( 'NONE',  ( 3.499999999999999556, 0.000000000000000000, 0.000000000000000000 ) ) ;
#14777=CARTESIAN_POINT ( 'NONE',  ( 3.499999999999999556, -6.700937042937042065, -2.183447440113257976 ) ) ;
#14782=ADVANCED_FACE ( 'NONE', ( #25479 ), #13107, .T. ) ;
#14789=CARTESIAN_POINT ( 'NONE',  ( -4.050050802731187005, -2.331437884370912705, 1.887961173149512062 ) ) ;
#14790=ORIENTED_EDGE ( 'NONE', *, *, #17611, .T. ) ;
#14791=CARTESIAN_POINT ( 'NONE',  ( -4.750050800000000351, -3.113457007523259268, 0.9222479816126455399 ) ) ;
#14795=CARTESIAN_POINT ( 'NONE',  ( -2.150050802731187538, 0.3135853898029611342, -2.983565686104819648 ) ) ;
#14796=CARTESIAN_POINT ( 'NONE',  ( 0.000000000000000000, 0.000000000000000000, 0.000000000000000000 ) ) ;
#14800=CARTESIAN_POINT ( 'NONE',  ( -2.900050800000000706, 0.3135853898029611342, -2.983565686104819648 ) ) ;
#14801=VERTEX_POINT ( 'NONE', #10436 ) ;
#14803=ORIENTED_EDGE ( 'NONE', *, *, #21018, .T. ) ;
#14814=CARTESIAN_POINT ( 'NONE',  ( 5.489344087273877015, -6.152099123112487078, 5.297876218488298150 ) ) ;
#14815=CARTESIAN_POINT ( 'NONE',  ( 5.489321676144490958, -3.969109389279916744, -7.082488557107332383 ) ) ;
#14816=CARTESIAN_POINT ( 'NONE',  ( 4.749760686538667009, -6.940565734314625423, 4.007137495034787555 ) ) ;
#14818=CARTESIAN_POINT ( 'NONE',  ( -8.000050800000000351, 2.947991532268304127, 1.750383400925231703 ) ) ;
#14819=DIRECTION ( 'NONE',  ( 1.000000000000000000, 0.000000000000000000, -0.000000000000000000 ) ) ;
#14823=CARTESIAN_POINT ( 'NONE',  ( -8.062550801365594211, 0.3701630799359330593, -3.521866450007987037 ) ) ;
#14825=CARTESIAN_POINT ( 'NONE',  ( -8.104531657079158791, -0.3127741368606806738, 2.975847129947406522 ) ) ;
#14832=ORIENTED_EDGE ( 'NONE', *, *, #9517, .T. ) ;
#14833=CARTESIAN_POINT ( 'NONE',  ( 6.037141812302425414, 1.911013226338409199, 8.256172215043582341 ) ) ;
#14837=CARTESIAN_POINT ( 'NONE',  ( 6.524595551582240915, 7.790581746767737847, 3.779376390944498620 ) ) ;
#14847=CARTESIAN_POINT ( 'NONE',  ( -2.437550801365593767, 3.675193018007247403, -1.088641768524161391 ) ) ;
#14849=CARTESIAN_POINT ( 'NONE',  ( 7.249760686538667009, -7.135485519862032611, 5.064320921489797733 ) ) ;
#14859=EDGE_CURVE ( 'NONE', #4708, #14801, #5942, .T. ) ;
#14865=DIRECTION ( 'NONE',  ( 0.000000000000000000, 0.000000000000000000, 1.000000000000000000 ) ) ;
#14871=B_SPLINE_CURVE_WITH_KNOTS ( 'NONE', 3,
 ( #6677, #29909, #11677, #16867, #27063, #4166, #27568, #29406, #14332, #4667 ),
 .UNSPECIFIED., .F., .F.,
 ( 4, 2, 2, 2, 4 ),
 ( 2.493548413898819905E-07, 0.0005478513795029398394, 0.001095453404164489775, 0.001643055428826039601, 0.002190657453487589428 ),
 .UNSPECIFIED. ) ;
#14880=VERTEX_POINT ( 'NONE', #11239 ) ;
#14900=ORIENTED_EDGE ( 'NONE', *, *, #1015, .T. ) ;
#14903=CARTESIAN_POINT ( 'NONE',  ( -6.587550801365593678, 0.3701630799359330593, -3.521866450007987037 ) ) ;
#14907=DIRECTION ( 'NONE',  ( 0.000000000000000000, -0.08715574274766134388, -0.9961946980917452121 ) ) ;
#14908=FACE_OUTER_BOUND ( 'NONE', #13915, .T. ) ;
#14923=PLANE ( 'NONE',  #27302 ) ;
#14931=( BOUNDED_CURVE ( )  B_SPLINE_CURVE ( 2, ( #22043, #19377, #24875, #4151, #27048, #24517, #32264, #4649, #1335, #11509, #29575 ),
 .UNSPECIFIED., .F., .F. ) 
 B_SPLINE_CURVE_WITH_KNOTS ( ( 3, 2, 2, 2, 2, 3 ),
 ( 0.7478822619934377691, 0.7500000000000000000, 0.7656250000000000000, 0.7812500000000000000, 0.7968750000000000000, 0.8103822619934377691 ),
 .UNSPECIFIED. ) 
 CURVE ( )  GEOMETRIC_REPRESENTATION_ITEM ( )  RATIONAL_B_SPLINE_CURVE ( ( 0.9821626249036861100, 0.9896829947469995004, 1.000000000000000000, 0.9238795325112867385, 1.000000000000000000, 0.9238795325112867385, 1.000000000000000000, 0.9238795325112867385, 1.000000000000000000, 0.9341965377642872381, 0.9821626249036861100 ) ) 
 REPRESENTATION_ITEM ( '' )  );
#14935=B_SPLINE_CURVE_WITH_KNOTS ( 'NONE', 3,
 ( #14165, #24363, #1480, #9135, #6967, #29730, #30386, #25017, #25191, #9318 ),
 .UNSPECIFIED., .F., .F.,
 ( 4, 2, 2, 2, 4 ),
 ( 3.032460776734494026E-07, 0.0005479053915603979358, 0.001095507537043122551, 0.001643109682525847057, 0.002190711828008571564 ),
 .UNSPECIFIED. ) ;
#14942=CARTESIAN_POINT ( 'NONE',  ( -4.200050802731187360, 0.9222479816126443186, 3.113457007523260156 ) ) ;
#14943=ORIENTED_EDGE ( 'NONE', *, *, #24860, .F. ) ;
#14944=CARTESIAN_POINT ( 'NONE',  ( -3.500050800000000351, 2.983565686104819648, 0.3135853898029609677 ) ) ;
#14952=ORIENTED_EDGE ( 'NONE', *, *, #2273, .F. ) ;
#14955=CARTESIAN_POINT ( 'NONE',  ( 3.500000000000000000, 0.000000000000000000, 0.000000000000000000 ) ) ;
#14958=ADVANCED_FACE ( 'NONE', ( #26786 ), #21618, .T. ) ;
#14963=CARTESIAN_POINT ( 'NONE',  ( 6.530491482054475050, -2.114164693852647048, 8.398420403995366712 ) ) ;
#14966=AXIS2_PLACEMENT_3D ( 'NONE', #9118, #26541, #6636 ) ;
#14967=DIRECTION ( 'NONE',  ( -0.000000000000000000, -0.9659258262890662028, -0.2588190451025286776 ) ) ;
#14968=CARTESIAN_POINT ( 'NONE',  ( 7.249760686538667009, 6.940565734314597002, 4.007137495034836405 ) ) ;
#14969=CIRCLE ( 'NONE', #1654, 8.500000000000000000 ) ;
#14976=CARTESIAN_POINT ( 'NONE',  ( -8.000050799999991469, 1.058074100335029355, 3.097767084515848701 ) ) ;
#14981=CARTESIAN_POINT ( 'NONE',  ( -5.162550801365593856, -2.752080473201636845, 2.228590825266444586 ) ) ;
#14983=CARTESIAN_POINT ( 'NONE',  ( -6.704531657079157547, 2.975847129947406522, 0.3127741368606808403 ) ) ;
#14992=CIRCLE ( 'NONE', #28894, 8.750000000000000000 ) ;
#14996=CARTESIAN_POINT ( 'NONE',  ( 6.356381935169120645, 2.055898738447997864, 8.357622142800094522 ) ) ;
#14998=ADVANCED_FACE ( 'NONE', ( #14080 ), #31661, .F. ) ;
#15003=CARTESIAN_POINT ( 'NONE',  ( 5.377543748152550762, 6.139290821770327256, -5.151476664237414127 ) ) ;
#15004=LINE ( 'NONE', #7838, #14563 ) ;
#15011=CARTESIAN_POINT ( 'NONE',  ( 5.377543748152548986, 7.892520144992453801, -1.391664247347147443 ) ) ;
#15013=CARTESIAN_POINT ( 'NONE',  ( -3.287550801365593856, 2.752080473201636845, -2.228590825266444142 ) ) ;
#15014=DIRECTION ( 'NONE',  ( 0.000000000000000000, 0.000000000000000000, -1.000000000000000000 ) ) ;
#15015=AXIS2_PLACEMENT_3D ( 'NONE', #23913, #13861, #715 ) ;
#15020=VERTEX_POINT ( 'NONE', #904 ) ;
#15035=ORIENTED_EDGE ( 'NONE', *, *, #16922, .F. ) ;
#15040=CIRCLE ( 'NONE', #8653, 2.999999999999999556 ) ;
#15054=CARTESIAN_POINT ( 'NONE',  ( -7.980601973981865882, 2.418815195390975781, -2.640139169206693115 ) ) ;
#15055=LINE ( 'NONE', #29682, #10806 ) ;
#15059=EDGE_LOOP ( 'NONE', ( #15260, #32774, #31973 ) ) ;
#15069=AXIS2_PLACEMENT_3D ( 'NONE', #29936, #7023, #14865 ) ;
#15074=CARTESIAN_POINT ( 'NONE',  ( -8.000050800000000351, -1.836970198721030181E-16, -3.000000000000000444 ) ) ;
#15079=CARTESIAN_POINT ( 'NONE',  ( 5.612974384376779646, -4.279837954023520297, 7.013635602076194075 ) ) ;
#15084=CARTESIAN_POINT ( 'NONE',  ( -6.037550801365593856, -3.675193018007245627, 1.088641768524163389 ) ) ;
#15086=AXIS2_PLACEMENT_3D ( 'NONE', #30915, #2845, #20559 ) ;
#15091=EDGE_LOOP ( 'NONE', ( #29817, #24492, #30335 ) ) ;
#15093=EDGE_CURVE ( 'NONE', #19561, #10302, #12905, .T. ) ;
#15095=VECTOR ( 'NONE', #18495, 1000.000000000000000 ) ;
#15096=DIRECTION ( 'NONE',  ( 0.000000000000000000, 0.9659258262890670910, 0.2588190451025253469 ) ) ;
#15100=CIRCLE ( 'NONE', #27403, 2.999999999999999112 ) ;
#15104=DIRECTION ( 'NONE',  ( 0.000000000000000000, 0.000000000000000000, -1.000000000000000000 ) ) ;
#15105=EDGE_CURVE ( 'NONE', #5620, #26082, #664, .T. ) ;
#15124=CIRCLE ( 'NONE', #27954, 8.750000000000000000 ) ;
#15127=AXIS2_PLACEMENT_3D ( 'NONE', #32577, #1649, #19697 ) ;
#15130=CARTESIAN_POINT ( 'NONE',  ( -1.750050802731187405, -0.3135853898029607456, 2.983565686104819648 ) ) ;
#15131=ORIENTED_EDGE ( 'NONE', *, *, #32704, .T. ) ;
#15134=CARTESIAN_POINT ( 'NONE',  ( -4.437550801365594211, -3.675193018007246071, 1.088641768524163167 ) ) ;
#15136=EDGE_CURVE ( 'NONE', #13848, #22878, #19860, .T. ) ;
#15139=ORIENTED_EDGE ( 'NONE', *, *, #12610, .T. ) ;
#15141=CARTESIAN_POINT ( 'NONE',  ( 5.489344087273876127, -5.297876218488277722, -6.152099123112504842 ) ) ;
#15146=ORIENTED_EDGE ( 'NONE', *, *, #4305, .T. ) ;
#15154=CARTESIAN_POINT ( 'NONE',  ( -2.354101222566610918, 0.8862716126563827679, 3.215327897825512427 ) ) ;
#15159=AXIS2_PLACEMENT_3D ( 'NONE', #19971, #30485, #2732 ) ;
#15160=DIRECTION ( 'NONE',  ( -1.000000000000000000, -0.000000000000000000, -0.000000000000000000 ) ) ;
#15163=ORIENTED_EDGE ( 'NONE', *, *, #1446, .T. ) ;
#15169=LINE ( 'NONE', #32910, #24133 ) ;
#15173=CARTESIAN_POINT ( 'NONE',  ( -7.262550801365593500, 0.3701630799359330593, -3.521866450007987037 ) ) ;
#15176=CARTESIAN_POINT ( 'NONE',  ( -8.004531657079157370, -2.325406398514293205, 1.883076972206379818 ) ) ;
#15177=AXIS2_PLACEMENT_3D ( 'NONE', #25689, #21180, #31377 ) ;
#15179=EDGE_CURVE ( 'NONE', #15684, #21443, #116, .T. ) ;
#15180=DIRECTION ( 'NONE',  ( 0.000000000000000000, 0.7071067811865442421, -0.7071067811865509034 ) ) ;
#15182=DIRECTION ( 'NONE',  ( -1.000000000000000000, -0.000000000000000000, -0.000000000000000000 ) ) ;
#15188=LINE ( 'NONE', #1381, #10222 ) ;
#15193=DIRECTION ( 'NONE',  ( 0.000000000000000000, 0.000000000000000000, 1.000000000000000000 ) ) ;
#15194=CARTESIAN_POINT ( 'NONE',  ( 4.749760686538667009, -7.892520144992443143, 1.391664247347202288 ) ) ;
#15196=CARTESIAN_POINT ( 'NONE',  ( -8.000050800000002127, -2.992755258463658308, -0.2534658811743740192 ) ) ;
#15203=CARTESIAN_POINT ( 'NONE',  ( -7.112550801365592257, 3.675193018007247403, -1.088641768524161391 ) ) ;
#15207=VERTEX_POINT ( 'NONE', #1013 ) ;
#15209=EDGE_LOOP ( 'NONE', ( #32999, #2421, #14832, #9372 ) ) ;
#15218=LINE ( 'NONE', #23073, #19921 ) ;
#15229=ORIENTED_EDGE ( 'NONE', *, *, #13642, .F. ) ;
#15231=CARTESIAN_POINT ( 'NONE',  ( -1.738758153310166144, 1.323625320507516134, 3.284597389079960461 ) ) ;
#15232=CARTESIAN_POINT ( 'NONE',  ( -6.412550801365592967, 1.828967928396027398, -3.368539882008727115 ) ) ;
#15233=DIRECTION ( 'NONE',  ( -1.000000000000000000, 0.000000000000000000, 0.000000000000000000 ) ) ;
#15244=EDGE_CURVE ( 'NONE', #29424, #15425, #9437, .T. ) ;
#15252=CARTESIAN_POINT ( 'NONE',  ( 3.499999999999999556, 7.003298780661427969, 4.817032923780590004 ) ) ;
#15253=CARTESIAN_POINT ( 'NONE',  ( 4.749760686538667009, 6.139290821770327256, -5.151476664237414127 ) ) ;
#15254=CARTESIAN_POINT ( 'NONE',  ( -7.837550801365593678, 1.088641768524161613, 3.675193018007246959 ) ) ;
#15257=CARTESIAN_POINT ( 'NONE',  ( 0.000000000000000000, -4.147285340411747789, -5.698247474649445365 ) ) ;
#15260=ORIENTED_EDGE ( 'NONE', *, *, #17101, .T. ) ;
#15272=DIRECTION ( 'NONE',  ( 0.000000000000000000, 0.000000000000000000, 1.000000000000000000 ) ) ;
#15275=CARTESIAN_POINT ( 'NONE',  ( -5.312942406915326821, -3.366872799099910998E-15, -3.000000000000000000 ) ) ;
#15286=CARTESIAN_POINT ( 'NONE',  ( 0.000000000000000000, 6.226349476952025341, -0.5315761383463578627 ) ) ;
#15287=CARTESIAN_POINT ( 'NONE',  ( 6.880159790065803804, 8.691376398188699781, 0.8322990769132707634 ) ) ;
#15293=CARTESIAN_POINT ( 'NONE',  ( -7.087550801365593678, 2.228590825266444142, 2.752080473201636845 ) ) ;
#15299=ORIENTED_EDGE ( 'NONE', *, *, #6048, .F. ) ;
#15309=ORIENTED_EDGE ( 'NONE', *, *, #24874, .F. ) ;
#15316=DIRECTION ( 'NONE',  ( 0.000000000000000000, 0.000000000000000000, 1.000000000000000000 ) ) ;
#15318=CARTESIAN_POINT ( 'NONE',  ( 4.749760686538667009, -1.391664247347174754, -7.892520144992448472 ) ) ;
#15322=DIRECTION ( 'NONE',  ( 0.000000000000000000, -0.08715574274764385787, -0.9961946980917467664 ) ) ;
#15326=ORIENTED_EDGE ( 'NONE', *, *, #1911, .F. ) ;
#15327=CARTESIAN_POINT ( 'NONE',  ( -5.562550801365593323, 2.752080473201636845, -2.228590825266444142 ) ) ;
#15328=ORIENTED_EDGE ( 'NONE', *, *, #2633, .F. ) ;
#15329=CARTESIAN_POINT ( 'NONE',  ( -8.350050799999999995, 3.113457007523260156, -0.9222479816126439855 ) ) ;
#15340=CARTESIAN_POINT ( 'NONE',  ( 7.249760686538667009, -4.007137495034764463, -6.940565734314639634 ) ) ;
#15344=DIRECTION ( 'NONE',  ( -1.000000000000000000, 0.000000000000000000, -0.000000000000000000 ) ) ;
#15345=CARTESIAN_POINT ( 'NONE',  ( 0.000000000000000000, -6.700937042937042065, 0.8165525598867410251 ) ) ;
#15347=CARTESIAN_POINT ( 'NONE',  ( -7.750050802731187183, 0.3135853898029611342, -2.983565686104819648 ) ) ;
#15349=EDGE_CURVE ( 'NONE', #9882, #29104, #21977, .T. ) ;
#15352=CARTESIAN_POINT ( 'NONE',  ( 6.883866482134012976, 8.691827696555170846, -0.8319830743949774288 ) ) ;
#15354=CARTESIAN_POINT ( 'NONE',  ( -7.012550801365593500, 3.368539882008727115, 1.828967928396026954 ) ) ;
#15358=ORIENTED_EDGE ( 'NONE', *, *, #18402, .F. ) ;
#15379=ORIENTED_EDGE ( 'NONE', *, *, #18557, .T. ) ;
#15380=EDGE_CURVE ( 'NONE', #26222, #21921, #28412, .T. ) ;
#15382=CARTESIAN_POINT ( 'NONE',  ( -7.312550801365594211, -1.088641768524163611, -3.675193018007245627 ) ) ;
#15383=EDGE_CURVE ( 'NONE', #23656, #18044, #28971, .T. ) ;
#15384=CARTESIAN_POINT ( 'NONE',  ( 5.887530024394195038, -8.008238305624862718, 2.518482652462528115 ) ) ;
#15389=ADVANCED_FACE ( 'NONE', ( #32943 ), #10667, .F. ) ;
#15403=DIRECTION ( 'NONE',  ( 0.000000000000000000, -0.9961946980917442129, -0.08715574274767322327 ) ) ;
#15405=ORIENTED_EDGE ( 'NONE', *, *, #19911, .F. ) ;
#15407=DIRECTION ( 'NONE',  ( -1.000000000000000000, 0.000000000000000000, 0.000000000000000000 ) ) ;
#15411=EDGE_CURVE ( 'NONE', #26986, #19129, #10170, .T. ) ;
#15412=CARTESIAN_POINT ( 'NONE',  ( 7.249760686538667009, 0.000000000000000000, 0.000000000000000000 ) ) ;
#15413=ORIENTED_EDGE ( 'NONE', *, *, #6788, .T. ) ;
#15423=CARTESIAN_POINT ( 'NONE',  ( 7.249760686538667009, -7.906491560603638113, -3.748318449932378282 ) ) ;
#15425=VERTEX_POINT ( 'NONE', #7849 ) ;
#15430=DIRECTION ( 'NONE',  ( 0.000000000000000000, -0.2079116908177663092, 0.9781476007338040235 ) ) ;
#15444=ORIENTED_EDGE ( 'NONE', *, *, #29075, .F. ) ;
#15445=CARTESIAN_POINT ( 'NONE',  ( -5.937550801365592434, -3.368539882008727115, -1.828967928396028064 ) ) ;
#15447=DIRECTION ( 'NONE',  ( 0.000000000000000000, 0.000000000000000000, 1.000000000000000000 ) ) ;
#15448=FACE_OUTER_BOUND ( 'NONE', #16530, .T. ) ;
#15454=EDGE_LOOP ( 'NONE', ( #13124, #3536, #10083, #7894 ) ) ;
#15458=VERTEX_POINT ( 'NONE', #23379 ) ;
#15463=AXIS2_PLACEMENT_3D ( 'NONE', #14775, #4755, #2438 ) ;
#15471=FACE_OUTER_BOUND ( 'NONE', #8998, .T. ) ;
#15476=DIRECTION ( 'NONE',  ( -1.000000000000000000, -0.000000000000000000, -0.000000000000000000 ) ) ;
#15479=CARTESIAN_POINT ( 'NONE',  ( -7.250050802731188071, -2.331437884370912705, 1.887961173149512062 ) ) ;
#15483=ORIENTED_EDGE ( 'NONE', *, *, #16304, .T. ) ;
#15484=CARTESIAN_POINT ( 'NONE',  ( -6.462550801365593678, 0.3701630799359330593, -3.521866450007987037 ) ) ;
#15486=CARTESIAN_POINT ( 'NONE',  ( -3.854531657079157014, -2.846291840500172921, -1.545410377633947618 ) ) ;
#15497=ADVANCED_FACE ( 'NONE', ( #483 ), #25732, .T. ) ;
#15498=VECTOR ( 'NONE', #17686, 1000.000000000000000 ) ;
#15502=CARTESIAN_POINT ( 'NONE',  ( 6.530491482054473273, -8.398420403995359607, -2.114164693852676358 ) ) ;
#15503=VECTOR ( 'NONE', #7049, 1000.000000000000227 ) ;
#15509=CARTESIAN_POINT ( 'NONE',  ( -7.600050802731185939, 3.113457007523260156, -0.9222479816126439855 ) ) ;
#15512=DIRECTION ( 'NONE',  ( 1.000000000000000000, -0.000000000000000000, 0.000000000000000000 ) ) ;
#15516=CARTESIAN_POINT ( 'NONE',  ( -4.862550801365594033, 0.3701630799359330593, -3.521866450007987037 ) ) ;
#15539=AXIS2_PLACEMENT_3D ( 'NONE', #8729, #18939, #24086 ) ;
#15548=ORIENTED_EDGE ( 'NONE', *, *, #11670, .F. ) ;
#15550=ORIENTED_EDGE ( 'NONE', *, *, #20235, .F. ) ;
#15552=CARTESIAN_POINT ( 'NONE',  ( -6.712550801365592790, -3.675193018007245627, 1.088641768524163389 ) ) ;
#15554=AXIS2_PLACEMENT_3D ( 'NONE', #17273, #32489, #9550 ) ;
#15567=EDGE_LOOP ( 'NONE', ( #20552, #3762, #21291, #14611, #31850, #11541, #14141, #321, #3711, #7339, #9503, #26046, #27804, #17988, #28783, #20008, #1065, #403, #23190, #11222, #17624, #32123, #20786, #14289, #29998, #1407, #24962, #5706, #7991, #11526, #6752, #29633, #21652, #26816, #29904, #19250, #11158, #20243, #9621, #19248, #27365, #12515, #18784, #14226, #31448, #14790, #33, #26676, #5096, #737, #19796, #28321, #30818, #24391, #18272, #13801, #26745 ) ) ;
#15575=CARTESIAN_POINT ( 'NONE',  ( 7.249760686538667009, 0.000000000000000000, 0.000000000000000000 ) ) ;
#15580=VECTOR ( 'NONE', #13784, 1000.000000000000000 ) ;
#15587=DIRECTION ( 'NONE',  ( 0.000000000000000000, 0.2588190451025358940, -0.9659258262890643154 ) ) ;
#15595=VECTOR ( 'NONE', #32676, 1000.000000000000114 ) ;
#15601=ORIENTED_EDGE ( 'NONE', *, *, #32175, .F. ) ;
#15604=CARTESIAN_POINT ( 'NONE',  ( 6.037141869538512395, -7.104659103919376939, 4.619542287584878615 ) ) ;
#15606=ORIENTED_EDGE ( 'NONE', *, *, #7611, .T. ) ;
#15608=ORIENTED_EDGE ( 'NONE', *, *, #19625, .T. ) ;
#15613=CARTESIAN_POINT ( 'NONE',  ( -3.356376981307136464, -0.1572233378491262878, 2.999999999999999556 ) ) ;
#15616=CIRCLE ( 'NONE', #683, 8.500000000000000000 ) ;
#15622=CIRCLE ( 'NONE', #6543, 8.500000000000000000 ) ;
#15623=AXIS2_PLACEMENT_3D ( 'NONE', #19397, #2001, #9662 ) ;
#15631=ADVANCED_FACE ( 'NONE', ( #3813 ), #11010, .F. ) ;
#15632=CARTESIAN_POINT ( 'NONE',  ( -4.787550801365593856, 3.521866450007987037, 0.3701630799359328372 ) ) ;
#15633=CIRCLE ( 'NONE', #675, 2.999999999999999112 ) ;
#15636=CARTESIAN_POINT ( 'NONE',  ( 0.000000000000000000, -7.673322273190749776, 3.656518192455051608 ) ) ;
#15643=VERTEX_POINT ( 'NONE', #21211 ) ;
#15653=CARTESIAN_POINT ( 'NONE',  ( -2.459135176628032049, 0.1657091670264760619, 3.101200306062372292 ) ) ;
#15659=ORIENTED_EDGE ( 'NONE', *, *, #25283, .T. ) ;
#15661=AXIS2_PLACEMENT_3D ( 'NONE', #8153, #3004, #18360 ) ;
#15663=CARTESIAN_POINT ( 'NONE',  ( 4.749760686538667009, 8.385837730238846314E-14, -8.014274990069656823 ) ) ;
#15665=CARTESIAN_POINT ( 'NONE',  ( 4.749760686538667009, 1.391664247347333294, -7.892520144992419162 ) ) ;
#15669=EDGE_CURVE ( 'NONE', #26254, #29588, #58, .T. ) ;
#15674=VERTEX_POINT ( 'NONE', #18684 ) ;
#15677=CARTESIAN_POINT ( 'NONE',  ( -2.512550801365593056, -1.088641768524163389, -3.675193018007246071 ) ) ;
#15679=CARTESIAN_POINT ( 'NONE',  ( -2.954531657079157547, -0.9198621039125872700, -3.105402419394638791 ) ) ;
#15684=VERTEX_POINT ( 'NONE', #31751 ) ;
#15685=CYLINDRICAL_SURFACE ( 'NONE', #25240, 2.999999999999999112 ) ;
#15696=CARTESIAN_POINT ( 'NONE',  ( 6.356382477965130562, 6.947086032709933967, 5.080803740829747284 ) ) ;
#15705=CARTESIAN_POINT ( 'NONE',  ( -5.562550801365593323, 2.752080473201636845, -2.228590825266444142 ) ) ;
#15722=ORIENTED_EDGE ( 'NONE', *, *, #29662, .F. ) ;
#15723=CARTESIAN_POINT ( 'NONE',  ( 7.249760686538667009, 0.000000000000000000, 0.000000000000000000 ) ) ;
#15726=EDGE_LOOP ( 'NONE', ( #11563, #25852, #26244 ) ) ;
#15728=AXIS2_PLACEMENT_3D ( 'NONE', #18832, #29032, #13941 ) ;
#15730=ORIENTED_EDGE ( 'NONE', *, *, #15179, .T. ) ;
#15731=CARTESIAN_POINT ( 'NONE',  ( -5.350050802731187716, 0.3135853898029611342, -2.983565686104819648 ) ) ;
#15744=AXIS2_PLACEMENT_3D ( 'NONE', #24043, #28433, #23891 ) ;
#15748=ADVANCED_FACE ( 'NONE', ( #24692 ), #14480, .T. ) ;
#15757=CARTESIAN_POINT ( 'NONE',  ( 7.249760686538667009, 8.721381771256204729, -0.7071067811865423547 ) ) ;
#15761=CARTESIAN_POINT ( 'NONE',  ( 4.749760686538667009, -2.789499415801756586E-14, 8.014274990069656823 ) ) ;
#15769=EDGE_CURVE ( 'NONE', #26082, #16537, #21057, .T. ) ;
#15787=EDGE_CURVE ( 'NONE', #12441, #14119, #19685, .T. ) ;
#15788=CARTESIAN_POINT ( 'NONE',  ( -6.906376978575949899, 0.1572233378491243172, -2.999999999999999556 ) ) ;
#15795=CARTESIAN_POINT ( 'NONE',  ( 5.612718383992090665, -8.123482740191962037, -1.229942497144119296 ) ) ;
#15798=CARTESIAN_POINT ( 'NONE',  ( -2.550050802731187005, -0.3135853898029607456, 2.983565686104819648 ) ) ;
#15801=LINE ( 'NONE', #25500, #6908 ) ;
#15809=FACE_OUTER_BOUND ( 'NONE', #16472, .T. ) ;
#15812=CARTESIAN_POINT ( 'NONE',  ( -2.374773405519150504, 0.7814962286037724359, 3.198731613255573425 ) ) ;
#15818=PLANE ( 'NONE',  #24164 ) ;
#15819=EDGE_CURVE ( 'NONE', #26682, #10466, #29429, .T. ) ;
#15822=CARTESIAN_POINT ( 'NONE',  ( -3.712942406915326288, 4.884725290497410777E-15, -2.999999999999999556 ) ) ;
#15830=CARTESIAN_POINT ( 'NONE',  ( -7.650050802731187538, 2.331437884370912705, -1.887961173149511618 ) ) ;
#15831=VERTEX_POINT ( 'NONE', #20532 ) ;
#15832=CARTESIAN_POINT ( 'NONE',  ( -3.454531657079157103, 2.846291840500173365, 1.545410377633946952 ) ) ;
#15845=CARTESIAN_POINT ( 'NONE',  ( 6.530491627857225367, 8.330327812606292071, -2.368289848745672277 ) ) ;
#15846=ORIENTED_EDGE ( 'NONE', *, *, #21738, .F. ) ;
#15847=DIRECTION ( 'NONE',  ( 1.000000000000000000, -0.000000000000000000, -0.000000000000000000 ) ) ;
#15848=DIRECTION ( 'NONE',  ( 1.000000000000000000, -0.000000000000000000, -0.000000000000000000 ) ) ;
#15852=CARTESIAN_POINT ( 'NONE',  ( -5.012550801365594388, -3.368539882008727115, -1.828967928396028064 ) ) ;
#15861=DIRECTION ( 'NONE',  ( 0.000000000000000000, -0.4067366430757888840, -0.9135454576426059736 ) ) ;
#15865=ORIENTED_EDGE ( 'NONE', *, *, #4088, .T. ) ;
#15882=CARTESIAN_POINT ( 'NONE',  ( -3.662550801365593411, -0.3701630799359326152, 3.521866450007987037 ) ) ;
#15883=CARTESIAN_POINT ( 'NONE',  ( 3.499999999999999556, -6.200809695932770538, -0.7745709230445805282 ) ) ;
#15900=ADVANCED_FACE ( 'NONE', ( #2477 ), #18154, .T. ) ;
#15901=DIRECTION ( 'NONE',  ( 0.000000000000000000, 0.9063077870366462729, 0.4226182617407076014 ) ) ;
#15907=CARTESIAN_POINT ( 'NONE',  ( 5.885541736258995904, -8.006759975090634640, -2.519172009312012683 ) ) ;
#15909=DIRECTION ( 'NONE',  ( -1.000000000000000000, 0.000000000000000000, 0.000000000000000000 ) ) ;
#15912=PLANE ( 'NONE',  #4856 ) ;
#15919=EDGE_CURVE ( 'NONE', #8879, #22005, #5471, .T. ) ;
#15921=PLANE ( 'NONE',  #7017 ) ;
#15925=LINE ( 'NONE', #16573, #17051 ) ;
#15930=DIRECTION ( 'NONE',  ( 0.000000000000000000, 0.9945218953682729568, 0.1045284632676571068 ) ) ;
#15934=CARTESIAN_POINT ( 'NONE',  ( -3.312942406915326377, -5.022711880624455567E-15, 2.999999999999999556 ) ) ;
#15938=PLANE ( 'NONE',  #21479 ) ;
#15943=CARTESIAN_POINT ( 'NONE',  ( 0.000000000000000000, 6.704570150426983233, 5.172265885002680363 ) ) ;
#15950=ORIENTED_EDGE ( 'NONE', *, *, #647, .T. ) ;
#15951=ORIENTED_EDGE ( 'NONE', *, *, #29718, .T. ) ;
#15955=CARTESIAN_POINT ( 'NONE',  ( 3.499999999999999556, 5.241389472434724084, -4.711457988287002685 ) ) ;
#15959=CARTESIAN_POINT ( 'NONE',  ( 5.489343806296445472, 1.307372367723745654, -8.012901424861395228 ) ) ;
#15963=CARTESIAN_POINT ( 'NONE',  ( -4.112942406915325755, -5.022711880624455567E-15, 2.999999999999999556 ) ) ;
#15966=CARTESIAN_POINT ( 'NONE',  ( 7.249760686538667009, 0.000000000000000000, 0.000000000000000000 ) ) ;
#15973=CARTESIAN_POINT ( 'NONE',  ( -3.062550801365593323, 3.521866450007987037, 0.3701630799359328372 ) ) ;
#15975=CARTESIAN_POINT ( 'NONE',  ( -4.404531657079157725, 2.325406398514293205, -1.883076972206379374 ) ) ;
#15978=CARTESIAN_POINT ( 'NONE',  ( -5.250050800000000351, 1.549418761218566143, -2.853674364686379583 ) ) ;
#15989=CARTESIAN_POINT ( 'NONE',  ( 5.489321486716459475, -7.976795196726676807, -1.512021494499669716 ) ) ;
#15990=CARTESIAN_POINT ( 'NONE',  ( 7.064632918400242545, 8.437262856154193358, -2.318425219014147665 ) ) ;
#15992=CARTESIAN_POINT ( 'NONE',  ( 7.064423600674403225, -8.466096581344336514, 2.210816291637388797 ) ) ;
#15997=CARTESIAN_POINT ( 'NONE',  ( -2.262550801365593056, 3.521866450007987037, 0.3701630799359328372 ) ) ;
#15999=DIRECTION ( 'NONE',  ( 0.000000000000000000, -0.9510565162951504226, -0.3090169943749573322 ) ) ;
#16001=EDGE_LOOP ( 'NONE', ( #15444, #18615, #26126, #20857 ) ) ;
#16003=FACE_OUTER_BOUND ( 'NONE', #385, .T. ) ;
#16006=CARTESIAN_POINT ( 'NONE',  ( 7.249760686538667009, -7.892520144992443143, 1.391664247347202288 ) ) ;
#16009=CARTESIAN_POINT ( 'NONE',  ( -2.787550801365593411, -3.521866450007987037, -0.3701630799359323931 ) ) ;
#16015=CARTESIAN_POINT ( 'NONE',  ( -5.762942409646513831, 3.284080845023683730E-15, 3.000000000000000000 ) ) ;
#16017=AXIS2_PLACEMENT_3D ( 'NONE', #20796, #22346, #10438 ) ;
#16022=LINE ( 'NONE', #16214, #3961 ) ;
#16023=ORIENTED_EDGE ( 'NONE', *, *, #11968, .F. ) ;
#16028=CARTESIAN_POINT ( 'NONE',  ( -5.612550801365594033, 1.828967928396027398, -3.368539882008727115 ) ) ;
#16033=CARTESIAN_POINT ( 'NONE',  ( -7.887550801365593500, 2.228590825266444142, 2.752080473201636845 ) ) ;
#16040=ORIENTED_EDGE ( 'NONE', *, *, #16053, .F. ) ;
#16047=DIRECTION ( 'NONE',  ( 1.000000000000000000, -0.000000000000000000, -0.000000000000000000 ) ) ;
#16049=EDGE_CURVE ( 'NONE', #18044, #26528, #13460, .T. ) ;
#16050=DIRECTION ( 'NONE',  ( -0.000000000000000000, -0.8191520442889868026, -0.5735764363510532649 ) ) ;
#16052=ORIENTED_EDGE ( 'NONE', *, *, #24435, .F. ) ;
#16053=EDGE_CURVE ( 'NONE', #18491, #31391, #28434, .T. ) ;
#16054=B_SPLINE_CURVE_WITH_KNOTS ( 'NONE', 3,
 ( #6265, #6121, #21808, #32015, #16805, #29328, #26361, #21317, #16618, #4105 ),
 .UNSPECIFIED., .F., .F.,
 ( 4, 2, 2, 2, 4 ),
 ( 1.968338519012285137E-07, 0.0005467926089500458166, 0.001093388384048190427, 0.001639984159146335146, 0.002186579934244479648 ),
 .UNSPECIFIED. ) ;
#16058=CARTESIAN_POINT ( 'NONE',  ( 6.880159540721329847, -8.414807581959442118, -2.328896285337273664 ) ) ;
#16061=DIRECTION ( 'NONE',  ( 0.000000000000000000, 0.000000000000000000, 1.000000000000000000 ) ) ;
#16066=CARTESIAN_POINT ( 'NONE',  ( -4.700050800000001416, -2.983565686104819648, -0.3135853898029605791 ) ) ;
#16069=DIRECTION ( 'NONE',  ( -1.000000000000000000, 0.000000000000000000, 0.000000000000000000 ) ) ;
#16071=VERTEX_POINT ( 'NONE', #6423 ) ;
#16078=CARTESIAN_POINT ( 'NONE',  ( 6.037141869538513284, -3.843044125430119529, 7.552970526864677403 ) ) ;
#16087=ADVANCED_FACE ( 'NONE', ( #32018 ), #9431, .T. ) ;
#16089=CARTESIAN_POINT ( 'NONE',  ( -6.850050799999999995, 1.549418761218566143, -2.853674364686379583 ) ) ;
#16094=CARTESIAN_POINT ( 'NONE',  ( 7.249760686538667009, 5.064320921489914973, -7.135485519861949122 ) ) ;
#16109=ORIENTED_EDGE ( 'NONE', *, *, #1497, .T. ) ;
#16114=ORIENTED_EDGE ( 'NONE', *, *, #21956, .F. ) ;
#16118=AXIS2_PLACEMENT_3D ( 'NONE', #9406, #11742, #27633 ) ;
#16123=AXIS2_PLACEMENT_3D ( 'NONE', #9328, #20051, #9145 ) ;
#16124=CIRCLE ( 'NONE', #17208, 8.750000000000000000 ) ;
#16132=CARTESIAN_POINT ( 'NONE',  ( 6.038144483126824724, -0.4487862922133833421, 8.463061282283012687 ) ) ;
#16134=CARTESIAN_POINT ( 'NONE',  ( 7.249760686538667009, 8.437262856154195134, -2.318425219014145444 ) ) ;
#16141=CARTESIAN_POINT ( 'NONE',  ( 3.500000000000000000, 7.347880794884119736E-16, -6.000000000000000000 ) ) ;
#16147=LINE ( 'NONE', #5649, #21454 ) ;
#16150=CIRCLE ( 'NONE', #32190, 8.500000000000000000 ) ;
#16152=CARTESIAN_POINT ( 'NONE',  ( -2.812550801365592879, -1.828967928396026510, 3.368539882008728004 ) ) ;
#16153=VERTEX_POINT ( 'NONE', #32866 ) ;
#16154=AXIS2_PLACEMENT_3D ( 'NONE', #5863, #16047, #23766 ) ;
#16156=CARTESIAN_POINT ( 'NONE',  ( -4.900050799999999818, -0.3135853898029607456, 2.983565686104819648 ) ) ;
#16170=AXIS2_PLACEMENT_3D ( 'NONE', #5814, #3506, #30772 ) ;
#16172=DIRECTION ( 'NONE',  ( 0.000000000000000000, 0.9510565162951544194, -0.3090169943749449533 ) ) ;
#16176=CARTESIAN_POINT ( 'NONE',  ( 5.885541615502094537, -8.193643496140865068, 1.821712961073320480 ) ) ;
#16183=CARTESIAN_POINT ( 'NONE',  ( -3.262550801365593056, 0.3701630799359330593, -3.521866450007987037 ) ) ;
#16193=LINE ( 'NONE', #26417, #16732 ) ;
#16197=CARTESIAN_POINT ( 'NONE',  ( 4.749760686538667009, 2.741043480754926875, 7.530955069117522882 ) ) ;
#16198=VECTOR ( 'NONE', #11923, 1000.000000000000000 ) ;
#16199=LINE ( 'NONE', #9481, #26284 ) ;
#16202=CIRCLE ( 'NONE', #5535, 8.750000000000000000 ) ;
#16205=ORIENTED_EDGE ( 'NONE', *, *, #427, .T. ) ;
#16214=CARTESIAN_POINT ( 'NONE',  ( 1.750000000000000222, 4.438567988583182355, -7.249076783337631724 ) ) ;
#16215=ORIENTED_EDGE ( 'NONE', *, *, #7251, .T. ) ;
#16220=CARTESIAN_POINT ( 'NONE',  ( -4.462550801365592790, -0.3701630799359326152, 3.521866450007987037 ) ) ;
#16223=( BOUNDED_SURFACE ( )  B_SPLINE_SURFACE ( 1, 2, ( 
 ( #988, #11168, #21372, #12016, #27879, #25024, #4993, #27701, #14825, #1833, #15176, #7316, #32266, #17667, #9327, #30244, #7168, #25381, #17506, #2138, #4317, #12318, #32757, #19871, #4651, #32575, #22538, #17361, #29737, #9833, #6815, #32419, #20050, #2489, #4807, #22714, #14983, #19540, #27204, #25202, #9986, #14494, #14677, #27554, #12658, #24707, #2325, #19695, #17003, #22210, #9645, #12507, #4503, #9480, #29893, #32917, #7466, #6974, #20197, #30393, #17181, #27392, #24877, #1989, #12162, #22360, #30085, #33063, #5798, #10137, #30753, #30576, #21032, #20849, #31060, #23510, #7825, #142, #20359, #5488, #10489, #20702, #15975, #26198, #18019, #462, #25700, #28206, #5308, #28555, #23020, #18357, #5652, #15486, #8315, #2826, #13002, #23212, #26042, #621, #317, #15832, #18511, #30903, #28057, #3144, #13155, #13302, #10330, #20543, #10817, #15679, #22861, #31240, #7974, #28705, #28372, #3306, #7660, #18167, #17858 ),
 ( #25888, #10642, #5154, #15329, #3002, #25535, #2641, #23355, #8149, #12806, #23989, #11476, #19007, #29341, #29193, #11134, #26850, #31878, #3967, #26529, #6623, #16463, #31540, #16816, #29047, #1297, #8945, #9101, #16320, #21333, #6136, #14137, #21671, #23844, #5957, #24337, #1449, #16638, #32030, #955, #3628, #8624, #18845, #13641, #809, #19152, #13787, #10987, #11626, #13477, #1111, #6433, #21821, #19328, #27015, #29536, #23693, #21189, #11306, #31387, #3485, #21515, #31727, #8801, #8462, #6280, #26670, #3783, #18656, #13952, #28857, #24174, #16156, #26384, #24654, #14791, #30030, #9599, #4616, #27165, #1784, #12464, #27342, #4770, #19823, #2276, #21990, #4462, #6933, #22677, #17132, #11977, #19504, #7427, #22173, #32383, #14444, #12278, #2099, #22492, #14944, #9442, #19660, #14285, #7125, #24836, #1954, #20159, #30358, #29852, #24988, #14636, #12126, #22323, #9789, #4269, #32707, #20010, #32535, #32879, #30205 ),
 ( #17321, #17625, #27515, #7277, #17468, #27667, #4117, #25156, #9946, #24480, #1598, #11787, #32220, #9287, #29697, #6778, #16966, #5438, #20663, #281, #28322, #17817, #15293, #3557, #17981, #28949, #10453, #26458, #12621, #28169, #30716, #13717, #7788, #2602, #10101, #31631, #25495, #12767, #5116, #2965, #10282, #22976, #5271, #31458, #6054, #15445, #882, #23918, #95, #33026, #23769, #18128, #21260, #20504, #25655, #8537, #30868, #27830, #18743, #2776, #1028, #7939, #16245, #4947, #12953, #25343, #23172, #11214, #15632, #25848, #13562, #11060, #22822, #21419, #8719, #15134, #20318, #2452, #30528, #7610, #28020, #16892, #24409, #1691, #1526, #16548, #32309, #4191, #9369, #31955, #12054, #21904, #3876, #22250, #1375, #6703, #14358, #14549, #21748, #26758, #11551, #24567, #24759, #14053, #24074, #11889, #9199, #22097, #29268, #24259, #19579, #11702, #18931, #29776, #9019, #4367, #32122, #6854, #29121, #16738, #16390 ) ),
 .UNSPECIFIED., .F., .F., .F. ) 
 B_SPLINE_SURFACE_WITH_KNOTS ( ( 2, 1, 2 ),
 ( 3, 2, 2, 2, 2, 2, 2, 2, 2, 2, 2, 2, 2, 2, 2, 2, 2, 2, 2, 2, 2, 2, 2, 2, 2, 2, 2, 2, 2, 2, 2, 2, 2, 2, 2, 2, 2, 2, 2, 2, 2, 2, 2, 2, 2, 2, 2, 2, 2, 2, 2, 2, 2, 2, 2, 2, 2, 2, 2, 2, 3 ),
 ( -0.01433874271596183303, 0.000000000000000000, 1.000000000000000000 ),
 ( 0.000000000000000000, 0.01562500000000000000, 0.03125000000000000000, 0.04687500000000000000, 0.06250000000000000000, 0.07812500000000000000, 0.09375000000000000000, 0.1093750000000000000, 0.1250000000000000000, 0.1406250000000000000, 0.1562500000000000000, 0.1718750000000000000, 0.1875000000000000000, 0.2031250000000000000, 0.2187500000000000000, 0.2343750000000000000, 0.2500000000000000000, 0.2656250000000000000, 0.2812500000000000000, 0.2968750000000000000, 0.3125000000000000000, 0.3281250000000000000, 0.3437500000000000000, 0.3593750000000000000, 0.3750000000000000000, 0.3906250000000000000, 0.4062500000000000000, 0.4218750000000000000, 0.4375000000000000000, 0.4531250000000000000, 0.4687500000000000000, 0.4843750000000000000, 0.5000000000000000000, 0.5156250000000000000, 0.5312500000000000000, 0.5468750000000000000, 0.5625000000000000000, 0.5781250000000000000, 0.5937500000000000000, 0.6093750000000000000, 0.6250000000000000000, 0.6406250000000000000, 0.6562500000000000000, 0.6718750000000000000, 0.6875000000000000000, 0.7031250000000000000, 0.7187500000000000000, 0.7343750000000000000, 0.7500000000000000000, 0.7656250000000000000, 0.7812500000000000000, 0.7968750000000000000, 0.8125000000000000000, 0.8281250000000000000, 0.8437500000000000000, 0.8593750000000000000, 0.8750000000000000000, 0.8906250000000000000, 0.9062500000000000000, 0.9218750000000000000, 0.9375000000000000000 ),
 .UNSPECIFIED. ) 
 GEOMETRIC_REPRESENTATION_ITEM ( )  RATIONAL_B_SPLINE_SURFACE ( (
 ( 1.000000000000000000, 0.9238795325112867385, 1.000000000000000000, 0.9238795325112867385, 1.000000000000000000, 0.9238795325112867385, 1.000000000000000000, 0.9238795325112867385, 1.000000000000000000, 0.9238795325112867385, 1.000000000000000000, 0.9238795325112867385, 1.000000000000000000, 0.9238795325112867385, 1.000000000000000000, 0.9238795325112867385, 1.000000000000000000, 0.9238795325112867385, 1.000000000000000000, 0.9238795325112867385, 1.000000000000000000, 0.9238795325112867385, 1.000000000000000000, 0.9238795325112867385, 1.000000000000000000, 0.9238795325112867385, 1.000000000000000000, 0.9238795325112867385, 1.000000000000000000, 0.9238795325112867385, 1.000000000000000000, 0.9238795325112867385, 1.000000000000000000, 0.9238795325112867385, 1.000000000000000000, 0.9238795325112867385, 1.000000000000000000, 0.9238795325112867385, 1.000000000000000000, 0.9238795325112867385, 1.000000000000000000, 0.9238795325112867385, 1.000000000000000000, 0.9238795325112867385, 1.000000000000000000, 0.9238795325112867385, 1.000000000000000000, 0.9238795325112867385, 1.000000000000000000, 0.9238795325112867385, 1.000000000000000000, 0.9238795325112867385, 1.000000000000000000, 0.9238795325112867385, 1.000000000000000000, 0.9238795325112867385, 1.000000000000000000, 0.9238795325112867385, 1.000000000000000000, 0.9238795325112867385, 1.000000000000000000, 0.9238795325112867385, 1.000000000000000000, 0.9238795325112867385, 1.000000000000000000, 0.9238795325112867385, 1.000000000000000000, 0.9238795325112867385, 1.000000000000000000, 0.9238795325112867385, 1.000000000000000000, 0.9238795325112867385, 1.000000000000000000, 0.9238795325112867385, 1.000000000000000000, 0.9238795325112867385, 1.000000000000000000, 0.9238795325112867385, 1.000000000000000000, 0.9238795325112867385, 1.000000000000000000, 0.9238795325112867385, 1.000000000000000000, 0.9238795325112867385, 1.000000000000000000, 0.9238795325112867385, 1.000000000000000000, 0.9238795325112867385, 1.000000000000000000, 0.9238795325112867385, 1.000000000000000000, 0.9238795325112867385, 1.000000000000000000, 0.9238795325112867385, 1.000000000000000000, 0.9238795325112867385, 1.000000000000000000, 0.9238795325112867385, 1.000000000000000000, 0.9238795325112867385, 1.000000000000000000, 0.9238795325112867385, 1.000000000000000000, 0.9238795325112867385, 1.000000000000000000, 0.9238795325112867385, 1.000000000000000000, 0.9238795325112867385, 1.000000000000000000, 0.9238795325112867385, 1.000000000000000000, 0.9238795325112867385, 1.000000000000000000, 0.9238795325112867385, 1.000000000000000000, 0.9238795325112867385, 1.000000000000000000, 0.9238795325112867385, 1.000000000000000000, 0.9238795325112867385, 1.000000000000000000),
 ( 1.000000000000000000, 0.9238795325112867385, 1.000000000000000000, 0.9238795325112867385, 1.000000000000000000, 0.9238795325112867385, 1.000000000000000000, 0.9238795325112867385, 1.000000000000000000, 0.9238795325112867385, 1.000000000000000000, 0.9238795325112867385, 1.000000000000000000, 0.9238795325112867385, 1.000000000000000000, 0.9238795325112867385, 1.000000000000000000, 0.9238795325112867385, 1.000000000000000000, 0.9238795325112867385, 1.000000000000000000, 0.9238795325112867385, 1.000000000000000000, 0.9238795325112867385, 1.000000000000000000, 0.9238795325112867385, 1.000000000000000000, 0.9238795325112867385, 1.000000000000000000, 0.9238795325112867385, 1.000000000000000000, 0.9238795325112867385, 1.000000000000000000, 0.9238795325112867385, 1.000000000000000000, 0.9238795325112867385, 1.000000000000000000, 0.9238795325112867385, 1.000000000000000000, 0.9238795325112867385, 1.000000000000000000, 0.9238795325112867385, 1.000000000000000000, 0.9238795325112867385, 1.000000000000000000, 0.9238795325112867385, 1.000000000000000000, 0.9238795325112867385, 1.000000000000000000, 0.9238795325112867385, 1.000000000000000000, 0.9238795325112867385, 1.000000000000000000, 0.9238795325112867385, 1.000000000000000000, 0.9238795325112867385, 1.000000000000000000, 0.9238795325112867385, 1.000000000000000000, 0.9238795325112867385, 1.000000000000000000, 0.9238795325112867385, 1.000000000000000000, 0.9238795325112867385, 1.000000000000000000, 0.9238795325112867385, 1.000000000000000000, 0.9238795325112867385, 1.000000000000000000, 0.9238795325112867385, 1.000000000000000000, 0.9238795325112867385, 1.000000000000000000, 0.9238795325112867385, 1.000000000000000000, 0.9238795325112867385, 1.000000000000000000, 0.9238795325112867385, 1.000000000000000000, 0.9238795325112867385, 1.000000000000000000, 0.9238795325112867385, 1.000000000000000000, 0.9238795325112867385, 1.000000000000000000, 0.9238795325112867385, 1.000000000000000000, 0.9238795325112867385, 1.000000000000000000, 0.9238795325112867385, 1.000000000000000000, 0.9238795325112867385, 1.000000000000000000, 0.9238795325112867385, 1.000000000000000000, 0.9238795325112867385, 1.000000000000000000, 0.9238795325112867385, 1.000000000000000000, 0.9238795325112867385, 1.000000000000000000, 0.9238795325112867385, 1.000000000000000000, 0.9238795325112867385, 1.000000000000000000, 0.9238795325112867385, 1.000000000000000000, 0.9238795325112867385, 1.000000000000000000, 0.9238795325112867385, 1.000000000000000000, 0.9238795325112867385, 1.000000000000000000, 0.9238795325112867385, 1.000000000000000000, 0.9238795325112867385, 1.000000000000000000, 0.9238795325112867385, 1.000000000000000000, 0.9238795325112867385, 1.000000000000000000),
 ( 1.000000000000000000, 0.9238795325112867385, 1.000000000000000000, 0.9238795325112867385, 1.000000000000000000, 0.9238795325112867385, 1.000000000000000000, 0.9238795325112867385, 1.000000000000000000, 0.9238795325112867385, 1.000000000000000000, 0.9238795325112867385, 1.000000000000000000, 0.9238795325112867385, 1.000000000000000000, 0.9238795325112867385, 1.000000000000000000, 0.9238795325112867385, 1.000000000000000000, 0.9238795325112867385, 1.000000000000000000, 0.9238795325112867385, 1.000000000000000000, 0.9238795325112867385, 1.000000000000000000, 0.9238795325112867385, 1.000000000000000000, 0.9238795325112867385, 1.000000000000000000, 0.9238795325112867385, 1.000000000000000000, 0.9238795325112867385, 1.000000000000000000, 0.9238795325112867385, 1.000000000000000000, 0.9238795325112867385, 1.000000000000000000, 0.9238795325112867385, 1.000000000000000000, 0.9238795325112867385, 1.000000000000000000, 0.9238795325112867385, 1.000000000000000000, 0.9238795325112867385, 1.000000000000000000, 0.9238795325112867385, 1.000000000000000000, 0.9238795325112867385, 1.000000000000000000, 0.9238795325112867385, 1.000000000000000000, 0.9238795325112867385, 1.000000000000000000, 0.9238795325112867385, 1.000000000000000000, 0.9238795325112867385, 1.000000000000000000, 0.9238795325112867385, 1.000000000000000000, 0.9238795325112867385, 1.000000000000000000, 0.9238795325112867385, 1.000000000000000000, 0.9238795325112867385, 1.000000000000000000, 0.9238795325112867385, 1.000000000000000000, 0.9238795325112867385, 1.000000000000000000, 0.9238795325112867385, 1.000000000000000000, 0.9238795325112867385, 1.000000000000000000, 0.9238795325112867385, 1.000000000000000000, 0.9238795325112867385, 1.000000000000000000, 0.9238795325112867385, 1.000000000000000000, 0.9238795325112867385, 1.000000000000000000, 0.9238795325112867385, 1.000000000000000000, 0.9238795325112867385, 1.000000000000000000, 0.9238795325112867385, 1.000000000000000000, 0.9238795325112867385, 1.000000000000000000, 0.9238795325112867385, 1.000000000000000000, 0.9238795325112867385, 1.000000000000000000, 0.9238795325112867385, 1.000000000000000000, 0.9238795325112867385, 1.000000000000000000, 0.9238795325112867385, 1.000000000000000000, 0.9238795325112867385, 1.000000000000000000, 0.9238795325112867385, 1.000000000000000000, 0.9238795325112867385, 1.000000000000000000, 0.9238795325112867385, 1.000000000000000000, 0.9238795325112867385, 1.000000000000000000, 0.9238795325112867385, 1.000000000000000000, 0.9238795325112867385, 1.000000000000000000, 0.9238795325112867385, 1.000000000000000000, 0.9238795325112867385, 1.000000000000000000, 0.9238795325112867385, 1.000000000000000000, 0.9238795325112867385, 1.000000000000000000) ) ) 
 REPRESENTATION_ITEM ( '' )  SURFACE ( )  );
#16228=CARTESIAN_POINT ( 'NONE',  ( -7.587550801365593678, -3.521866450007987037, -0.3701630799359323931 ) ) ;
#16231=DIRECTION ( 'NONE',  ( -1.000000000000000000, 0.000000000000000000, -0.000000000000000000 ) ) ;
#16232=EDGE_CURVE ( 'NONE', #12355, #25433, #4205, .T. ) ;
#16245=CARTESIAN_POINT ( 'NONE',  ( -5.087550801365593678, -2.228590825266444586, -2.752080473201636401 ) ) ;
#16247=AXIS2_PLACEMENT_3D ( 'NONE', #14128, #32206, #8613 ) ;
#16248=DIRECTION ( 'NONE',  ( 1.000000000000000000, -0.000000000000000000, -0.000000000000000000 ) ) ;
#16250=CARTESIAN_POINT ( 'NONE',  ( 0.000000000000000000, 1.106368468154430129, 8.427689411260576691 ) ) ;
#16253=CARTESIAN_POINT ( 'NONE',  ( -4.650050800000000706, -2.853674364686378695, -1.549418761218566809 ) ) ;
#16257=ORIENTED_EDGE ( 'NONE', *, *, #8759, .F. ) ;
#16261=ADVANCED_FACE ( 'NONE', ( #17456 ), #17614, .F. ) ;
#16277=DIRECTION ( 'NONE',  ( -0.000000000000000000, 1.000000000000000000, 1.224646799147353207E-16 ) ) ;
#16281=EDGE_CURVE ( 'NONE', #1567, #32424, #16594, .T. ) ;
#16287=VERTEX_POINT ( 'NONE', #10937 ) ;
#16289=CARTESIAN_POINT ( 'NONE',  ( 5.377543748152549874, 2.741043480755029016, -7.530955069117485579 ) ) ;
#16300=CARTESIAN_POINT ( 'NONE',  ( 7.249760686538667009, -2.789499415801756586E-14, 8.014274990069656823 ) ) ;
#16301=DIRECTION ( 'NONE',  ( -1.000000000000000000, 0.000000000000000000, 0.000000000000000000 ) ) ;
#16304=EDGE_CURVE ( 'NONE', #19070, #20542, #26898, .T. ) ;
#16310=LINE ( 'NONE', #32021, #1861 ) ;
#16317=CARTESIAN_POINT ( 'NONE',  ( -3.962550801365593234, 2.752080473201636845, -2.228590825266444142 ) ) ;
#16320=CARTESIAN_POINT ( 'NONE',  ( -7.100050799999999995, -2.983565686104819648, -0.3135853898029605791 ) ) ;
#16321=B_SPLINE_CURVE_WITH_KNOTS ( 'NONE', 3,
 ( #14121, #15959, #1433, #23668, #11609, #21804, #789, #32011, #5782, #27651 ),
 .UNSPECIFIED., .F., .F.,
 ( 4, 2, 2, 2, 4 ),
 ( 3.032460776716650747E-07, 0.0005479053915603972853, 0.001095507537043122767, 0.001643109682525848358, 0.002190711828008574166 ),
 .UNSPECIFIED. ) ;
#16322=LINE ( 'NONE', #21336, #19949 ) ;
#16325=VERTEX_POINT ( 'NONE', #24399 ) ;
#16327=VERTEX_POINT ( 'NONE', #25993 ) ;
#16340=DIRECTION ( 'NONE',  ( -1.000000000000000000, -0.000000000000000000, -0.000000000000000000 ) ) ;
#16342=CARTESIAN_POINT ( 'NONE',  ( -4.262550801365594388, -3.521866450007987037, -0.3701630799359323931 ) ) ;
#16344=DIRECTION ( 'NONE',  ( -1.000000000000000000, 0.000000000000000000, 0.000000000000000000 ) ) ;
#16345=VERTEX_POINT ( 'NONE', #18463 ) ;
#16351=DIRECTION ( 'NONE',  ( -1.000000000000000000, 0.000000000000000000, 0.000000000000000000 ) ) ;
#16352=VERTEX_POINT ( 'NONE', #25832 ) ;
#16357=CARTESIAN_POINT ( 'NONE',  ( -2.887550801365593500, -2.752080473201636845, 2.228590825266444586 ) ) ;
#16360=ORIENTED_EDGE ( 'NONE', *, *, #25747, .T. ) ;
#16362=VERTEX_POINT ( 'NONE', #31338 ) ;
#16365=ADVANCED_FACE ( 'NONE', ( #8417 ), #18610, .F. ) ;
#16368=FACE_OUTER_BOUND ( 'NONE', #20509, .T. ) ;
#16370=EDGE_LOOP ( 'NONE', ( #17418, #16114, #24538, #22717 ) ) ;
#16371=LINE ( 'NONE', #8515, #7508 ) ;
#16372=CARTESIAN_POINT ( 'NONE',  ( -5.962550801365593678, -2.752080473201636845, 2.228590825266444586 ) ) ;
#16375=CARTESIAN_POINT ( 'NONE',  ( 3.499999999999999556, -6.200809695932780308, 0.7745709230444962623 ) ) ;
#16377=CARTESIAN_POINT ( 'NONE',  ( -6.787550801365593856, -3.521866450007987037, -0.3701630799359323931 ) ) ;
#16390=CARTESIAN_POINT ( 'NONE',  ( -2.187550801365593767, -0.3701630799359326152, 3.521866450007987037 ) ) ;
#16393=DIRECTION ( 'NONE',  ( -0.000000000000000000, 0.2588190451025172423, 0.9659258262890692004 ) ) ;
#16395=CARTESIAN_POINT ( 'NONE',  ( 5.377543748152548098, -6.940565734314625423, 4.007137495034787555 ) ) ;
#16397=VERTEX_POINT ( 'NONE', #22744 ) ;
#16400=CARTESIAN_POINT ( 'NONE',  ( 0.000000000000000000, 3.771202944355708020, 4.982773259188384429 ) ) ;
#16401=ORIENTED_EDGE ( 'NONE', *, *, #1944, .F. ) ;
#16410=ORIENTED_EDGE ( 'NONE', *, *, #9879, .F. ) ;
#16416=CARTESIAN_POINT ( 'NONE',  ( -3.007304909706596696, -1.062355717592093463, -3.000000000000000888 ) ) ;
#16421=CARTESIAN_POINT ( 'NONE',  ( 0.000000000000000000, 6.704570150427012543, -2.172265885002588437 ) ) ;
#16422=ORIENTED_EDGE ( 'NONE', *, *, #17575, .F. ) ;
#16423=CARTESIAN_POINT ( 'NONE',  ( -6.200050800000000528, -1.887961173149512062, -2.331437884370912261 ) ) ;
#16427=CARTESIAN_POINT ( 'NONE',  ( 0.000000000000000000, 0.000000000000000000, 0.000000000000000000 ) ) ;
#16429=ORIENTED_EDGE ( 'NONE', *, *, #1022, .F. ) ;
#16430=CARTESIAN_POINT ( 'NONE',  ( 5.612974441954677651, 6.420536856480007160, -5.126870824538697136 ) ) ;
#16433=EDGE_CURVE ( 'NONE', #31391, #9461, #30517, .T. ) ;
#16440=EDGE_LOOP ( 'NONE', ( #5821, #27621, #18447 ) ) ;
#16442=VERTEX_POINT ( 'NONE', #17031 ) ;
#16452=DIRECTION ( 'NONE',  ( 0.000000000000000000, 0.4067366430758009299, -0.9135454576426005335 ) ) ;
#16455=CARTESIAN_POINT ( 'NONE',  ( 6.883866557622098092, 7.943335131955005401, 3.625395379390111916 ) ) ;
#16461=CARTESIAN_POINT ( 'NONE',  ( -7.300050802731188782, -1.549418761218565477, 2.853674364686380471 ) ) ;
#16463=CARTESIAN_POINT ( 'NONE',  ( -7.450050800000001416, 2.853674364686379583, 1.549418761218565921 ) ) ;
#16466=EDGE_CURVE ( 'NONE', #10433, #32858, #20885, .T. ) ;
#16470=CARTESIAN_POINT ( 'NONE',  ( -7.150050800000000706, -3.113457007523259268, 0.9222479816126455399 ) ) ;
#16472=EDGE_LOOP ( 'NONE', ( #20126, #30173, #30274 ) ) ;
#16481=CARTESIAN_POINT ( 'NONE',  ( 7.249760686538667009, -2.741043480754977946, 7.530955069117504230 ) ) ;
#16483=ADVANCED_FACE ( 'NONE', ( #9683 ), #32608, .T. ) ;
#16487=EDGE_CURVE ( 'NONE', #19582, #29588, #24608, .T. ) ;
#16488=CARTESIAN_POINT ( 'NONE',  ( 4.749760686538667009, -7.892520144992426268, -1.391664247347309535 ) ) ;
#16493=LINE ( 'NONE', #19366, #11964 ) ;
#16494=EDGE_CURVE ( 'NONE', #23747, #10694, #25566, .T. ) ;
#16495=CARTESIAN_POINT ( 'NONE',  ( 7.249760686538667009, 7.892520144992453801, -1.391664247347147443 ) ) ;
#16496=DIRECTION ( 'NONE',  ( -1.000000000000000000, 0.000000000000000000, 0.000000000000000000 ) ) ;
#16498=ORIENTED_EDGE ( 'NONE', *, *, #25504, .T. ) ;
#16501=ORIENTED_EDGE ( 'NONE', *, *, #31484, .T. ) ;
#16505=CARTESIAN_POINT ( 'NONE',  ( -3.737550801365593589, -1.828967928396026732, 3.368539882008728004 ) ) ;
#16506=EDGE_CURVE ( 'NONE', #292, #29424, #14992, .T. ) ;
#16509=DIRECTION ( 'NONE',  ( 0.000000000000000000, 0.000000000000000000, 1.000000000000000000 ) ) ;
#16518=ORIENTED_EDGE ( 'NONE', *, *, #3103, .T. ) ;
#16523=CARTESIAN_POINT ( 'NONE',  ( -4.612550801365594921, 3.368539882008727115, 1.828967928396027176 ) ) ;
#16527=AXIS2_PLACEMENT_3D ( 'NONE', #12395, #9394, #17422 ) ;
#16529=DIRECTION ( 'NONE',  ( 0.000000000000000000, 0.9510565162951544194, -0.3090169943749448977 ) ) ;
#16530=EDGE_LOOP ( 'NONE', ( #15405, #6945, #32548, #6023 ) ) ;
#16531=CARTESIAN_POINT ( 'NONE',  ( -6.337550801365593678, 3.368539882008727115, 1.828967928396026954 ) ) ;
#16537=VERTEX_POINT ( 'NONE', #28086 ) ;
#16548=CARTESIAN_POINT ( 'NONE',  ( -3.937550801365593323, 3.368539882008727115, 1.828967928396026954 ) ) ;
#16557=CARTESIAN_POINT ( 'NONE',  ( 7.249760686538667009, -7.530955069117495349, -2.741043480755002371 ) ) ;
#16558=VERTEX_POINT ( 'NONE', #26068 ) ;
#16565=VECTOR ( 'NONE', #18672, 1000.000000000000000 ) ;
#16566=EDGE_CURVE ( 'NONE', #26528, #23643, #2522, .T. ) ;
#16573=CARTESIAN_POINT ( 'NONE',  ( 3.499999999999999556, -6.700937042937042065, 0.8165525598867410251 ) ) ;
#16578=CARTESIAN_POINT ( 'NONE',  ( 7.064423637759001728, 3.647351267792902529, 7.953573330858847434 ) ) ;
#16584=CARTESIAN_POINT ( 'NONE',  ( -3.306376978575949366, -0.1572233378491262878, 2.999999999999999556 ) ) ;
#16586=ORIENTED_EDGE ( 'NONE', *, *, #12186, .F. ) ;
#16590=CIRCLE ( 'NONE', #29421, 8.750000000000000000 ) ;
#16592=DIRECTION ( 'NONE',  ( -1.000000000000000000, 0.000000000000000000, 0.000000000000000000 ) ) ;
#16594=CIRCLE ( 'NONE', #13935, 6.248999999999998778 ) ;
#16605=DIRECTION ( 'NONE',  ( -1.000000000000000000, 0.000000000000000000, 0.000000000000000000 ) ) ;
#16611=CARTESIAN_POINT ( 'NONE',  ( 5.887530024394193262, -7.753515897409866575, -3.218326717262334657 ) ) ;
#16618=CARTESIAN_POINT ( 'NONE',  ( 5.489321708267612898, 5.138670926724898003, 6.285661071314490478 ) ) ;
#16622=VECTOR ( 'NONE', #14472, 1000.000000000000227 ) ;
#16627=AXIS2_PLACEMENT_3D ( 'NONE', #10431, #18106, #25822 ) ;
#16633=DIRECTION ( 'NONE',  ( 0.000000000000000000, 0.4067366430758010964, -0.9135454576426006446 ) ) ;
#16635=CARTESIAN_POINT ( 'NONE',  ( 3.499999999999999556, 2.429606751577119805, -5.757344182232886354 ) ) ;
#16636=CARTESIAN_POINT ( 'NONE',  ( -6.750050802731187183, 2.983565686104819648, 0.3135853898029609677 ) ) ;
#16638=CARTESIAN_POINT ( 'NONE',  ( -6.650050800000002482, 2.853674364686379583, 1.549418761218565921 ) ) ;
#16640=CARTESIAN_POINT ( 'NONE',  ( -5.600050802731187716, -3.113457007523259268, 0.9222479816126455399 ) ) ;
#16642=ORIENTED_EDGE ( 'NONE', *, *, #1222, .F. ) ;
#16644=AXIS2_PLACEMENT_3D ( 'NONE', #13149, #20190, #27869 ) ;
#16647=ORIENTED_EDGE ( 'NONE', *, *, #2015, .T. ) ;
#16651=ORIENTED_EDGE ( 'NONE', *, *, #32867, .T. ) ;
#16663=EDGE_CURVE ( 'NONE', #14221, #11829, #3999, .T. ) ;
#16664=FACE_OUTER_BOUND ( 'NONE', #32894, .T. ) ;
#16667=CARTESIAN_POINT ( 'NONE',  ( 7.064632816082964339, -8.721381771256204729, -0.7071067811865412445 ) ) ;
#16676=CARTESIAN_POINT ( 'NONE',  ( 7.249760686538667009, -5.151476664237435443, -6.139290821770307716 ) ) ;
#16677=DIRECTION ( 'NONE',  ( 0.000000000000000000, -0.5877852522924799095, 0.8090169943749425663 ) ) ;
#16694=VECTOR ( 'NONE', #7449, 1000.000000000000000 ) ;
#16697=CIRCLE ( 'NONE', #31660, 2.999999999999999112 ) ;
#16703=CARTESIAN_POINT ( 'NONE',  ( -3.362942409646513031, -5.022711880624455567E-15, 2.999999999999999556 ) ) ;
#16710=CARTESIAN_POINT ( 'NONE',  ( -2.462550801365593678, 0.3701630799359330593, -3.521866450007987037 ) ) ;
#16715=CARTESIAN_POINT ( 'NONE',  ( -6.937550801365595099, -1.828967928396026510, 3.368539882008728004 ) ) ;
#16721=CARTESIAN_POINT ( 'NONE',  ( 4.749760686538667009, 5.151476664237477188, 6.139290821770273077 ) ) ;
#16732=VECTOR ( 'NONE', #26069, 1000.000000000000000 ) ;
#16733=CARTESIAN_POINT ( 'NONE',  ( -6.350050802731187716, -2.983565686104819648, -0.3135853898029605791 ) ) ;
#16738=CARTESIAN_POINT ( 'NONE',  ( -2.237550801365593589, 1.088641768524161613, 3.675193018007247403 ) ) ;
#16742=DIRECTION ( 'NONE',  ( 0.000000000000000000, 0.000000000000000000, 1.000000000000000000 ) ) ;
#16744=CARTESIAN_POINT ( 'NONE',  ( 6.880159790065804692, -2.190520500543428728, -8.451885315426448386 ) ) ;
#16747=VECTOR ( 'NONE', #8046, 1000.000000000000114 ) ;
#16750=VERTEX_POINT ( 'NONE', #28729 ) ;
#16753=ORIENTED_EDGE ( 'NONE', *, *, #8346, .T. ) ;
#16756=ADVANCED_FACE ( 'NONE', ( #16003 ), #31413, .T. ) ;
#16764=ADVANCED_FACE ( 'NONE', ( #19185 ), #24209, .T. ) ;
#16769=EDGE_CURVE ( 'NONE', #9461, #2248, #6309, .T. ) ;
#16776=VERTEX_POINT ( 'NONE', #8975 ) ;
#16785=DIRECTION ( 'NONE',  ( 0.000000000000000000, 0.000000000000000000, -1.000000000000000000 ) ) ;
#16787=ORIENTED_EDGE ( 'NONE', *, *, #25321, .T. ) ;
#16788=DIRECTION ( 'NONE',  ( -0.000000000000000000, -0.2588190451025240701, -0.9659258262890673130 ) ) ;
#16790=EDGE_LOOP ( 'NONE', ( #20371, #2664, #11069 ) ) ;
#16791=CARTESIAN_POINT ( 'NONE',  ( 7.064632918400240769, 3.647351267791677731, -7.953573330858177748 ) ) ;
#16792=CARTESIAN_POINT ( 'NONE',  ( 6.038144853276843804, -8.412419482080416344, 1.027626812407973267 ) ) ;
#16803=CARTESIAN_POINT ( 'NONE',  ( 7.249760686538667009, 0.000000000000000000, 0.000000000000000000 ) ) ;
#16805=CARTESIAN_POINT ( 'NONE',  ( 6.357668022120090079, 5.080751859797355330, 6.947679035623472998 ) ) ;
#16809=CARTESIAN_POINT ( 'NONE',  ( 7.249760686538667009, -2.741043480754977946, 7.530955069117504230 ) ) ;
#16813=EDGE_CURVE ( 'NONE', #1604, #23747, #23058, .T. ) ;
#16814=CARTESIAN_POINT ( 'NONE',  ( -5.650050802731187538, -2.331437884370912705, 1.887961173149512062 ) ) ;
#16815=ORIENTED_EDGE ( 'NONE', *, *, #28587, .F. ) ;
#16816=CARTESIAN_POINT ( 'NONE',  ( -7.350050800000000883, 0.9222479816126443186, 3.113457007523260156 ) ) ;
#16822=ORIENTED_EDGE ( 'NONE', *, *, #31521, .F. ) ;
#16825=ORIENTED_EDGE ( 'NONE', *, *, #3599, .T. ) ;
#16828=EDGE_CURVE ( 'NONE', #14119, #6329, #27197, .T. ) ;
#16833=( BOUNDED_CURVE ( )  B_SPLINE_CURVE ( 1, ( #14277, #27157 ),
 .UNSPECIFIED., .F., .F. ) 
 B_SPLINE_CURVE_WITH_KNOTS ( ( 2, 2 ),
 ( 0.000000000000000000, 1.000000000000000000 ),
 .UNSPECIFIED. ) 
 CURVE ( )  GEOMETRIC_REPRESENTATION_ITEM ( )  RATIONAL_B_SPLINE_CURVE ( ( 0.9641176721898547797, 0.9641176721898547797 ) ) 
 REPRESENTATION_ITEM ( '' )  );
#16834=EDGE_CURVE ( 'NONE', #4959, #6174, #11826, .T. ) ;
#16839=DIRECTION ( 'NONE',  ( 0.000000000000000000, 0.000000000000000000, 1.000000000000000000 ) ) ;
#16840=VERTEX_POINT ( 'NONE', #6809 ) ;
#16841=CARTESIAN_POINT ( 'NONE',  ( 7.249760686538667009, -8.721381771256204729, -0.7071067811865429098 ) ) ;
#16846=DIRECTION ( 'NONE',  ( 0.000000000000000000, 0.000000000000000000, -1.000000000000000000 ) ) ;
#16855=LINE ( 'NONE', #6975, #6072 ) ;
#16856=CARTESIAN_POINT ( 'NONE',  ( 3.499999999999999556, -6.700937042937072263, 2.183447440113167826 ) ) ;
#16861=EDGE_CURVE ( 'NONE', #25021, #9041, #8989, .T. ) ;
#16867=CARTESIAN_POINT ( 'NONE',  ( 5.885541838704151374, 6.185046950422397494, -5.674471607902377812 ) ) ;
#16868=ORIENTED_EDGE ( 'NONE', *, *, #18613, .F. ) ;
#16875=ORIENTED_EDGE ( 'NONE', *, *, #7288, .F. ) ;
#16876=CARTESIAN_POINT ( 'NONE',  ( -3.987550801365593145, 3.521866450007987037, 0.3701630799359328372 ) ) ;
#16892=CARTESIAN_POINT ( 'NONE',  ( -4.137550801365594388, 1.828967928396027176, -3.368539882008727115 ) ) ;
#16898=EDGE_CURVE ( 'NONE', #28422, #28176, #24364, .T. ) ;
#16900=DIRECTION ( 'NONE',  ( 0.000000000000000000, -0.08715574274766567375, 0.9961946980917449901 ) ) ;
#16911=CARTESIAN_POINT ( 'NONE',  ( 6.038145268433179780, 5.783741681378160138, -6.194606843114025096 ) ) ;
#16914=ORIENTED_EDGE ( 'NONE', *, *, #28428, .T. ) ;
#16920=EDGE_LOOP ( 'NONE', ( #26095, #26087, #27314 ) ) ;
#16922=EDGE_CURVE ( 'NONE', #33081, #33059, #20043, .T. ) ;
#16924=CARTESIAN_POINT ( 'NONE',  ( 4.749760686538667009, 7.892520144992435149, 1.391664247347255134 ) ) ;
#16925=DIRECTION ( 'NONE',  ( 0.000000000000000000, -0.7071067811865516806, 0.7071067811865434649 ) ) ;
#16930=CARTESIAN_POINT ( 'NONE',  ( 3.499999999999999556, -6.106419733534973027, -3.518755179752868223 ) ) ;
#16939=ORIENTED_EDGE ( 'NONE', *, *, #32177, .F. ) ;
#16942=CYLINDRICAL_SURFACE ( 'NONE', #27200, 8.500000000000000000 ) ;
#16946=EDGE_CURVE ( 'NONE', #8809, #15458, #31096, .T. ) ;
#16949=CARTESIAN_POINT ( 'NONE',  ( 6.038145077921538650, -7.799182446117172596, -3.316258947000939816 ) ) ;
#16952=CARTESIAN_POINT ( 'NONE',  ( 5.612974259723590542, -7.786824029658784063, 2.621729824970357114 ) ) ;
#16953=CARTESIAN_POINT ( 'NONE',  ( 3.499999999999999556, 6.704570150426983233, 5.172265885002680363 ) ) ;
#16956=EDGE_CURVE ( 'NONE', #12143, #15684, #2790, .T. ) ;
#16961=DIRECTION ( 'NONE',  ( -1.000000000000000000, 0.000000000000000000, -0.000000000000000000 ) ) ;
#16963=DIRECTION ( 'NONE',  ( 1.000000000000000000, -0.000000000000000000, -0.000000000000000000 ) ) ;
#16964=CARTESIAN_POINT ( 'NONE',  ( -4.800050802731187005, -3.113457007523259268, 0.9222479816126455399 ) ) ;
#16966=CARTESIAN_POINT ( 'NONE',  ( -7.387550801365593500, 0.3701630799359330593, -3.521866450007987037 ) ) ;
#16969=DIRECTION ( 'NONE',  ( 0.000000000000000000, -0.9961946980917453232, 0.08715574274766135776 ) ) ;
#16977=CARTESIAN_POINT ( 'NONE',  ( -2.512942406915326110, -5.022711880624455567E-15, 2.999999999999999556 ) ) ;
#16978=ORIENTED_EDGE ( 'NONE', *, *, #3036, .F. ) ;
#16983=DIRECTION ( 'NONE',  ( 0.000000000000000000, -0.9063077870366542665, 0.4226182617406900599 ) ) ;
#16996=CARTESIAN_POINT ( 'NONE',  ( 7.249760686538667009, -6.226446564517873483, -6.147671362329282019 ) ) ;
#16998=FACE_OUTER_BOUND ( 'NONE', #25463, .T. ) ;
#17003=CARTESIAN_POINT ( 'NONE',  ( -6.104531657079157014, 0.3127741368606810068, -2.975847129947406522 ) ) ;
#17006=CARTESIAN_POINT ( 'NONE',  ( -8.000050800000000351, 0.3701630799359330593, -3.521866450007987037 ) ) ;
#17009=ORIENTED_EDGE ( 'NONE', *, *, #20097, .T. ) ;
#17010=FACE_OUTER_BOUND ( 'NONE', #16001, .T. ) ;
#17017=ORIENTED_EDGE ( 'NONE', *, *, #16566, .T. ) ;
#17018=CARTESIAN_POINT ( 'NONE',  ( 6.530491751506348308, 6.216163082443066479, 6.030130624359195224 ) ) ;
#17019=CARTESIAN_POINT ( 'NONE',  ( -2.262550801365593056, 3.521866450007987037, 0.3701630799359328372 ) ) ;
#17024=CARTESIAN_POINT ( 'NONE',  ( -3.787550801365593411, -0.3701630799359326152, 3.521866450007987037 ) ) ;
#17026=DIRECTION ( 'NONE',  ( 0.000000000000000000, -0.7431448254773863615, -0.6691306063588671194 ) ) ;
#17029=CARTESIAN_POINT ( 'NONE',  ( 4.749760686538667009, -6.139290821770289064, 5.151476664237455871 ) ) ;
#17031=CARTESIAN_POINT ( 'NONE',  ( 7.249760686538667009, -7.530955069117495349, -2.741043480755002371 ) ) ;
#17032=CARTESIAN_POINT ( 'NONE',  ( 7.064632879756604034, 8.466096581343480310, 2.210816291636240383 ) ) ;
#17048=DIRECTION ( 'NONE',  ( -0.000000000000000000, -0.4226182617407029940, -0.9063077870366482713 ) ) ;
#17051=VECTOR ( 'NONE', #26136, 1000.000000000000000 ) ;
#17058=ORIENTED_EDGE ( 'NONE', *, *, #11940, .T. ) ;
#17073=CARTESIAN_POINT ( 'NONE',  ( 5.377543748152549874, -2.741043480754877582, -7.530955069117540646 ) ) ;
#17075=EDGE_CURVE ( 'NONE', #11908, #516, #21146, .T. ) ;
#17078=DIRECTION ( 'NONE',  ( 0.000000000000000000, 0.000000000000000000, -1.000000000000000000 ) ) ;
#17080=( BOUNDED_CURVE ( )  B_SPLINE_CURVE ( 2, ( #17557, #10199, #15731, #5201, #2695, #12865, #10535, #23088, #506, #2384, #20746 ),
 .UNSPECIFIED., .F., .F. ) 
 B_SPLINE_CURVE_WITH_KNOTS ( ( 3, 2, 2, 2, 2, 3 ),
 ( 0.3728822619934377136, 0.3750000000000000000, 0.3906250000000000000, 0.4062500000000000000, 0.4218750000000000000, 0.4353822619934377136 ),
 .UNSPECIFIED. ) 
 CURVE ( )  GEOMETRIC_REPRESENTATION_ITEM ( )  RATIONAL_B_SPLINE_CURVE ( ( 0.9821626249036857770, 0.9896829947469991673, 1.000000000000000000, 0.9238795325112867385, 1.000000000000000000, 0.9238795325112867385, 1.000000000000000000, 0.9238795325112867385, 1.000000000000000000, 0.9341965377642874602, 0.9821626249036857770 ) ) 
 REPRESENTATION_ITEM ( '' )  );
#17082=CARTESIAN_POINT ( 'NONE',  ( 3.499999999999999556, 2.429606751577043422, 5.757344182232919216 ) ) ;
#17086=ORIENTED_EDGE ( 'NONE', *, *, #23776, .T. ) ;
#17089=AXIS2_PLACEMENT_3D ( 'NONE', #157, #10346, #20558 ) ;
#17096=ORIENTED_EDGE ( 'NONE', *, *, #16466, .T. ) ;
#17097=CARTESIAN_POINT ( 'NONE',  ( 7.249760686538667009, 4.007137495034812424, 6.940565734314612101 ) ) ;
#17099=CARTESIAN_POINT ( 'NONE',  ( 6.357667697713671018, -8.557242355892494601, 0.9262207444595624839 ) ) ;
#17101=EDGE_CURVE ( 'NONE', #12129, #10411, #24165, .T. ) ;
#17115=CIRCLE ( 'NONE', #5396, 2.999999999999999556 ) ;
#17117=DIRECTION ( 'NONE',  ( -1.000000000000000000, 0.000000000000000000, -0.000000000000000000 ) ) ;
#17124=LINE ( 'NONE', #16809, #2197 ) ;
#17130=CARTESIAN_POINT ( 'NONE',  ( -6.500050802731188959, -1.549418761218565477, 2.853674364686380471 ) ) ;
#17132=CARTESIAN_POINT ( 'NONE',  ( -4.000050800000000351, -2.331437884370912705, 1.887961173149512062 ) ) ;
#17133=AXIS2_PLACEMENT_3D ( 'NONE', #3185, #23080, #13347 ) ;
#17135=CARTESIAN_POINT ( 'NONE',  ( -3.950050802731187360, -2.983565686104819648, -0.3135853898029605791 ) ) ;
#17139=EDGE_CURVE ( 'NONE', #26968, #5714, #19311, .T. ) ;
#17144=CARTESIAN_POINT ( 'NONE',  ( 5.489344087273876127, 5.297876218488320355, 6.152099123112469314 ) ) ;
#17146=ORIENTED_EDGE ( 'NONE', *, *, #2015, .F. ) ;
#17153=AXIS2_PLACEMENT_3D ( 'NONE', #18606, #14234, #13586 ) ;
#17155=ORIENTED_EDGE ( 'NONE', *, *, #29211, .F. ) ;
#17160=AXIS2_PLACEMENT_3D ( 'NONE', #11984, #4622, #4470 ) ;
#17172=CARTESIAN_POINT ( 'NONE',  ( 6.038145268433180668, -6.194606843114042860, -5.783741681378140598 ) ) ;
#17173=CARTESIAN_POINT ( 'NONE',  ( -2.512942406915326110, -5.022711880624455567E-15, 2.999999999999999556 ) ) ;
#17174=CARTESIAN_POINT ( 'NONE',  ( 6.749760686538667009, 0.000000000000000000, 5.000000000000000000 ) ) ;
#17177=CARTESIAN_POINT ( 'NONE',  ( 5.489321606599602887, 2.678948506461329426, 7.664118171219008069 ) ) ;
#17181=CARTESIAN_POINT ( 'NONE',  ( -5.504531657079157370, -2.975847129947406522, -0.3127741368606805072 ) ) ;
#17188=VERTEX_POINT ( 'NONE', #3621 ) ;
#17199=CARTESIAN_POINT ( 'NONE',  ( 5.489344046532321109, 7.082516960462315048, 3.969101778623947308 ) ) ;
#17206=CARTESIAN_POINT ( 'NONE',  ( 7.064423659272769385, -7.906491560605053870, -3.748318449931996810 ) ) ;
#17208=AXIS2_PLACEMENT_3D ( 'NONE', #5430, #8092, #28991 ) ;
#17210=VECTOR ( 'NONE', #21508, 1000.000000000000000 ) ;
#17214=CARTESIAN_POINT ( 'NONE',  ( -3.687550801365593323, -2.752080473201636845, 2.228590825266444586 ) ) ;
#17215=DIRECTION ( 'NONE',  ( -1.000000000000000000, 0.000000000000000000, 0.000000000000000000 ) ) ;
#17216=ADVANCED_FACE ( 'NONE', ( #14630 ), #27509, .T. ) ;
#17219=CARTESIAN_POINT ( 'NONE',  ( 7.249760686538667009, -2.741043480754877582, -7.530955069117540646 ) ) ;
#17221=ORIENTED_EDGE ( 'NONE', *, *, #28804, .F. ) ;
#17239=LINE ( 'NONE', #12203, #13966 ) ;
#17240=ORIENTED_EDGE ( 'NONE', *, *, #30553, .F. ) ;
#17242=TOROIDAL_SURFACE ( 'NONE', #2855, 6.000000000000000000, 2.750000000000000444 ) ;
#17254=EDGE_CURVE ( 'NONE', #19445, #15207, #24112, .T. ) ;
#17273=CARTESIAN_POINT ( 'NONE',  ( 4.749760686538667009, 5.151476664237558900, -6.139290821770204687 ) ) ;
#17277=CARTESIAN_POINT ( 'NONE',  ( 7.249760686538667009, 7.892520144992435149, 1.391664247347255134 ) ) ;
#17279=CARTESIAN_POINT ( 'NONE',  ( 5.377543748152549874, -4.007137495034861274, 6.940565734314584567 ) ) ;
#17281=CARTESIAN_POINT ( 'NONE',  ( -7.993687720252830253, 3.540685504229389213, 0.1911117393897334982 ) ) ;
#17283=VECTOR ( 'NONE', #31485, 1000.000000000000000 ) ;
#17284=CARTESIAN_POINT ( 'NONE',  ( 6.530491712438075247, 7.792522225867695163, -3.778856441136638544 ) ) ;
#17290=CIRCLE ( 'NONE', #14074, 6.248999999999999666 ) ;
#17291=ADVANCED_FACE ( 'NONE', ( #7114 ), #24983, .T. ) ;
#17293=CARTESIAN_POINT ( 'NONE',  ( 3.499999999999999556, -4.724769925181202090, 4.089810527897741466 ) ) ;
#17302=ORIENTED_EDGE ( 'NONE', *, *, #183, .F. ) ;
#17303=DIRECTION ( 'NONE',  ( -1.000000000000000000, -0.000000000000000000, -0.000000000000000000 ) ) ;
#17306=LINE ( 'NONE', #20490, #14064 ) ;
#17318=DIRECTION ( 'NONE',  ( 1.000000000000000000, -0.000000000000000000, 0.000000000000000000 ) ) ;
#17319=CARTESIAN_POINT ( 'NONE',  ( -3.750050802731187627, 0.3135853898029611342, -2.983565686104819648 ) ) ;
#17321=CARTESIAN_POINT ( 'NONE',  ( -8.187550801365594211, 0.3701630799359330593, -3.521866450007987037 ) ) ;
#17322=EDGE_CURVE ( 'NONE', #16071, #30224, #24638, .T. ) ;
#17324=CARTESIAN_POINT ( 'NONE',  ( -4.000050802731187183, -3.113457007523259268, 0.9222479816126455399 ) ) ;
#17327=CIRCLE ( 'NONE', #2954, 8.750000000000000000 ) ;
#17350=PLANE ( 'NONE',  #3798 ) ;
#17353=CARTESIAN_POINT ( 'NONE',  ( 0.000000000000000000, -7.009698679648292519, 0.7308381473896670144 ) ) ;
#17354=AXIS2_PLACEMENT_3D ( 'NONE', #4182, #29767, #19416 ) ;
#17360=ORIENTED_EDGE ( 'NONE', *, *, #9409, .T. ) ;
#17361=CARTESIAN_POINT ( 'NONE',  ( -7.154531657079157725, -3.105402419394638791, 0.9198621039125867149 ) ) ;
#17366=ORIENTED_EDGE ( 'NONE', *, *, #8981, .T. ) ;
#17374=CARTESIAN_POINT ( 'NONE',  ( 6.038145208238973716, 4.620191422127224001, -7.104833038995668204 ) ) ;
#17376=DIRECTION ( 'NONE',  ( 0.000000000000000000, 0.000000000000000000, 1.000000000000000000 ) ) ;
#17378=CARTESIAN_POINT ( 'NONE',  ( -7.550050802731187893, 2.983565686104819648, 0.3135853898029609677 ) ) ;
#17379=CARTESIAN_POINT ( 'NONE',  ( 7.249760686538667009, -7.906491560603638113, -3.748318449932378282 ) ) ;
#17383=ORIENTED_EDGE ( 'NONE', *, *, #21871, .F. ) ;
#17384=CARTESIAN_POINT ( 'NONE',  ( -2.387550801365593056, 3.521866450007987037, 0.3701630799359328372 ) ) ;
#17391=ADVANCED_FACE ( 'NONE', ( #4263 ), #20658, .T. ) ;
#17413=ORIENTED_EDGE ( 'NONE', *, *, #22773, .T. ) ;
#17418=ORIENTED_EDGE ( 'NONE', *, *, #23501, .T. ) ;
#17420=DIRECTION ( 'NONE',  ( 0.000000000000000000, 0.000000000000000000, 1.000000000000000000 ) ) ;
#17422=DIRECTION ( 'NONE',  ( 0.000000000000000000, 0.000000000000000000, 1.000000000000000000 ) ) ;
#17427=CARTESIAN_POINT ( 'NONE',  ( -8.000050800000000351, 3.673940397442060361E-16, 3.000000000000000444 ) ) ;
#17433=EDGE_CURVE ( 'NONE', #14000, #32878, #26124, .T. ) ;
#17434=CARTESIAN_POINT ( 'NONE',  ( -5.237550801365594033, -3.675193018007245627, 1.088641768524163389 ) ) ;
#17442=EDGE_LOOP ( 'NONE', ( #15951, #24808, #13300, #25106 ) ) ;
#17455=CARTESIAN_POINT ( 'NONE',  ( -7.362942409646514363, 1.214281993118000652E-15, 3.000000000000000000 ) ) ;
#17456=FACE_OUTER_BOUND ( 'NONE', #18486, .T. ) ;
#17465=CARTESIAN_POINT ( 'NONE',  ( -1.900050802731187316, 2.853674364686379583, 1.549418761218565921 ) ) ;
#17468=CARTESIAN_POINT ( 'NONE',  ( -7.987550801365593145, 3.521866450007987037, 0.3701630799359328372 ) ) ;
#17470=CARTESIAN_POINT ( 'NONE',  ( -6.912942406915326465, 7.727249047114547632E-16, -2.999999999999999556 ) ) ;
#17472=CARTESIAN_POINT ( 'NONE',  ( 0.000000000000000000, -5.848742439617962141, 6.167836887840968174 ) ) ;
#17473=CARTESIAN_POINT ( 'NONE',  ( 7.064423669210280643, -6.147671362330640044, -6.226446564518105298 ) ) ;
#17481=ORIENTED_EDGE ( 'NONE', *, *, #27935, .T. ) ;
#17487=ORIENTED_EDGE ( 'NONE', *, *, #25747, .F. ) ;
#17497=EDGE_CURVE ( 'NONE', #20265, #23931, #2284, .T. ) ;
#17498=CARTESIAN_POINT ( 'NONE',  ( 6.037141752603385036, 0.4483113388088468820, 8.462586328878536790 ) ) ;
#17499=CARTESIAN_POINT ( 'NONE',  ( 7.249760686538667009, 4.007137495034812424, 6.940565734314612101 ) ) ;
#17504=CARTESIAN_POINT ( 'NONE',  ( -5.262550801365593500, -0.3701630799359326152, 3.521866450007987037 ) ) ;
#17506=CARTESIAN_POINT ( 'NONE',  ( -7.604531657079157903, 2.325406398514293205, -1.883076972206379374 ) ) ;
#17521=CARTESIAN_POINT ( 'NONE',  ( -8.000050800000000351, 0.000000000000000000, 0.000000000000000000 ) ) ;
#17528=CARTESIAN_POINT ( 'NONE',  ( 6.357667697713671018, 8.557242355892499930, -0.9262207444595036421 ) ) ;
#17530=CARTESIAN_POINT ( 'NONE',  ( -3.737550801365593589, -1.828967928396026510, 3.368539882008728004 ) ) ;
#17547=LINE ( 'NONE', #27744, #13500 ) ;
#17550=CARTESIAN_POINT ( 'NONE',  ( -7.312942406915325044, -8.831141768130910875E-16, 2.999999999999999556 ) ) ;
#17557=CARTESIAN_POINT ( 'NONE',  ( -5.362942409646513475, -3.366872799099910998E-15, -3.000000000000000000 ) ) ;
#17560=ORIENTED_EDGE ( 'NONE', *, *, #8759, .T. ) ;
#17573=CARTESIAN_POINT ( 'NONE',  ( 0.000000000000000000, 0.000000000000000000, 0.000000000000000000 ) ) ;
#17575=EDGE_CURVE ( 'NONE', #31514, #21400, #31633, .T. ) ;
#17579=ORIENTED_EDGE ( 'NONE', *, *, #3772, .T. ) ;
#17581=CIRCLE ( 'NONE', #24515, 5.000000000000000000 ) ;
#17583=CARTESIAN_POINT ( 'NONE',  ( -7.787550801365593856, -0.3701630799359326152, 3.521866450007987037 ) ) ;
#17587=CARTESIAN_POINT ( 'NONE',  ( -5.450050802731187360, -1.887961173149512062, -2.331437884370912261 ) ) ;
#17590=DIRECTION ( 'NONE',  ( 0.000000000000000000, 0.7431448254773954654, -0.6691306063588569053 ) ) ;
#17599=ORIENTED_EDGE ( 'NONE', *, *, #31164, .T. ) ;
#17600=ORIENTED_EDGE ( 'NONE', *, *, #31294, .F. ) ;
#17604=CARTESIAN_POINT ( 'NONE',  ( 7.249760686538667009, 7.199384779417119518, 4.973063321323901498 ) ) ;
#17606=ORIENTED_EDGE ( 'NONE', *, *, #7097, .F. ) ;
#17610=CARTESIAN_POINT ( 'NONE',  ( 1.750000000000000222, 1.106368468154540263, -8.427689411260562480 ) ) ;
#17611=EDGE_CURVE ( 'NONE', #10072, #6731, #19212, .T. ) ;
#17614=PLANE ( 'NONE',  #26234 ) ;
#17623=CARTESIAN_POINT ( 'NONE',  ( -1.950050802731187138, 2.983565686104819648, 0.3135853898029609677 ) ) ;
#17624=ORIENTED_EDGE ( 'NONE', *, *, #11968, .T. ) ;
#17625=CARTESIAN_POINT ( 'NONE',  ( -8.137550801365593500, 1.828967928396027176, -3.368539882008727115 ) ) ;
#17630=CARTESIAN_POINT ( 'NONE',  ( -1.900050802731187760, 2.853674364686379583, 1.549418761218565921 ) ) ;
#17638=ORIENTED_EDGE ( 'NONE', *, *, #22660, .T. ) ;
#17642=CARTESIAN_POINT ( 'NONE',  ( 3.499999999999999556, 6.226349476952025341, 0.5315761383463585288 ) ) ;
#17651=EDGE_CURVE ( 'NONE', #6731, #11524, #22779, .T. ) ;
#17665=CARTESIAN_POINT ( 'NONE',  ( -5.812550801365592434, -3.368539882008727115, -1.828967928396028064 ) ) ;
#17667=CARTESIAN_POINT ( 'NONE',  ( -7.854531657079157903, -2.846291840500172921, -1.545410377633947618 ) ) ;
#17678=VECTOR ( 'NONE', #15848, 1000.000000000000000 ) ;
#17681=CARTESIAN_POINT ( 'NONE',  ( 7.249760686538667009, -5.064320921489867899, 7.135485519861982873 ) ) ;
#17685=ADVANCED_FACE ( 'NONE', ( #21457 ), #8573, .T. ) ;
#17686=DIRECTION ( 'NONE',  ( 1.000000000000000000, -0.000000000000000000, 0.000000000000000000 ) ) ;
#17688=FACE_OUTER_BOUND ( 'NONE', #20880, .T. ) ;
#17696=CARTESIAN_POINT ( 'NONE',  ( -7.462550801365593678, -3.521866450007987037, -0.3701630799359323931 ) ) ;
#17700=DIRECTION ( 'NONE',  ( -0.000000000000000000, -0.9961946980917461003, 0.08715574274765135188 ) ) ;
#17706=DIRECTION ( 'NONE',  ( 0.000000000000000000, 0.000000000000000000, -1.000000000000000000 ) ) ;
#17710=EDGE_CURVE ( 'NONE', #6622, #19623, #16124, .T. ) ;
#17711=VECTOR ( 'NONE', #31607, 1000.000000000000000 ) ;
#17731=AXIS2_PLACEMENT_3D ( 'NONE', #32294, #19565, #17026 ) ;
#17736=ORIENTED_EDGE ( 'NONE', *, *, #14567, .T. ) ;
#17737=EDGE_CURVE ( 'NONE', #6649, #20892, #24664, .T. ) ;
#17741=CARTESIAN_POINT ( 'NONE',  ( -6.762550801365593500, -2.752080473201636845, 2.228590825266444586 ) ) ;
#17750=CARTESIAN_POINT ( 'NONE',  ( 3.499999999999999556, -7.851777359434021442, 3.255701506262407730 ) ) ;
#17752=CARTESIAN_POINT ( 'NONE',  ( 1.750000000000000222, 0.6700234925292691823, 8.473551116235677583 ) ) ;
#17754=VECTOR ( 'NONE', #22935, 1000.000000000000000 ) ;
#17757=VECTOR ( 'NONE', #32834, 1000.000000000000000 ) ;
#17761=CARTESIAN_POINT ( 'NONE',  ( 5.489344046532323773, 6.978601450725543387, -4.149088721182456752 ) ) ;
#17764=DIRECTION ( 'NONE',  ( -1.000000000000000000, -0.000000000000000000, -0.000000000000000000 ) ) ;
#17767=CARTESIAN_POINT ( 'NONE',  ( -5.137550801365594388, -3.368539882008727115, -1.828967928396027842 ) ) ;
#17772=VERTEX_POINT ( 'NONE', #29149 ) ;
#17775=ORIENTED_EDGE ( 'NONE', *, *, #16828, .T. ) ;
#17781=AXIS2_PLACEMENT_3D ( 'NONE', #25305, #11628, #21823 ) ;
#17790=AXIS2_PLACEMENT_3D ( 'NONE', #21258, #31456, #26456 ) ;
#17792=CARTESIAN_POINT ( 'NONE',  ( 6.356382399260309235, -7.150437133400964207, 4.790388219480536947 ) ) ;
#17794=ORIENTED_EDGE ( 'NONE', *, *, #6222, .T. ) ;
#17795=CARTESIAN_POINT ( 'NONE',  ( -5.357304906975410397, -1.062355717592097015, -2.999999999999998668 ) ) ;
#17797=PRODUCT_DEFINITION_FORMATION_WITH_SPECIFIED_SOURCE ( 'ANY', '', #2027, .NOT_KNOWN. ) ;
#17800=CARTESIAN_POINT ( 'NONE',  ( 6.357667408475528248, 8.588075071450651521, 0.5738000813809884804 ) ) ;
#17803=EDGE_CURVE ( 'NONE', #29357, #6843, #10787, .T. ) ;
#17808=CARTESIAN_POINT ( 'NONE',  ( 7.064423600674403225, 8.711672189282626988, 0.8180878109953719779 ) ) ;
#17810=CIRCLE ( 'NONE', #22084, 2.999999999999999556 ) ;
#17812=CARTESIAN_POINT ( 'NONE',  ( 1.750000000000000222, 6.745408891279611296, -5.171987904998037067 ) ) ;
#17813=CARTESIAN_POINT ( 'NONE',  ( -3.300050802731187893, -1.549418761218565477, 2.853674364686380471 ) ) ;
#17817=CARTESIAN_POINT ( 'NONE',  ( -7.137550801365592612, 3.368539882008727115, 1.828967928396026954 ) ) ;
#17821=VERTEX_POINT ( 'NONE', #1556 ) ;
#17823=CARTESIAN_POINT ( 'NONE',  ( 5.612718825656738630, -5.432357446996367578, -6.163864706064005716 ) ) ;
#17826=CARTESIAN_POINT ( 'NONE',  ( 7.249760686538667009, 0.000000000000000000, 0.000000000000000000 ) ) ;
#17836=ORIENTED_EDGE ( 'NONE', *, *, #11125, .T. ) ;
#17837=AXIS2_PLACEMENT_3D ( 'NONE', #26179, #8128, #20685 ) ;
#17839=CARTESIAN_POINT ( 'NONE',  ( 0.000000000000000000, 8.265874651078044977, -1.981241088980699061 ) ) ;
#17841=CARTESIAN_POINT ( 'NONE',  ( 7.249760686538667009, 6.940565734314653845, -4.007137495034738706 ) ) ;
#17842=DIRECTION ( 'NONE',  ( -1.000000000000000000, 0.000000000000000000, -0.000000000000000000 ) ) ;
#17846=CARTESIAN_POINT ( 'NONE',  ( 3.499999999999999556, 0.000000000000000000, 0.000000000000000000 ) ) ;
#17847=DIRECTION ( 'NONE',  ( 0.000000000000000000, 0.5735764363510406083, 0.8191520442889956843 ) ) ;
#17850=ADVANCED_FACE ( 'NONE', ( #14243 ), #31675, .T. ) ;
#17851=LINE ( 'NONE', #10635, #14543 ) ;
#17856=CARTESIAN_POINT ( 'NONE',  ( -5.612550801365594033, 1.828967928396027176, -3.368539882008727115 ) ) ;
#17858=CARTESIAN_POINT ( 'NONE',  ( -2.504531657079157370, -0.3127741368606806738, 2.975847129947406522 ) ) ;
#17859=VECTOR ( 'NONE', #27006, 1000.000000000000114 ) ;
#17878=B_SPLINE_CURVE_WITH_KNOTS ( 'NONE', 3,
 ( #3886, #29273, #9026, #19247, #11404, #6545, #29126, #6212, #26948, #16395 ),
 .UNSPECIFIED., .F., .F.,
 ( 4, 2, 2, 2, 4 ),
 ( 1.968338519004493493E-07, 0.0005467926395225675444, 0.001093388445193234099, 0.001639984250863900546, 0.002186580056534566992 ),
 .UNSPECIFIED. ) ;
#17879=ORIENTED_EDGE ( 'NONE', *, *, #1183, .F. ) ;
#17880=CARTESIAN_POINT ( 'NONE',  ( -8.000050800000000351, -1.091513931690352157, -2.808169894813009382 ) ) ;
#17884=CARTESIAN_POINT ( 'NONE',  ( 7.249760686538667009, 8.711672189281440382, -0.8180878109960949551 ) ) ;
#17886=AXIS2_PLACEMENT_3D ( 'NONE', #24437, #1554, #16925 ) ;
#17887=CARTESIAN_POINT ( 'NONE',  ( -6.912550801365593856, 1.088641768524161613, 3.675193018007247403 ) ) ;
#17888=CARTESIAN_POINT ( 'NONE',  ( 5.377543748152549874, 5.151476664237558900, -6.139290821770204687 ) ) ;
#17901=LINE ( 'NONE', #25746, #6573 ) ;
#17917=CARTESIAN_POINT ( 'NONE',  ( -7.962550801365594566, 2.752080473201636845, -2.228590825266444142 ) ) ;
#17918=CARTESIAN_POINT ( 'NONE',  ( 6.530491627857225367, -8.330327812606277860, 2.368289848745726456 ) ) ;
#17921=ORIENTED_EDGE ( 'NONE', *, *, #30286, .F. ) ;
#17943=CARTESIAN_POINT ( 'NONE',  ( -4.987550801365594033, 0.3701630799359330593, -3.521866450007987037 ) ) ;
#17950=ORIENTED_EDGE ( 'NONE', *, *, #26518, .F. ) ;
#17952=ORIENTED_EDGE ( 'NONE', *, *, #14376, .T. ) ;
#17956=ORIENTED_EDGE ( 'NONE', *, *, #8866, .F. ) ;
#17957=CARTESIAN_POINT ( 'NONE',  ( 7.249760686538667009, -4.973063321323826003, -7.199384779417172808 ) ) ;
#17958=EDGE_CURVE ( 'NONE', #26824, #24117, #27381, .T. ) ;
#17961=DIRECTION ( 'NONE',  ( -1.000000000000000000, 0.000000000000000000, 0.000000000000000000 ) ) ;
#17963=CARTESIAN_POINT ( 'NONE',  ( -5.600050800000000883, -2.331437884370912705, 1.887961173149512062 ) ) ;
#17968=CARTESIAN_POINT ( 'NONE',  ( 5.887529311434773760, 8.386653846779019261, 0.3723788567093603841 ) ) ;
#17971=DIRECTION ( 'NONE',  ( 0.000000000000000000, -0.9659258262890650926, -0.2588190451025325634 ) ) ;
#17977=CARTESIAN_POINT ( 'NONE',  ( 5.489343806296449024, -8.012901424861405886, -1.307372367723720563 ) ) ;
#17979=CARTESIAN_POINT ( 'NONE',  ( -2.350050802731187272, -2.983565686104819648, -0.3135853898029605791 ) ) ;
#17981=CARTESIAN_POINT ( 'NONE',  ( -6.987550801365594033, -0.3701630799359326152, 3.521866450007987037 ) ) ;
#17988=ORIENTED_EDGE ( 'NONE', *, *, #183, .T. ) ;
#18005=ORIENTED_EDGE ( 'NONE', *, *, #29581, .F. ) ;
#18009=CARTESIAN_POINT ( 'NONE',  ( -6.950050802731187360, 0.3135853898029611342, -2.983565686104819648 ) ) ;
#18011=CARTESIAN_POINT ( 'NONE',  ( -7.356376981307137797, -0.1572233378491232070, 3.000000000000000444 ) ) ;
#18016=CARTESIAN_POINT ( 'NONE',  ( -5.062550801365593323, -3.521866450007987037, -0.3701630799359323931 ) ) ;
#18017=ORIENTED_EDGE ( 'NONE', *, *, #14376, .F. ) ;
#18018=B_SPLINE_CURVE_WITH_KNOTS ( 'NONE', 3,
 ( #12221, #19601, #6873, #19946, #22425, #32640, #9720, #30154, #7229, #7378 ),
 .UNSPECIFIED., .F., .F.,
 ( 4, 2, 2, 2, 4 ),
 ( 2.571685856645629606E-07, 0.0005478592107668797933, 0.001095461252948095026, 0.001643063295129310259, 0.002190665337310525491 ),
 .UNSPECIFIED. ) ;
#18019=CARTESIAN_POINT ( 'NONE',  ( -4.304531657079157192, 2.975847129947406522, 0.3127741368606808403 ) ) ;
#18029=ADVANCED_FACE ( 'NONE', ( #8052 ), #13225, .T. ) ;
#18031=CYLINDRICAL_SURFACE ( 'NONE', #12418, 6.248999999999999666 ) ;
#18032=CARTESIAN_POINT ( 'NONE',  ( 6.357667873252802693, 8.266402141659474623, -2.398098878660871680 ) ) ;
#18034=CARTESIAN_POINT ( 'NONE',  ( -8.000050800000002127, -2.542211635524239455, 1.618308171042345034 ) ) ;
#18039=ORIENTED_EDGE ( 'NONE', *, *, #16494, .T. ) ;
#18040=CARTESIAN_POINT ( 'NONE',  ( -5.112550801365594033, -3.675193018007246071, 1.088641768524163167 ) ) ;
#18044=VERTEX_POINT ( 'NONE', #31455 ) ;
#18047=DIRECTION ( 'NONE',  ( 0.000000000000000000, -0.08715574274766617335, 0.9961946980917448791 ) ) ;
#18067=CARTESIAN_POINT ( 'NONE',  ( -6.162550801365593856, 2.228590825266444142, 2.752080473201636845 ) ) ;
#18085=CARTESIAN_POINT ( 'NONE',  ( 5.612718761614564400, 7.013540705848238410, -4.279483796478951163 ) ) ;
#18087=EDGE_LOOP ( 'NONE', ( #5632, #22741, #18632, #19484 ) ) ;
#18090=ORIENTED_EDGE ( 'NONE', *, *, #5808, .T. ) ;
#18099=( BOUNDED_CURVE ( )  B_SPLINE_CURVE ( 2, ( #15934, #16584, #11249, #21625, #28660, #6091, #23636, #26627, #912, #18782, #21289 ),
 .UNSPECIFIED., .F., .F. ) 
 B_SPLINE_CURVE_WITH_KNOTS ( ( 3, 2, 2, 2, 2, 3 ),
 ( 0.8103822619934377691, 0.8125000000000000000, 0.8281250000000000000, 0.8437500000000000000, 0.8593750000000000000, 0.8728822619934377691 ),
 .UNSPECIFIED. ) 
 CURVE ( )  GEOMETRIC_REPRESENTATION_ITEM ( )  RATIONAL_B_SPLINE_CURVE ( ( 0.9821626249036861100, 0.9896829947469995004, 1.000000000000000000, 0.9238795325112867385, 1.000000000000000000, 0.9238795325112867385, 1.000000000000000000, 0.9238795325112867385, 1.000000000000000000, 0.9341965377642872381, 0.9821626249036861100 ) ) 
 REPRESENTATION_ITEM ( '' )  );
#18103=ORIENTED_EDGE ( 'NONE', *, *, #28557, .T. ) ;
#18105=ORIENTED_EDGE ( 'NONE', *, *, #12254, .T. ) ;
#18106=DIRECTION ( 'NONE',  ( -1.000000000000000000, -0.000000000000000000, -0.000000000000000000 ) ) ;
#18109=ORIENTED_EDGE ( 'NONE', *, *, #6126, .T. ) ;
#18110=ORIENTED_EDGE ( 'NONE', *, *, #20616, .T. ) ;
#18115=CARTESIAN_POINT ( 'NONE',  ( 7.249760686538667009, 0.000000000000000000, 0.000000000000000000 ) ) ;
#18122=CARTESIAN_POINT ( 'NONE',  ( 3.499999999999999556, 0.000000000000000000, 0.000000000000000000 ) ) ;
#18123=CARTESIAN_POINT ( 'NONE',  ( 6.038145268433179780, -5.783741681378121946, 6.194606843114065953 ) ) ;
#18126=DIRECTION ( 'NONE',  ( -0.000000000000000000, 0.4226182617406975539, -0.9063077870366508249 ) ) ;
#18127=ORIENTED_EDGE ( 'NONE', *, *, #24976, .T. ) ;
#18128=CARTESIAN_POINT ( 'NONE',  ( -5.637550801365595277, 3.675193018007247403, -1.088641768524161391 ) ) ;
#18134=AXIS2_PLACEMENT_3D ( 'NONE', #9795, #27836, #19828 ) ;
#18138=CARTESIAN_POINT ( 'NONE',  ( 0.000000000000000000, -5.979767908488830663, -1.814490771706242622 ) ) ;
#18148=FACE_OUTER_BOUND ( 'NONE', #17442, .T. ) ;
#18154=CYLINDRICAL_SURFACE ( 'NONE', #8662, 6.248999999999999666 ) ;
#18158=CARTESIAN_POINT ( 'NONE',  ( -8.000050800000000351, 0.8940492601045104681, 3.137005928241842323 ) ) ;
#18161=CARTESIAN_POINT ( 'NONE',  ( 7.249760686538667009, 1.391664247347333294, -7.892520144992419162 ) ) ;
#18164=CARTESIAN_POINT ( 'NONE',  ( -7.612550801365593145, -1.828967928396026510, 3.368539882008728004 ) ) ;
#18167=CARTESIAN_POINT ( 'NONE',  ( -2.554531657079157192, 0.9198621039125853827, 3.105402419394639235 ) ) ;
#18177=VECTOR ( 'NONE', #12138, 1000.000000000000000 ) ;
#18183=DIRECTION ( 'NONE',  ( 0.000000000000000000, 0.000000000000000000, 1.000000000000000000 ) ) ;
#18184=CARTESIAN_POINT ( 'NONE',  ( 3.499999999999999556, -4.724769925181202090, 4.089810527897741466 ) ) ;
#18185=VERTEX_POINT ( 'NONE', #26236 ) ;
#18195=CARTESIAN_POINT ( 'NONE',  ( -7.262550801365593500, 0.3701630799359330593, -3.521866450007987037 ) ) ;
#18200=CARTESIAN_POINT ( 'NONE',  ( 7.249760686538667009, -2.789499415801756586E-14, 8.014274990069656823 ) ) ;
#18201=DIRECTION ( 'NONE',  ( 0.000000000000000000, -0.2588190451025291772, 0.9659258262890660918 ) ) ;
#18207=EDGE_CURVE ( 'NONE', #20158, #20265, #28464, .T. ) ;
#18208=CARTESIAN_POINT ( 'NONE',  ( -2.962942409646513564, 4.884725290497410777E-15, -2.999999999999999556 ) ) ;
#18212=CARTESIAN_POINT ( 'NONE',  ( 4.749760686538667009, 4.007137495034909236, -6.940565734314555257 ) ) ;
#18221=DIRECTION ( 'NONE',  ( -1.000000000000000000, 0.000000000000000000, -0.000000000000000000 ) ) ;
#18225=VERTEX_POINT ( 'NONE', #18208 ) ;
#18226=VECTOR ( 'NONE', #24416, 1000.000000000000000 ) ;
#18228=CARTESIAN_POINT ( 'NONE',  ( -1.996286585346913167, -0.3178988483021041866, 3.024605502323847173 ) ) ;
#18231=LINE ( 'NONE', #20752, #29494 ) ;
#18247=AXIS2_PLACEMENT_3D ( 'NONE', #26867, #6453, #16172 ) ;
#18251=CARTESIAN_POINT ( 'NONE',  ( 6.880160201030087741, 8.703862158141008720, -0.6895871680713464569 ) ) ;
#18257=VERTEX_POINT ( 'NONE', #21070 ) ;
#18272=ORIENTED_EDGE ( 'NONE', *, *, #15244, .T. ) ;
#18276=EDGE_LOOP ( 'NONE', ( #27650, #8005, #18455, #4232 ) ) ;
#18278=PLANE ( 'NONE',  #23038 ) ;
#18279=CARTESIAN_POINT ( 'NONE',  ( 6.524595551582241804, -7.168326838404976087, 4.857153507487923072 ) ) ;
#18282=AXIS2_PLACEMENT_3D ( 'NONE', #21170, #6262, #31368 ) ;
#18285=AXIS2_PLACEMENT_3D ( 'NONE', #16930, #19967, #32658 ) ;
#18289=DIRECTION ( 'NONE',  ( -1.000000000000000000, -0.000000000000000000, -0.000000000000000000 ) ) ;
#18292=AXIS2_PLACEMENT_3D ( 'NONE', #26488, #24294, #1408 ) ;
#18297=AXIS2_PLACEMENT_3D ( 'NONE', #1653, #21713, #16509 ) ;
#18300=DIRECTION ( 'NONE',  ( 0.000000000000000000, -0.2588190451025325634, 0.9659258262890650926 ) ) ;
#18303=CARTESIAN_POINT ( 'NONE',  ( 5.489321708267612898, -5.297846913781735445, 6.152096559282818511 ) ) ;
#18310=VECTOR ( 'NONE', #8536, 1000.000000000000227 ) ;
#18322=CARTESIAN_POINT ( 'NONE',  ( 3.499999999999999556, 6.704570150427012543, -2.172265885002588437 ) ) ;
#18328=DIRECTION ( 'NONE',  ( 0.000000000000000000, 0.2079116908177532363, 0.9781476007338069101 ) ) ;
#18329=ORIENTED_EDGE ( 'NONE', *, *, #26945, .F. ) ;
#18337=B_SPLINE_CURVE_WITH_KNOTS ( 'NONE', 3,
 ( #4693, #22093, #32956, #27437, #14714, #9516, #9367, #7206, #30281, #32457 ),
 .UNSPECIFIED., .F., .F.,
 ( 4, 2, 2, 2, 4 ),
 ( 1.968338519011545307E-07, 0.0005467926395225681949, 0.001093388445193235184, 0.001639984250863902281, 0.002186580056534569161 ),
 .UNSPECIFIED. ) ;
#18344=AXIS2_PLACEMENT_3D ( 'NONE', #6393, #18967, #21782 ) ;
#18346=AXIS2_PLACEMENT_3D ( 'NONE', #12662, #33068, #1993 ) ;
#18347=VECTOR ( 'NONE', #18201, 999.9999999999998863 ) ;
#18348=CARTESIAN_POINT ( 'NONE',  ( -8.000050799999998574, -0.6196328501511008113, 3.096707085269658766 ) ) ;
#18350=DIRECTION ( 'NONE',  ( 0.000000000000000000, 0.000000000000000000, 1.000000000000000000 ) ) ;
#18355=CARTESIAN_POINT ( 'NONE',  ( -2.962550801365593234, 2.228590825266444142, 2.752080473201636845 ) ) ;
#18357=CARTESIAN_POINT ( 'NONE',  ( -3.954531657079157547, -3.105402419394638791, 0.9198621039125867149 ) ) ;
#18360=DIRECTION ( 'NONE',  ( 0.000000000000000000, 0.000000000000000000, 1.000000000000000000 ) ) ;
#18373=DIRECTION ( 'NONE',  ( -1.000000000000000000, 0.000000000000000000, 0.000000000000000000 ) ) ;
#18380=EDGE_CURVE ( 'NONE', #25632, #292, #9602, .T. ) ;
#18383=CARTESIAN_POINT ( 'NONE',  ( -5.462550801365593678, 3.521866450007987037, 0.3701630799359328372 ) ) ;
#18388=( BOUNDED_SURFACE ( )  B_SPLINE_SURFACE ( 1, 2, ( 
 ( #14823, #30391, #22533, #28054, #2136, #7464, #10487, #30572, #20541, #18164, #28204, #5152, #28369, #20357, #20047, #2322, #15173, #30242, #4991, #4805, #2821, #25022, #27875, #23210, #25379, #315, #30751, #10328, #25698, #25198, #20699, #12804, #15484, #22712, #12505, #12316, #7658, #2487, #12655, #23017, #22859, #32914, #33061, #9984, #20195, #17665, #10134, #139, #7314, #17856, #15327, #25532, #30901, #32755, #2639, #9831, #17504, #27699, #14981, #7822, #18016, #13000, #8622, #31724, #10985, #23690, #619, #29045, #10812, #459, #18509, #28855, #31057, #21187, #18840, #3000, #6134, #31385, #5650, #8460, #8144, #5796, #16317, #8313, #3482, #31238, #23508, #21030, #23353, #26195, #28703, #5954, #5484, #18654, #25886, #26527, #8799, #13153, #10640, #20847, #15973, #26382, #18355, #3626, #21331, #16152, #26039, #23842, #23987, #953, #1109, #15677, #3304, #13639, #13473, #807, #13785, #11132, #11304, #21512, #31538 ),
 ( #19005, #28553, #15830, #3142, #13299, #29190, #11624, #3781, #9285, #16461, #21818, #24833, #11785, #1781, #32533, #9440, #19502, #9597, #1595, #1295, #16636, #29532, #11473, #19326, #19150, #17130, #6278, #9099, #4458, #6621, #14634, #11974, #24652, #6931, #6431, #1952, #27163, #29850, #3965, #26846, #26668, #21988, #16814, #27013, #4267, #4115, #14135, #14283, #24334, #1447, #32028, #24478, #14441, #21669, #32216, #29695, #6776, #12124, #13950, #16964, #22321, #24171, #31876, #8942, #29339, #32381, #22171, #19658, #27339, #25341, #4945, #14942, #10280, #25154, #14789, #32877, #10098, #12276, #2450, #22973, #17319, #20501, #12619, #20007, #22820, #22490, #20157, #30714, #22675, #17813, #12460, #4768, #2274, #4613, #7425, #9944, #20316, #19821, #33024, #7120, #7786, #23169, #27513, #24986, #2097, #30355, #7608, #32705, #17979, #2600, #30526, #7275, #30203, #28167, #30028, #9785, #17623, #17465, #27665, #27828, #15130 ) ),
 .UNSPECIFIED., .F., .F., .F. ) 
 B_SPLINE_SURFACE_WITH_KNOTS ( ( 2, 2 ),
 ( 3, 2, 2, 2, 2, 2, 2, 2, 2, 2, 2, 2, 2, 2, 2, 2, 2, 2, 2, 2, 2, 2, 2, 2, 2, 2, 2, 2, 2, 2, 2, 2, 2, 2, 2, 2, 2, 2, 2, 2, 2, 2, 2, 2, 2, 2, 2, 2, 2, 2, 2, 2, 2, 2, 2, 2, 2, 2, 2, 2, 3 ),
 ( 0.000000000000000000, 1.000000000000000000 ),
 ( 0.000000000000000000, 0.01562500000000000000, 0.03125000000000000000, 0.04687500000000000000, 0.06250000000000000000, 0.07812500000000000000, 0.09375000000000000000, 0.1093750000000000000, 0.1250000000000000000, 0.1406250000000000000, 0.1562500000000000000, 0.1718750000000000000, 0.1875000000000000000, 0.2031250000000000000, 0.2187500000000000000, 0.2343750000000000000, 0.2500000000000000000, 0.2656250000000000000, 0.2812500000000000000, 0.2968750000000000000, 0.3125000000000000000, 0.3281250000000000000, 0.3437500000000000000, 0.3593750000000000000, 0.3750000000000000000, 0.3906250000000000000, 0.4062500000000000000, 0.4218750000000000000, 0.4375000000000000000, 0.4531250000000000000, 0.4687500000000000000, 0.4843750000000000000, 0.5000000000000000000, 0.5156250000000000000, 0.5312500000000000000, 0.5468750000000000000, 0.5625000000000000000, 0.5781250000000000000, 0.5937500000000000000, 0.6093750000000000000, 0.6250000000000000000, 0.6406250000000000000, 0.6562500000000000000, 0.6718750000000000000, 0.6875000000000000000, 0.7031250000000000000, 0.7187500000000000000, 0.7343750000000000000, 0.7500000000000000000, 0.7656250000000000000, 0.7812500000000000000, 0.7968750000000000000, 0.8125000000000000000, 0.8281250000000000000, 0.8437500000000000000, 0.8593750000000000000, 0.8750000000000000000, 0.8906250000000000000, 0.9062500000000000000, 0.9218750000000000000, 0.9375000000000000000 ),
 .UNSPECIFIED. ) 
 GEOMETRIC_REPRESENTATION_ITEM ( )  RATIONAL_B_SPLINE_SURFACE ( (
 ( 1.000000000000000000, 0.9238795325112867385, 1.000000000000000000, 0.9238795325112867385, 1.000000000000000000, 0.9238795325112867385, 1.000000000000000000, 0.9238795325112867385, 1.000000000000000000, 0.9238795325112867385, 1.000000000000000000, 0.9238795325112867385, 1.000000000000000000, 0.9238795325112867385, 1.000000000000000000, 0.9238795325112867385, 1.000000000000000000, 0.9238795325112867385, 1.000000000000000000, 0.9238795325112867385, 1.000000000000000000, 0.9238795325112867385, 1.000000000000000000, 0.9238795325112867385, 1.000000000000000000, 0.9238795325112867385, 1.000000000000000000, 0.9238795325112867385, 1.000000000000000000, 0.9238795325112867385, 1.000000000000000000, 0.9238795325112867385, 1.000000000000000000, 0.9238795325112867385, 1.000000000000000000, 0.9238795325112867385, 1.000000000000000000, 0.9238795325112867385, 1.000000000000000000, 0.9238795325112867385, 1.000000000000000000, 0.9238795325112867385, 1.000000000000000000, 0.9238795325112867385, 1.000000000000000000, 0.9238795325112867385, 1.000000000000000000, 0.9238795325112867385, 1.000000000000000000, 0.9238795325112867385, 1.000000000000000000, 0.9238795325112867385, 1.000000000000000000, 0.9238795325112867385, 1.000000000000000000, 0.9238795325112867385, 1.000000000000000000, 0.9238795325112867385, 1.000000000000000000, 0.9238795325112867385, 1.000000000000000000, 0.9238795325112867385, 1.000000000000000000, 0.9238795325112867385, 1.000000000000000000, 0.9238795325112867385, 1.000000000000000000, 0.9238795325112867385, 1.000000000000000000, 0.9238795325112867385, 1.000000000000000000, 0.9238795325112867385, 1.000000000000000000, 0.9238795325112867385, 1.000000000000000000, 0.9238795325112867385, 1.000000000000000000, 0.9238795325112867385, 1.000000000000000000, 0.9238795325112867385, 1.000000000000000000, 0.9238795325112867385, 1.000000000000000000, 0.9238795325112867385, 1.000000000000000000, 0.9238795325112867385, 1.000000000000000000, 0.9238795325112867385, 1.000000000000000000, 0.9238795325112867385, 1.000000000000000000, 0.9238795325112867385, 1.000000000000000000, 0.9238795325112867385, 1.000000000000000000, 0.9238795325112867385, 1.000000000000000000, 0.9238795325112867385, 1.000000000000000000, 0.9238795325112867385, 1.000000000000000000, 0.9238795325112867385, 1.000000000000000000, 0.9238795325112867385, 1.000000000000000000, 0.9238795325112867385, 1.000000000000000000, 0.9238795325112867385, 1.000000000000000000, 0.9238795325112867385, 1.000000000000000000, 0.9238795325112867385, 1.000000000000000000, 0.9238795325112867385, 1.000000000000000000, 0.9238795325112867385, 1.000000000000000000, 0.9238795325112867385, 1.000000000000000000, 0.9238795325112867385, 1.000000000000000000),
 ( 1.000000000000000000, 0.9238795325112867385, 1.000000000000000000, 0.9238795325112867385, 1.000000000000000000, 0.9238795325112867385, 1.000000000000000000, 0.9238795325112867385, 1.000000000000000000, 0.9238795325112867385, 1.000000000000000000, 0.9238795325112867385, 1.000000000000000000, 0.9238795325112867385, 1.000000000000000000, 0.9238795325112867385, 1.000000000000000000, 0.9238795325112867385, 1.000000000000000000, 0.9238795325112867385, 1.000000000000000000, 0.9238795325112867385, 1.000000000000000000, 0.9238795325112867385, 1.000000000000000000, 0.9238795325112867385, 1.000000000000000000, 0.9238795325112867385, 1.000000000000000000, 0.9238795325112867385, 1.000000000000000000, 0.9238795325112867385, 1.000000000000000000, 0.9238795325112867385, 1.000000000000000000, 0.9238795325112867385, 1.000000000000000000, 0.9238795325112867385, 1.000000000000000000, 0.9238795325112867385, 1.000000000000000000, 0.9238795325112867385, 1.000000000000000000, 0.9238795325112867385, 1.000000000000000000, 0.9238795325112867385, 1.000000000000000000, 0.9238795325112867385, 1.000000000000000000, 0.9238795325112867385, 1.000000000000000000, 0.9238795325112867385, 1.000000000000000000, 0.9238795325112867385, 1.000000000000000000, 0.9238795325112867385, 1.000000000000000000, 0.9238795325112867385, 1.000000000000000000, 0.9238795325112867385, 1.000000000000000000, 0.9238795325112867385, 1.000000000000000000, 0.9238795325112867385, 1.000000000000000000, 0.9238795325112867385, 1.000000000000000000, 0.9238795325112867385, 1.000000000000000000, 0.9238795325112867385, 1.000000000000000000, 0.9238795325112867385, 1.000000000000000000, 0.9238795325112867385, 1.000000000000000000, 0.9238795325112867385, 1.000000000000000000, 0.9238795325112867385, 1.000000000000000000, 0.9238795325112867385, 1.000000000000000000, 0.9238795325112867385, 1.000000000000000000, 0.9238795325112867385, 1.000000000000000000, 0.9238795325112867385, 1.000000000000000000, 0.9238795325112867385, 1.000000000000000000, 0.9238795325112867385, 1.000000000000000000, 0.9238795325112867385, 1.000000000000000000, 0.9238795325112867385, 1.000000000000000000, 0.9238795325112867385, 1.000000000000000000, 0.9238795325112867385, 1.000000000000000000, 0.9238795325112867385, 1.000000000000000000, 0.9238795325112867385, 1.000000000000000000, 0.9238795325112867385, 1.000000000000000000, 0.9238795325112867385, 1.000000000000000000, 0.9238795325112867385, 1.000000000000000000, 0.9238795325112867385, 1.000000000000000000, 0.9238795325112867385, 1.000000000000000000, 0.9238795325112867385, 1.000000000000000000, 0.9238795325112867385, 1.000000000000000000, 0.9238795325112867385, 1.000000000000000000, 0.9238795325112867385, 1.000000000000000000) ) ) 
 REPRESENTATION_ITEM ( '' )  SURFACE ( )  );
#18392=ORIENTED_EDGE ( 'NONE', *, *, #5221, .F. ) ;
#18393=CARTESIAN_POINT ( 'NONE',  ( -8.000050800000000351, 0.000000000000000000, -3.000000000000000444 ) ) ;
#18402=EDGE_CURVE ( 'NONE', #572, #9138, #3520, .T. ) ;
#18412=DIRECTION ( 'NONE',  ( 1.000000000000000000, -0.000000000000000000, -0.000000000000000000 ) ) ;
#18417=CARTESIAN_POINT ( 'NONE',  ( -5.312550801365593323, 1.088641768524161613, 3.675193018007246959 ) ) ;
#18419=ADVANCED_FACE ( 'NONE', ( #3663 ), #29230, .F. ) ;
#18438=CARTESIAN_POINT ( 'NONE',  ( 0.000000000000000000, 6.100541242131516384, -3.528937025535512362 ) ) ;
#18447=ORIENTED_EDGE ( 'NONE', *, *, #31005, .F. ) ;
#18454=CARTESIAN_POINT ( 'NONE',  ( 5.885541806331897163, -3.871259391815505602, 7.447669719165321389 ) ) ;
#18455=ORIENTED_EDGE ( 'NONE', *, *, #11663, .T. ) ;
#18463=CARTESIAN_POINT ( 'NONE',  ( 0.000000000000000000, -5.522688772756442432, 6.461416928141223259 ) ) ;
#18468=CARTESIAN_POINT ( 'NONE',  ( 7.064423669210280643, 5.064320921489786187, -7.135485519863410175 ) ) ;
#18478=DIRECTION ( 'NONE',  ( -0.000000000000000000, 1.000000000000000000, 1.224646799147353207E-16 ) ) ;
#18486=EDGE_LOOP ( 'NONE', ( #21552, #766, #7617 ) ) ;
#18489=CARTESIAN_POINT ( 'NONE',  ( -7.600050800000000883, 2.331437884370912705, -1.887961173149511618 ) ) ;
#18491=VERTEX_POINT ( 'NONE', #21859 ) ;
#18495=DIRECTION ( 'NONE',  ( 0.000000000000000000, 0.4226182617407134856, -0.9063077870366433864 ) ) ;
#18497=DIRECTION ( 'NONE',  ( -1.000000000000000000, 0.000000000000000000, 0.000000000000000000 ) ) ;
#18502=EDGE_CURVE ( 'NONE', #3656, #17188, #31581, .T. ) ;
#18503=ADVANCED_FACE ( 'NONE', ( #11662 ), #16223, .F. ) ;
#18504=CARTESIAN_POINT ( 'NONE',  ( -8.000050800000000351, -1.393745829612481169, 2.767030136172837107 ) ) ;
#18507=CARTESIAN_POINT ( 'NONE',  ( 5.885541838704148709, -6.662285765435181695, -5.105720535585480668 ) ) ;
#18509=CARTESIAN_POINT ( 'NONE',  ( -4.562550801365594211, 2.228590825266444142, 2.752080473201636845 ) ) ;
#18511=CARTESIAN_POINT ( 'NONE',  ( -3.404531657079157281, 1.883076972206379374, 2.325406398514293205 ) ) ;
#18513=CARTESIAN_POINT ( 'NONE',  ( -7.712942406915323623, 7.727249047114547632E-16, -2.999999999999999556 ) ) ;
#18518=ORIENTED_EDGE ( 'NONE', *, *, #14468, .F. ) ;
#18522=CARTESIAN_POINT ( 'NONE',  ( 3.499999999999999556, 1.418488851014487073, -6.085876303339362359 ) ) ;
#18523=CARTESIAN_POINT ( 'NONE',  ( 5.885541838704153150, 6.662285765435218110, 5.105720535585435371 ) ) ;
#18525=CARTESIAN_POINT ( 'NONE',  ( 6.880159790065803804, -8.451885315426441281, 2.190520500543459814 ) ) ;
#18526=LINE ( 'NONE', #31257, #6484 ) ;
#18531=EDGE_LOOP ( 'NONE', ( #17481, #2066, #30899 ) ) ;
#18532=CARTESIAN_POINT ( 'NONE',  ( -2.662550801365593411, -3.521866450007987037, -0.3701630799359323931 ) ) ;
#18533=DIRECTION ( 'NONE',  ( 0.000000000000000000, -0.9063077870366466060, -0.4226182617407066022 ) ) ;
#18557=EDGE_CURVE ( 'NONE', #26682, #7898, #1201, .T. ) ;
#18558=ORIENTED_EDGE ( 'NONE', *, *, #33027, .T. ) ;
#18560=LINE ( 'NONE', #8217, #3285 ) ;
#18561=CARTESIAN_POINT ( 'NONE',  ( -3.712550801365593234, 1.088641768524161613, 3.675193018007246959 ) ) ;
#18563=DIRECTION ( 'NONE',  ( 1.000000000000000000, -0.000000000000000000, -0.000000000000000000 ) ) ;
#18565=CARTESIAN_POINT ( 'NONE',  ( 5.612718622971683224, 7.650113768151216576, -2.996580135471449413 ) ) ;
#18566=VERTEX_POINT ( 'NONE', #8873 ) ;
#18567=CARTESIAN_POINT ( 'NONE',  ( -7.237550801365592257, 3.675193018007247403, -1.088641768524161391 ) ) ;
#18580=CARTESIAN_POINT ( 'NONE',  ( 7.249760686538667009, 6.139290821770257089, 5.151476664237498504 ) ) ;
#18585=ORIENTED_EDGE ( 'NONE', *, *, #11689, .T. ) ;
#18587=CARTESIAN_POINT ( 'NONE',  ( -2.562942409646512321, -5.022711880624455567E-15, 2.999999999999999556 ) ) ;
#18590=CARTESIAN_POINT ( 'NONE',  ( 3.499999999999999556, 5.241389472434663688, 4.711457988287072851 ) ) ;
#18592=ORIENTED_EDGE ( 'NONE', *, *, #23692, .F. ) ;
#18596=CARTESIAN_POINT ( 'NONE',  ( 7.249760686538667009, -8.721381771256204729, -0.7071067811865429098 ) ) ;
#18597=ORIENTED_EDGE ( 'NONE', *, *, #489, .T. ) ;
#18604=ORIENTED_EDGE ( 'NONE', *, *, #16898, .T. ) ;
#18606=CARTESIAN_POINT ( 'NONE',  ( 4.749760686538667009, -7.530955069117533540, 2.741043480754901118 ) ) ;
#18610=PLANE ( 'NONE',  #32662 ) ;
#18613=EDGE_CURVE ( 'NONE', #10070, #26504, #25066, .T. ) ;
#18615=ORIENTED_EDGE ( 'NONE', *, *, #12169, .F. ) ;
#18618=CARTESIAN_POINT ( 'NONE',  ( 7.249760686538667009, 2.741043480754926875, 7.530955069117522882 ) ) ;
#18632=ORIENTED_EDGE ( 'NONE', *, *, #1018, .F. ) ;
#18636=CARTESIAN_POINT ( 'NONE',  ( 6.357667408475528248, 0.5738000813810777423, -8.588075071450642639 ) ) ;
#18638=ORIENTED_EDGE ( 'NONE', *, *, #20097, .F. ) ;
#18642=LINE ( 'NONE', #28839, #29894 ) ;
#18648=CARTESIAN_POINT ( 'NONE',  ( -6.562942409646512765, -8.831141768130910875E-16, 2.999999999999999556 ) ) ;
#18654=CARTESIAN_POINT ( 'NONE',  ( -3.412550801365593411, -3.368539882008727115, -1.828967928396028064 ) ) ;
#18656=CARTESIAN_POINT ( 'NONE',  ( -5.100050799999999995, 2.983565686104819648, 0.3135853898029609677 ) ) ;
#18659=VECTOR ( 'NONE', #16393, 1000.000000000000114 ) ;
#18663=EDGE_LOOP ( 'NONE', ( #21761, #6167, #9141, #2781 ) ) ;
#18667=CARTESIAN_POINT ( 'NONE',  ( 7.249760686538667009, 5.064320921489820826, 7.135485519862015735 ) ) ;
#18670=EDGE_CURVE ( 'NONE', #19623, #14119, #17547, .T. ) ;
#18672=DIRECTION ( 'NONE',  ( -1.000000000000000000, 0.000000000000000000, 0.000000000000000000 ) ) ;
#18674=ORIENTED_EDGE ( 'NONE', *, *, #30206, .F. ) ;
#18677=CARTESIAN_POINT ( 'NONE',  ( 7.249760686538667009, 8.711672189281440382, -0.8180878109960949551 ) ) ;
#18681=CARTESIAN_POINT ( 'NONE',  ( -2.062550801365593323, -0.3701630799359326152, 3.521866450007987037 ) ) ;
#18684=CARTESIAN_POINT ( 'NONE',  ( 3.499999999999999556, -0.1221666339523235223, -6.247805719894684806 ) ) ;
#18685=LINE ( 'NONE', #26065, #10734 ) ;
#18686=ORIENTED_EDGE ( 'NONE', *, *, #27160, .T. ) ;
#18688=CARTESIAN_POINT ( 'NONE',  ( 7.249760686538667009, 8.466096581343482086, 2.210816291636243047 ) ) ;
#18695=CARTESIAN_POINT ( 'NONE',  ( -1.783740934873500272, -0.1784080614500640760, 3.046698672529837726 ) ) ;
#18696=CARTESIAN_POINT ( 'NONE',  ( -4.537550801365592967, -1.828967928396026732, 3.368539882008728004 ) ) ;
#18701=CARTESIAN_POINT ( 'NONE',  ( 7.249760686538667009, 3.748318449932293905, 7.906491560603678082 ) ) ;
#18702=AXIS2_PLACEMENT_3D ( 'NONE', #31566, #16340, #16839 ) ;
#18705=VERTEX_POINT ( 'NONE', #31423 ) ;
#18708=AXIS2_PLACEMENT_3D ( 'NONE', #4289, #19845, #4481 ) ;
#18716=CARTESIAN_POINT ( 'NONE',  ( -4.312550801365593323, -3.675193018007245627, 1.088641768524163389 ) ) ;
#18717=CARTESIAN_POINT ( 'NONE',  ( 7.249760686538667009, -4.007137495034861274, 6.940565734314584567 ) ) ;
#18719=CARTESIAN_POINT ( 'NONE',  ( 6.356382228872880624, 7.873648075250545553, -3.475951004017252988 ) ) ;
#18720=ORIENTED_EDGE ( 'NONE', *, *, #24656, .F. ) ;
#18721=CARTESIAN_POINT ( 'NONE',  ( -7.837550801365593678, 1.088641768524161613, 3.675193018007247403 ) ) ;
#18725=CARTESIAN_POINT ( 'NONE',  ( 6.530491482054472385, 2.114164693852704335, -8.398420403995354278 ) ) ;
#18732=AXIS2_PLACEMENT_3D ( 'NONE', #28074, #32936, #30919 ) ;
#18736=CARTESIAN_POINT ( 'NONE',  ( 6.038144853276843804, -1.027626812407944179, -8.412419482080418121 ) ) ;
#18743=CARTESIAN_POINT ( 'NONE',  ( -5.287550801365593856, -2.752080473201636845, 2.228590825266444586 ) ) ;
#18746=ADVANCED_FACE ( 'NONE', ( #29394 ), #32079, .F. ) ;
#18751=EDGE_CURVE ( 'NONE', #11524, #7301, #11924, .T. ) ;
#18753=AXIS2_PLACEMENT_3D ( 'NONE', #4536, #12192, #22392 ) ;
#18758=ORIENTED_EDGE ( 'NONE', *, *, #18765, .F. ) ;
#18763=CARTESIAN_POINT ( 'NONE',  ( 5.377543748152549874, -6.940565734314570356, -4.007137495034885255 ) ) ;
#18765=EDGE_CURVE ( 'NONE', #20892, #29013, #14585, .T. ) ;
#18769=LINE ( 'NONE', #28973, #15503 ) ;
#18780=AXIS2_PLACEMENT_3D ( 'NONE', #13813, #21701, #3515 ) ;
#18782=CARTESIAN_POINT ( 'NONE',  ( -2.957304906975409597, -1.062355717592093463, -3.000000000000000888 ) ) ;
#18783=DIRECTION ( 'NONE',  ( -1.000000000000000000, 0.000000000000000000, 0.000000000000000000 ) ) ;
#18784=ORIENTED_EDGE ( 'NONE', *, *, #29281, .T. ) ;
#18785=CARTESIAN_POINT ( 'NONE',  ( -6.112942406915326643, -3.366872799099910998E-15, -3.000000000000000000 ) ) ;
#18793=AXIS2_PLACEMENT_3D ( 'NONE', #13170, #28570, #5663 ) ;
#18803=VERTEX_POINT ( 'NONE', #31587 ) ;
#18807=AXIS2_PLACEMENT_3D ( 'NONE', #9058, #16277, #916 ) ;
#18810=ORIENTED_EDGE ( 'NONE', *, *, #7423, .T. ) ;
#18815=ORIENTED_EDGE ( 'NONE', *, *, #32948, .T. ) ;
#18816=CARTESIAN_POINT ( 'NONE',  ( 5.377543748152548986, -7.530955069117495349, -2.741043480755002371 ) ) ;
#18818=ORIENTED_EDGE ( 'NONE', *, *, #30261, .F. ) ;
#18825=LINE ( 'NONE', #14271, #27953 ) ;
#18826=CARTESIAN_POINT ( 'NONE',  ( 7.249760686538667009, 8.014274990069656823, -8.669741416787380218E-17 ) ) ;
#18832=CARTESIAN_POINT ( 'NONE',  ( 0.000000000000000000, -6.700937042937042065, -2.183447440113257976 ) ) ;
#18834=VECTOR ( 'NONE', #15233, 1000.000000000000000 ) ;
#18840=CARTESIAN_POINT ( 'NONE',  ( -4.362550801365593145, -2.752080473201636845, 2.228590825266444586 ) ) ;
#18841=ORIENTED_EDGE ( 'NONE', *, *, #6048, .T. ) ;
#18845=CARTESIAN_POINT ( 'NONE',  ( -6.400050800000000706, -2.331437884370912705, 1.887961173149512062 ) ) ;
#18846=CIRCLE ( 'NONE', #4442, 8.500000000000000000 ) ;
#18850=AXIS2_PLACEMENT_3D ( 'NONE', #23516, #23698, #31065 ) ;
#18865=ADVANCED_FACE ( 'NONE', ( #12512 ), #2341, .T. ) ;
#18867=AXIS2_PLACEMENT_3D ( 'NONE', #4656, #15182, #30248 ) ;
#18869=VECTOR ( 'NONE', #31953, 1000.000000000000000 ) ;
#18872=CARTESIAN_POINT ( 'NONE',  ( -3.712550801365592790, 1.088641768524161613, 3.675193018007247403 ) ) ;
#18879=DIRECTION ( 'NONE',  ( 0.000000000000000000, 0.08715574274764703588, 0.9961946980917465444 ) ) ;
#18880=DIRECTION ( 'NONE',  ( -1.000000000000000000, 0.000000000000000000, 0.000000000000000000 ) ) ;
#18886=CARTESIAN_POINT ( 'NONE',  ( 7.064423637758999952, 2.318425219013722227, -8.437262856155470558 ) ) ;
#18887=AXIS2_PLACEMENT_3D ( 'NONE', #8932, #23829, #24323 ) ;
#18890=CARTESIAN_POINT ( 'NONE',  ( -4.187550801365593323, 0.3701630799359330593, -3.521866450007987037 ) ) ;
#18892=DIRECTION ( 'NONE',  ( 0.000000000000000000, 0.000000000000000000, 1.000000000000000000 ) ) ;
#18893=ORIENTED_EDGE ( 'NONE', *, *, #29807, .T. ) ;
#18894=CARTESIAN_POINT ( 'NONE',  ( 7.249760686538667009, -2.318425219014288885, 8.437262856154156054 ) ) ;
#18907=CARTESIAN_POINT ( 'NONE',  ( -2.962550801365593234, 2.228590825266444142, 2.752080473201636845 ) ) ;
#18908=DIRECTION ( 'NONE',  ( -1.000000000000000000, -0.000000000000000000, 0.000000000000000000 ) ) ;
#18912=VECTOR ( 'NONE', #21698, 1000.000000000000000 ) ;
#18914=CARTESIAN_POINT ( 'NONE',  ( -7.337550801365593678, 1.828967928396027176, -3.368539882008727115 ) ) ;
#18922=CARTESIAN_POINT ( 'NONE',  ( 0.000000000000000000, 0.000000000000000000, 0.000000000000000000 ) ) ;
#18925=CARTESIAN_POINT ( 'NONE',  ( 0.000000000000000000, 5.904264776415128146, -2.046865518294647579 ) ) ;
#18930=CARTESIAN_POINT ( 'NONE',  ( 3.499999999999999556, 5.904264776415098837, 2.046865518294726183 ) ) ;
#18931=CARTESIAN_POINT ( 'NONE',  ( -2.587550801365593678, 0.3701630799359330593, -3.521866450007987037 ) ) ;
#18934=CARTESIAN_POINT ( 'NONE',  ( 1.750000000000000222, 4.438567988583082879, 7.249076783337693008 ) ) ;
#18936=CARTESIAN_POINT ( 'NONE',  ( 1.750000000000000222, -2.834406817834963732, 8.013497238472769624 ) ) ;
#18939=DIRECTION ( 'NONE',  ( -1.000000000000000000, 0.000000000000000000, 0.000000000000000000 ) ) ;
#18948=EDGE_LOOP ( 'NONE', ( #13908, #12381, #4753, #13230 ) ) ;
#18954=CARTESIAN_POINT ( 'NONE',  ( 0.000000000000000000, -1.179494851233943598, 6.136676046192483192 ) ) ;
#18955=CARTESIAN_POINT ( 'NONE',  ( -4.962942409646514008, 3.284080845023683730E-15, 3.000000000000000000 ) ) ;
#18956=ADVANCED_FACE ( 'NONE', ( #32761 ), #2493, .T. ) ;
#18958=DIRECTION ( 'NONE',  ( 1.000000000000000000, -0.000000000000000000, 0.000000000000000000 ) ) ;
#18961=CARTESIAN_POINT ( 'NONE',  ( 6.880159540721329847, 8.414807581959459881, 2.328896285337215488 ) ) ;
#18964=CARTESIAN_POINT ( 'NONE',  ( -6.400050800000000706, -2.331437884370912705, 1.887961173149512062 ) ) ;
#18967=DIRECTION ( 'NONE',  ( 1.000000000000000000, -0.000000000000000000, -0.000000000000000000 ) ) ;
#18969=CARTESIAN_POINT ( 'NONE',  ( -2.556376981307135754, -0.1572233378491262878, 2.999999999999999556 ) ) ;
#18974=ORIENTED_EDGE ( 'NONE', *, *, #21438, .T. ) ;
#18980=ORIENTED_EDGE ( 'NONE', *, *, #15093, .T. ) ;
#18985=CARTESIAN_POINT ( 'NONE',  ( 7.249760686538667009, -7.953573330858190182, -3.647351267791651974 ) ) ;
#18989=CARTESIAN_POINT ( 'NONE',  ( 6.883866357751289300, -0.6899766464188280546, 8.704251636488461230 ) ) ;
#19002=CARTESIAN_POINT ( 'NONE',  ( 5.377543748152549874, 4.007137495034909236, -6.940565734314555257 ) ) ;
#19004=ADVANCED_FACE ( 'NONE', ( #29196 ), #6284, .F. ) ;
#19005=CARTESIAN_POINT ( 'NONE',  ( -7.750050802731187183, 0.3135853898029611342, -2.983565686104819648 ) ) ;
#19006=ORIENTED_EDGE ( 'NONE', *, *, #28804, .T. ) ;
#19007=CARTESIAN_POINT ( 'NONE',  ( -7.900050800000000706, -2.983565686104819648, -0.3135853898029605791 ) ) ;
#19014=B_SPLINE_CURVE_WITH_KNOTS ( 'NONE', 3,
 ( #28134, #12907, #25461, #17284, #2570, #7754, #27636, #12587, #10068, #12736 ),
 .UNSPECIFIED., .F., .F.,
 ( 4, 2, 2, 2, 4 ),
 ( 1.968338519013029732E-07, 0.0005467926395225671107, 0.001093388445193233232, 0.001639984250863899245, 0.002186580056534565691 ),
 .UNSPECIFIED. ) ;
#19016=ORIENTED_EDGE ( 'NONE', *, *, #2861, .F. ) ;
#19023=CARTESIAN_POINT ( 'NONE',  ( -5.362942409646513475, -3.366872799099910998E-15, -3.000000000000000000 ) ) ;
#19029=ORIENTED_EDGE ( 'NONE', *, *, #18402, .T. ) ;
#19030=CARTESIAN_POINT ( 'NONE',  ( -4.412550801365593856, -1.828967928396026510, 3.368539882008728004 ) ) ;
#19041=CARTESIAN_POINT ( 'NONE',  ( -2.039411552024039231, 1.053646271254045308, 3.241837583267886291 ) ) ;
#19042=CARTESIAN_POINT ( 'NONE',  ( -4.387550801365594388, -3.521866450007987037, -0.3701630799359323931 ) ) ;
#19047=EDGE_CURVE ( 'NONE', #7898, #112, #11938, .T. ) ;
#19053=CARTESIAN_POINT ( 'NONE',  ( -3.407304909706596607, 1.062355717592091686, 3.000000000000001332 ) ) ;
#19059=CARTESIAN_POINT ( 'NONE',  ( -3.562550801365592879, -2.752080473201636845, 2.228590825266444586 ) ) ;
#19060=EDGE_CURVE ( 'NONE', #10466, #25076, #30122, .T. ) ;
#19064=ORIENTED_EDGE ( 'NONE', *, *, #423, .F. ) ;
#19065=CARTESIAN_POINT ( 'NONE',  ( -7.187550801365593323, 3.521866450007987037, 0.3701630799359328372 ) ) ;
#19069=DIRECTION ( 'NONE',  ( -1.000000000000000000, -0.000000000000000000, -0.000000000000000000 ) ) ;
#19070=VERTEX_POINT ( 'NONE', #17470 ) ;
#19071=CARTESIAN_POINT ( 'NONE',  ( 7.249760686538667009, -7.199384779417084879, -4.973063321323951236 ) ) ;
#19072=VERTEX_POINT ( 'NONE', #30360 ) ;
#19073=B_SPLINE_CURVE_WITH_KNOTS ( 'NONE', 3,
 ( #21742, #23590, #8868, #11391, #6046, #18736, #21413, #11054, #1192, #13859 ),
 .UNSPECIFIED., .F., .F.,
 ( 4, 2, 2, 2, 4 ),
 ( 1.968338519010599806E-07, 0.0005467928198071728228, 0.001093388805762444439, 0.001639984791717716056, 0.002186580777672988106 ),
 .UNSPECIFIED. ) ;
#19084=CARTESIAN_POINT ( 'NONE',  ( 6.037141812302426302, 8.256172215043603657, -1.911013226338322157 ) ) ;
#19088=DIRECTION ( 'NONE',  ( 0.000000000000000000, 0.000000000000000000, 1.000000000000000000 ) ) ;
#19089=ORIENTED_EDGE ( 'NONE', *, *, #7202, .F. ) ;
#19090=B_SPLINE_CURVE_WITH_KNOTS ( 'NONE', 3,
 ( #19790, #14258, #29498, #19125, #17099, #16792, #29316, #1929, #11448, #11758 ),
 .UNSPECIFIED., .F., .F.,
 ( 4, 2, 2, 2, 4 ),
 ( 1.968338519010600071E-07, 0.0005467928198071723891, 0.001093388805762443572, 0.001639984791717714755, 0.002186580777672986371 ),
 .UNSPECIFIED. ) ;
#19091=CARTESIAN_POINT ( 'NONE',  ( -7.850050800000000883, -2.853674364686378695, -1.549418761218566809 ) ) ;
#19094=ORIENTED_EDGE ( 'NONE', *, *, #32948, .F. ) ;
#19097=EDGE_CURVE ( 'NONE', #32424, #17772, #25345, .T. ) ;
#19100=ORIENTED_EDGE ( 'NONE', *, *, #4474, .T. ) ;
#19112=ORIENTED_EDGE ( 'NONE', *, *, #13108, .F. ) ;
#19120=ORIENTED_EDGE ( 'NONE', *, *, #6788, .F. ) ;
#19125=CARTESIAN_POINT ( 'NONE',  ( 6.530491482054475050, -8.615020591497808411, 0.8857639883442617323 ) ) ;
#19129=VERTEX_POINT ( 'NONE', #24659 ) ;
#19141=ADVANCED_FACE ( 'NONE', ( #2454 ), #33030, .T. ) ;
#19144=CARTESIAN_POINT ( 'NONE',  ( 6.357667873252800028, 7.873899671211493256, 3.476490553296878616 ) ) ;
#19145=CARTESIAN_POINT ( 'NONE',  ( 0.000000000000000000, 0.000000000000000000, 0.000000000000000000 ) ) ;
#19147=B_SPLINE_CURVE_WITH_KNOTS ( 'NONE', 3,
 ( #7933, #12948, #28663, #8094, #31198, #18123, #2960, #23319, #18303, #421 ),
 .UNSPECIFIED., .F., .F.,
 ( 4, 2, 2, 2, 4 ),
 ( 1.968338519012285137E-07, 0.0005467926089500455998, 0.001093388384048189993, 0.001639984159146334278, 0.002186579934244478780 ),
 .UNSPECIFIED. ) ;
#19150=CARTESIAN_POINT ( 'NONE',  ( -6.550050802731187005, -0.3135853898029607456, 2.983565686104819648 ) ) ;
#19152=CARTESIAN_POINT ( 'NONE',  ( -6.250050800000000351, -2.853674364686378695, -1.549418761218566809 ) ) ;
#19164=ADVANCED_FACE ( 'NONE', ( #15448 ), #20503, .T. ) ;
#19167=CARTESIAN_POINT ( 'NONE',  ( -6.050050800000001061, 1.549418761218566143, -2.853674364686379583 ) ) ;
#19171=( BOUNDED_CURVE ( )  B_SPLINE_CURVE ( 2, ( #15347, #30770, #22730, #15509, #17378, #12827, #25723, #23044, #27571 ),
 .UNSPECIFIED., .F., .F. ) 
 B_SPLINE_CURVE_WITH_KNOTS ( ( 3, 2, 2, 2, 3 ),
 ( 0.000000000000000000, 0.01562500000000000000, 0.03125000000000000000, 0.04687500000000000694, 0.06038226199343772749 ),
 .UNSPECIFIED. ) 
 CURVE ( )  GEOMETRIC_REPRESENTATION_ITEM ( )  RATIONAL_B_SPLINE_CURVE ( ( 1.000000000000000000, 0.9238795325112867385, 1.000000000000000000, 0.9238795325112867385, 1.000000000000000000, 0.9238795325112867385, 1.000000000000000000, 0.9341965377642874602, 0.9821626249036858880 ) ) 
 REPRESENTATION_ITEM ( '' )  );
#19183=EDGE_CURVE ( 'NONE', #19677, #12332, #5011, .T. ) ;
#19185=FACE_OUTER_BOUND ( 'NONE', #8550, .T. ) ;
#19186=DIRECTION ( 'NONE',  ( -1.000000000000000000, 0.000000000000000000, -0.000000000000000000 ) ) ;
#19189=ORIENTED_EDGE ( 'NONE', *, *, #9172, .T. ) ;
#19208=AXIS2_PLACEMENT_3D ( 'NONE', #26989, #16605, #9570 ) ;
#19210=CARTESIAN_POINT ( 'NONE',  ( 5.612974384376779646, 3.934067627273206025, 7.213266193303272011 ) ) ;
#19212=B_SPLINE_CURVE_WITH_KNOTS ( 'NONE', 3,
 ( #6557, #21924, #32144, #9217, #19447, #16911, #29640, #19597, #6721, #32327 ),
 .UNSPECIFIED., .F., .F.,
 ( 4, 2, 2, 2, 4 ),
 ( 1.968338519003748898E-07, 0.0005467926089500447324, 0.001093388384048189126, 0.001639984159146333411, 0.002186579934244477913 ),
 .UNSPECIFIED. ) ;
#19214=VERTEX_POINT ( 'NONE', #28022 ) ;
#19220=DIRECTION ( 'NONE',  ( -1.000000000000000000, 0.000000000000000000, 0.000000000000000000 ) ) ;
#19221=VERTEX_POINT ( 'NONE', #15943 ) ;
#19222=CARTESIAN_POINT ( 'NONE',  ( -7.787550801365593856, -0.3701630799359326152, 3.521866450007987037 ) ) ;
#19224=CARTESIAN_POINT ( 'NONE',  ( 5.377543748152547209, 1.391664247347333294, -7.892520144992419162 ) ) ;
#19230=CARTESIAN_POINT ( 'NONE',  ( 4.749760686538667009, 4.007137495034909236, -6.940565734314555257 ) ) ;
#19246=CARTESIAN_POINT ( 'NONE',  ( -3.450050800000000084, 2.853674364686379583, 1.549418761218565921 ) ) ;
#19247=CARTESIAN_POINT ( 'NONE',  ( 6.530491712438077023, -7.792522225867670294, 3.778856441136694500 ) ) ;
#19248=ORIENTED_EDGE ( 'NONE', *, *, #28587, .T. ) ;
#19250=ORIENTED_EDGE ( 'NONE', *, *, #6005, .T. ) ;
#19255=VERTEX_POINT ( 'NONE', #15636 ) ;
#19257=CARTESIAN_POINT ( 'NONE',  ( -5.900050802731187538, 2.853674364686379583, 1.549418761218565921 ) ) ;
#19259=ORIENTED_EDGE ( 'NONE', *, *, #2657, .F. ) ;
#19260=CARTESIAN_POINT ( 'NONE',  ( -4.112942406915325755, -5.022711880624455567E-15, 2.999999999999999556 ) ) ;
#19277=CARTESIAN_POINT ( 'NONE',  ( 7.249760686538667009, 2.741043480754926875, 7.530955069117522882 ) ) ;
#19278=B_SPLINE_CURVE_WITH_KNOTS ( 'NONE', 3,
 ( #19071, #11540, #27077, #4352, #12190, #19410, #32297, #24397, #26744, #1366 ),
 .UNSPECIFIED., .F., .F.,
 ( 4, 2, 2, 2, 4 ),
 ( 1.968338519011545042E-07, 0.0005467926395225672191, 0.001093388445193233232, 0.001639984250863899245, 0.002186580056534565258 ),
 .UNSPECIFIED. ) ;
#19280=CARTESIAN_POINT ( 'NONE',  ( -10.00000000000000000, 0.000000000000000000, 0.000000000000000000 ) ) ;
#19283=ORIENTED_EDGE ( 'NONE', *, *, #27162, .T. ) ;
#19293=ORIENTED_EDGE ( 'NONE', *, *, #22273, .T. ) ;
#19296=CARTESIAN_POINT ( 'NONE',  ( 7.249760686538667009, 3.647351267791679508, -7.953573330858177748 ) ) ;
#19310=DIRECTION ( 'NONE',  ( 1.000000000000000000, -0.000000000000000000, -0.000000000000000000 ) ) ;
#19311=CIRCLE ( 'NONE', #3852, 2.999999999999999112 ) ;
#19313=AXIS2_PLACEMENT_3D ( 'NONE', #20647, #30853, #7922 ) ;
#19320=VECTOR ( 'NONE', #32773, 1000.000000000000000 ) ;
#19322=CARTESIAN_POINT ( 'NONE',  ( 6.530491627857224479, 7.903708701126691771, 3.540416224243698284 ) ) ;
#19325=CARTESIAN_POINT ( 'NONE',  ( 3.499999999999999556, -5.979767908488853756, 1.814490771706161354 ) ) ;
#19326=CARTESIAN_POINT ( 'NONE',  ( -6.600050802731186828, 0.9222479816126443186, 3.113457007523260156 ) ) ;
#19328=CARTESIAN_POINT ( 'NONE',  ( -5.850050800000001772, 2.853674364686379583, 1.549418761218565921 ) ) ;
#19329=AXIS2_PLACEMENT_3D ( 'NONE', #2415, #16969, #14907 ) ;
#19332=CARTESIAN_POINT ( 'NONE',  ( -5.762942409646513831, 3.284080845023683730E-15, 3.000000000000000000 ) ) ;
#19340=ORIENTED_EDGE ( 'NONE', *, *, #21438, .F. ) ;
#19357=FACE_OUTER_BOUND ( 'NONE', #30176, .T. ) ;
#19359=VECTOR ( 'NONE', #3612, 1000.000000000000000 ) ;
#19364=CARTESIAN_POINT ( 'NONE',  ( -4.350050802731187716, 2.983565686104819648, 0.3135853898029609677 ) ) ;
#19366=CARTESIAN_POINT ( 'NONE',  ( 7.249760686538667009, -7.530955069117495349, -2.741043480755002371 ) ) ;
#19369=AXIS2_PLACEMENT_3D ( 'NONE', #12763, #19816, #7783 ) ;
#19372=CARTESIAN_POINT ( 'NONE',  ( 3.499999999999999556, 6.704570150427012543, -2.172265885002588437 ) ) ;
#19377=CARTESIAN_POINT ( 'NONE',  ( -2.956376981307136553, 0.1572233378491263989, -2.999999999999999556 ) ) ;
#19380=DIRECTION ( 'NONE',  ( 1.000000000000000000, 0.000000000000000000, -0.000000000000000000 ) ) ;
#19382=CYLINDRICAL_SURFACE ( 'NONE', #31176, 2.999999999999999112 ) ;
#19384=DIRECTION ( 'NONE',  ( 0.000000000000000000, 0.2588190451025359495, -0.9659258262890643154 ) ) ;
#19385=EDGE_LOOP ( 'NONE', ( #17413, #21476, #3893 ) ) ;
#19387=EDGE_CURVE ( 'NONE', #24063, #4399, #8232, .T. ) ;
#19393=VECTOR ( 'NONE', #8982, 1000.000000000000000 ) ;
#19397=CARTESIAN_POINT ( 'NONE',  ( 4.749760686538667009, 1.391664247347333294, -7.892520144992419162 ) ) ;
#19401=CARTESIAN_POINT ( 'NONE',  ( 5.489344046532323773, -7.082516960462288402, -3.969101778623997046 ) ) ;
#19404=CARTESIAN_POINT ( 'NONE',  ( 6.356382399260308347, 3.797266095948589992, -7.723816458760309089 ) ) ;
#19406=CARTESIAN_POINT ( 'NONE',  ( -3.087550801365593234, 2.228590825266444142, 2.752080473201636845 ) ) ;
#19410=CARTESIAN_POINT ( 'NONE',  ( 6.038145208238973716, -7.104833038995682415, -4.620191422127199132 ) ) ;
#19411=EDGE_LOOP ( 'NONE', ( #7430, #13827, #8357, #13351 ) ) ;
#19413=CIRCLE ( 'NONE', #9247, 3.000000000000000444 ) ;
#19416=DIRECTION ( 'NONE',  ( 0.000000000000000000, -0.4067366430757887175, -0.9135454576426059736 ) ) ;
#19419=EDGE_CURVE ( 'NONE', #3811, #22609, #17290, .T. ) ;
#19423=CARTESIAN_POINT ( 'NONE',  ( -6.250050802731187183, -1.887961173149512062, -2.331437884370912261 ) ) ;
#19431=CARTESIAN_POINT ( 'NONE',  ( 4.749760686538667009, 4.007137495034812424, 6.940565734314612101 ) ) ;
#19434=CARTESIAN_POINT ( 'NONE',  ( 0.000000000000000000, 0.000000000000000000, 0.000000000000000000 ) ) ;
#19435=PLANE ( 'NONE',  #1161 ) ;
#19445=VERTEX_POINT ( 'NONE', #4421 ) ;
#19447=CARTESIAN_POINT ( 'NONE',  ( 6.357668022120091855, 5.959864878090759710, -6.210015626210324768 ) ) ;
#19453=CARTESIAN_POINT ( 'NONE',  ( 5.377543748152549874, -2.741043480754977946, 7.530955069117504230 ) ) ;
#19459=CARTESIAN_POINT ( 'NONE',  ( 7.249760686538667009, -7.135485519862032611, 5.064320921489797733 ) ) ;
#19464=AXIS2_PLACEMENT_3D ( 'NONE', #13294, #7965, #8136 ) ;
#19466=CARTESIAN_POINT ( 'NONE',  ( -6.450050800000000528, -1.549418761218565255, 2.853674364686380471 ) ) ;
#19474=EDGE_LOOP ( 'NONE', ( #3332, #16052, #26706 ) ) ;
#19480=DIRECTION ( 'NONE',  ( 0.000000000000000000, 0.000000000000000000, 1.000000000000000000 ) ) ;
#19484=ORIENTED_EDGE ( 'NONE', *, *, #22846, .T. ) ;
#19489=ORIENTED_EDGE ( 'NONE', *, *, #18207, .F. ) ;
#19492=CARTESIAN_POINT ( 'NONE',  ( 6.530491482054472385, 0.8857639883442899320, 8.615020591497804858 ) ) ;
#19502=CARTESIAN_POINT ( 'NONE',  ( -6.950050802731187360, 0.3135853898029611342, -2.983565686104819648 ) ) ;
#19504=CARTESIAN_POINT ( 'NONE',  ( -3.900050800000000706, -2.983565686104819648, -0.3135853898029605791 ) ) ;
#19521=EDGE_LOOP ( 'NONE', ( #18039, #16257, #26076 ) ) ;
#19522=EDGE_CURVE ( 'NONE', #1245, #24117, #28634, .T. ) ;
#19540=CARTESIAN_POINT ( 'NONE',  ( -6.654531657079158613, 2.846291840500173365, 1.545410377633946952 ) ) ;
#19550=EDGE_CURVE ( 'NONE', #3413, #4708, #14709, .T. ) ;
#19554=EDGE_LOOP ( 'NONE', ( #31931, #2494, #18720 ) ) ;
#19556=CARTESIAN_POINT ( 'NONE',  ( -2.662550801365593411, -3.521866450007987037, -0.3701630799359323931 ) ) ;
#19560=CARTESIAN_POINT ( 'NONE',  ( 6.524595551582239139, 3.779376390944578556, -7.790581746767696991 ) ) ;
#19561=VERTEX_POINT ( 'NONE', #29271 ) ;
#19562=CARTESIAN_POINT ( 'NONE',  ( -3.537550801365593411, -3.368539882008727115, -1.828967928396028064 ) ) ;
#19564=EDGE_CURVE ( 'NONE', #12129, #18566, #20709, .T. ) ;
#19565=DIRECTION ( 'NONE',  ( -1.000000000000000000, -0.000000000000000000, 0.000000000000000000 ) ) ;
#19569=VERTEX_POINT ( 'NONE', #31639 ) ;
#19579=CARTESIAN_POINT ( 'NONE',  ( -2.687550801365593323, -2.228590825266444586, -2.752080473201636401 ) ) ;
#19582=VERTEX_POINT ( 'NONE', #13871 ) ;
#19590=ORIENTED_EDGE ( 'NONE', *, *, #13624, .F. ) ;
#19591=CARTESIAN_POINT ( 'NONE',  ( 7.249760686538667009, 5.151476664237477188, 6.139290821770273077 ) ) ;
#19593=ORIENTED_EDGE ( 'NONE', *, *, #32476, .F. ) ;
#19597=CARTESIAN_POINT ( 'NONE',  ( 5.612974441954674987, 5.432722698947240580, -6.163896661468919014 ) ) ;
#19600=VERTEX_POINT ( 'NONE', #21264 ) ;
#19601=CARTESIAN_POINT ( 'NONE',  ( 5.489344046532323773, 4.149088721182530470, 6.978601450725500754 ) ) ;
#19609=CARTESIAN_POINT ( 'NONE',  ( 6.530491627857225367, -2.368289848745700699, -8.330327812606284965 ) ) ;
#19610=CARTESIAN_POINT ( 'NONE',  ( 3.499999999999999556, 5.241389472434663688, 4.711457988287072851 ) ) ;
#19613=CARTESIAN_POINT ( 'NONE',  ( 3.499999999999999556, -7.009698679648292519, 3.730838147389666126 ) ) ;
#19616=CARTESIAN_POINT ( 'NONE',  ( 6.038145208238977268, -4.620191422127173375, 7.104833038995700178 ) ) ;
#19623=VERTEX_POINT ( 'NONE', #26292 ) ;
#19625=EDGE_CURVE ( 'NONE', #33011, #6174, #26461, .T. ) ;
#19634=EDGE_CURVE ( 'NONE', #29013, #31514, #2498, .T. ) ;
#19637=VERTEX_POINT ( 'NONE', #32316 ) ;
#19642=DIRECTION ( 'NONE',  ( -1.000000000000000000, -0.000000000000000000, -0.000000000000000000 ) ) ;
#19650=CARTESIAN_POINT ( 'NONE',  ( 3.499999999999999556, -1.471047635026914380, 6.892461014225956362 ) ) ;
#19652=EDGE_CURVE ( 'NONE', #14402, #11109, #23456, .T. ) ;
#19653=DIRECTION ( 'NONE',  ( -1.000000000000000000, -0.000000000000000000, -0.000000000000000000 ) ) ;
#19658=CARTESIAN_POINT ( 'NONE',  ( -4.400050802731188426, 3.113457007523260156, -0.9222479816126439855 ) ) ;
#19660=CARTESIAN_POINT ( 'NONE',  ( -3.400050800000000262, 1.887961173149511618, 2.331437884370912705 ) ) ;
#19662=CARTESIAN_POINT ( 'NONE',  ( -4.112942406915325755, -5.022711880624455567E-15, 2.999999999999999556 ) ) ;
#19670=CARTESIAN_POINT ( 'NONE',  ( -2.800050800000000173, 2.331437884370912705, -1.887961173149511618 ) ) ;
#19677=VERTEX_POINT ( 'NONE', #11899 ) ;
#19678=DIRECTION ( 'NONE',  ( 0.000000000000000000, 0.000000000000000000, 1.000000000000000000 ) ) ;
#19683=CARTESIAN_POINT ( 'NONE',  ( 5.377543748152548986, -8.014274990069656823, 8.669741416787380218E-17 ) ) ;
#19685=LINE ( 'NONE', #14665, #11867 ) ;
#19686=DIRECTION ( 'NONE',  ( 0.000000000000000000, 0.000000000000000000, 1.000000000000000000 ) ) ;
#19688=CARTESIAN_POINT ( 'NONE',  ( 7.064423539573518873, 0.7071067811875524356, 8.721381771257245674 ) ) ;
#19693=CARTESIAN_POINT ( 'NONE',  ( 6.530491627857225367, 2.368289848745754878, 8.330327812606270754 ) ) ;
#19694=ORIENTED_EDGE ( 'NONE', *, *, #8796, .F. ) ;
#19695=CARTESIAN_POINT ( 'NONE',  ( -6.154531657079158613, -0.9198621039125872700, -3.105402419394638791 ) ) ;
#19697=DIRECTION ( 'NONE',  ( 0.000000000000000000, 0.000000000000000000, -1.000000000000000000 ) ) ;
#19698=LINE ( 'NONE', #19875, #14578 ) ;
#19701=EDGE_CURVE ( 'NONE', #20949, #33059, #27889, .T. ) ;
#19712=VERTEX_POINT ( 'NONE', #29628 ) ;
#19714=CARTESIAN_POINT ( 'NONE',  ( -2.562550801365592879, -2.228590825266444586, -2.752080473201636401 ) ) ;
#19719=CARTESIAN_POINT ( 'NONE',  ( -4.137550801365594388, 1.828967928396027176, -3.368539882008727115 ) ) ;
#19720=CARTESIAN_POINT ( 'NONE',  ( 3.499999999999999556, -6.700937042937042065, -2.183447440113257976 ) ) ;
#19728=DIRECTION ( 'NONE',  ( 0.000000000000000000, 0.000000000000000000, 1.000000000000000000 ) ) ;
#19759=CYLINDRICAL_SURFACE ( 'NONE', #13329, 8.500000000000000000 ) ;
#19768=DIRECTION ( 'NONE',  ( -1.000000000000000000, -0.000000000000000000, 0.000000000000000000 ) ) ;
#19770=AXIS2_PLACEMENT_3D ( 'NONE', #25522, #7813, #15316 ) ;
#19772=CARTESIAN_POINT ( 'NONE',  ( 3.499999999999999556, 8.357095590591338663, 1.552080310331533486 ) ) ;
#19773=EDGE_CURVE ( 'NONE', #3605, #31514, #33092, .T. ) ;
#19776=CARTESIAN_POINT ( 'NONE',  ( -5.687550801365593323, 2.752080473201636845, -2.228590825266444142 ) ) ;
#19786=AXIS2_PLACEMENT_3D ( 'NONE', #30046, #29355, #29708 ) ;
#19790=CARTESIAN_POINT ( 'NONE',  ( 7.249760686538667009, -8.711672189281431500, 0.8180878109961559064 ) ) ;
#19796=ORIENTED_EDGE ( 'NONE', *, *, #10816, .T. ) ;
#19816=DIRECTION ( 'NONE',  ( 1.000000000000000000, 0.000000000000000000, 0.000000000000000000 ) ) ;
#19817=AXIS2_PLACEMENT_3D ( 'NONE', #7683, #7334, #27719 ) ;
#19821=CARTESIAN_POINT ( 'NONE',  ( -2.900050802731187094, 1.549418761218566143, -2.853674364686379583 ) ) ;
#19823=CARTESIAN_POINT ( 'NONE',  ( -4.300050800000000173, 2.983565686104819648, 0.3135853898029609677 ) ) ;
#19825=DIRECTION ( 'NONE',  ( 0.000000000000000000, 0.9659258262890703106, -0.2588190451025135785 ) ) ;
#19826=CARTESIAN_POINT ( 'NONE',  ( -4.400050799999999818, 2.331437884370912705, -1.887961173149511618 ) ) ;
#19828=DIRECTION ( 'NONE',  ( 0.000000000000000000, -0.2079116908177663092, 0.9781476007338040235 ) ) ;
#19834=VERTEX_POINT ( 'NONE', #15286 ) ;
#19839=VERTEX_POINT ( 'NONE', #30709 ) ;
#19845=DIRECTION ( 'NONE',  ( -1.000000000000000000, 0.000000000000000000, 0.000000000000000000 ) ) ;
#19857=PLANE ( 'NONE',  #27297 ) ;
#19860=B_SPLINE_CURVE_WITH_KNOTS ( 'NONE', 3,
 ( #30157, #14579, #30305, #4882, #25280, #2396, #32152, #24782, #11917, #19453 ),
 .UNSPECIFIED., .F., .F.,
 ( 4, 2, 2, 2, 4 ),
 ( 1.968338519012340724E-07, 0.0005467927057105483133, 0.001093388577569195420, 0.001639984449427842527, 0.002186580321286489634 ),
 .UNSPECIFIED. ) ;
#19861=DIRECTION ( 'NONE',  ( 0.000000000000000000, 0.000000000000000000, -1.000000000000000000 ) ) ;
#19862=CARTESIAN_POINT ( 'NONE',  ( 4.749760686538667009, -6.940565734314570356, -4.007137495034885255 ) ) ;
#19864=CARTESIAN_POINT ( 'NONE',  ( 4.749760686538667009, -7.530955069117495349, -2.741043480755002371 ) ) ;
#19868=ORIENTED_EDGE ( 'NONE', *, *, #11152, .T. ) ;
#19869=VECTOR ( 'NONE', #21327, 1000.000000000000000 ) ;
#19871=CARTESIAN_POINT ( 'NONE',  ( -7.354531657079157903, 0.9198621039125853827, 3.105402419394639235 ) ) ;
#19873=B_SPLINE_CURVE_WITH_KNOTS ( 'NONE', 3,
 ( #25362, #10304, #7805, #15653, #25864, #2981, #23337, #441, #8121, #15812, #27851, #15154, #6415, #21168, #23490 ),
 .UNSPECIFIED., .F., .F.,
 ( 4, 2, 2, 2, 1, 2, 2, 4 ),
 ( 0.000000000000000000, 0.2500000000000000000, 0.3750000000000000000, 0.5000000000000001110, 0.6250000000000000000, 0.6875000000000000000, 0.7500000000000000000, 1.000000000000000000 ),
 .UNSPECIFIED. ) ;
#19875=CARTESIAN_POINT ( 'NONE',  ( -8.000050800000000351, 0.000000000000000000, -3.000000000000000444 ) ) ;
#19878=VERTEX_POINT ( 'NONE', #18138 ) ;
#19886=CARTESIAN_POINT ( 'NONE',  ( 6.357667975083867162, 4.790963222208105776, -7.150591204917344790 ) ) ;
#19888=CARTESIAN_POINT ( 'NONE',  ( 6.038145208238974604, 3.842870190353700810, 7.553619661406923314 ) ) ;
#19890=AXIS2_PLACEMENT_3D ( 'NONE', #27512, #16963, #24651 ) ;
#19891=ORIENTED_EDGE ( 'NONE', *, *, #13079, .F. ) ;
#19901=CARTESIAN_POINT ( 'NONE',  ( -3.037550801365593411, 1.088641768524161613, 3.675193018007247403 ) ) ;
#19908=EDGE_CURVE ( 'NONE', #13197, #12969, #13303, .T. ) ;
#19911=EDGE_CURVE ( 'NONE', #19677, #24063, #17581, .T. ) ;
#19921=VECTOR ( 'NONE', #12854, 1000.000000000000000 ) ;
#19933=ORIENTED_EDGE ( 'NONE', *, *, #29795, .T. ) ;
#19946=CARTESIAN_POINT ( 'NONE',  ( 5.885541806331895387, 4.514241479885547470, 7.076443837533973991 ) ) ;
#19948=CIRCLE ( 'NONE', #3926, 5.500000000000000000 ) ;
#19949=VECTOR ( 'NONE', #31242, 1000.000000000000114 ) ;
#19967=DIRECTION ( 'NONE',  ( -1.000000000000000000, 0.000000000000000000, 0.000000000000000000 ) ) ;
#19968=CARTESIAN_POINT ( 'NONE',  ( -7.037550801365593856, 1.088641768524161613, 3.675193018007246959 ) ) ;
#19970=VECTOR ( 'NONE', #31523, 1000.000000000000000 ) ;
#19971=CARTESIAN_POINT ( 'NONE',  ( -10.00000000000000000, 0.000000000000000000, 0.000000000000000000 ) ) ;
#19987=DIRECTION ( 'NONE',  ( 0.000000000000000000, 0.000000000000000000, -1.000000000000000000 ) ) ;
#19988=ADVANCED_FACE ( 'NONE', ( #11108 ), #23964, .F. ) ;
#19997=EDGE_CURVE ( 'NONE', #32892, #22736, #11706, .T. ) ;
#20005=CIRCLE ( 'NONE', #1035, 8.500000000000000000 ) ;
#20007=CARTESIAN_POINT ( 'NONE',  ( -3.600050802731187272, 3.113457007523260156, -0.9222479816126439855 ) ) ;
#20008=ORIENTED_EDGE ( 'NONE', *, *, #11645, .T. ) ;
#20010=CARTESIAN_POINT ( 'NONE',  ( -2.650050800000000262, 2.853674364686379583, 1.549418761218565921 ) ) ;
#20013=CARTESIAN_POINT ( 'NONE',  ( -4.506376978575949543, 0.1572233378491263989, -2.999999999999999556 ) ) ;
#20018=ORIENTED_EDGE ( 'NONE', *, *, #837, .T. ) ;
#20023=ORIENTED_EDGE ( 'NONE', *, *, #29041, .F. ) ;
#20029=CARTESIAN_POINT ( 'NONE',  ( 3.499999999999999556, -6.200809695932770538, -0.7745709230445805282 ) ) ;
#20035=DIRECTION ( 'NONE',  ( -0.000000000000000000, 0.5735764363510439390, 0.8191520442889932418 ) ) ;
#20042=DIRECTION ( 'NONE',  ( -1.000000000000000000, -0.000000000000000000, 0.000000000000000000 ) ) ;
#20043=LINE ( 'NONE', #32068, #13959 ) ;
#20046=ORIENTED_EDGE ( 'NONE', *, *, #13088, .T. ) ;
#20047=CARTESIAN_POINT ( 'NONE',  ( -7.362550801365593145, -2.228590825266444586, -2.752080473201636401 ) ) ;
#20050=CARTESIAN_POINT ( 'NONE',  ( -6.904531657079157725, 0.3127741368606810068, -2.975847129947406522 ) ) ;
#20051=DIRECTION ( 'NONE',  ( -1.000000000000000000, 0.000000000000000000, -0.000000000000000000 ) ) ;
#20055=CARTESIAN_POINT ( 'NONE',  ( 3.499999999999999556, 0.000000000000000000, 0.000000000000000000 ) ) ;
#20057=CARTESIAN_POINT ( 'NONE',  ( 6.356382477965130562, -5.080803740829769488, 6.947086032709915315 ) ) ;
#20062=CARTESIAN_POINT ( 'NONE',  ( 3.499999999999999556, 0.000000000000000000, 0.000000000000000000 ) ) ;
#20064=VERTEX_POINT ( 'NONE', #32186 ) ;
#20066=CARTESIAN_POINT ( 'NONE',  ( 7.249760686538667009, 0.000000000000000000, 0.000000000000000000 ) ) ;
#20070=CARTESIAN_POINT ( 'NONE',  ( 6.038144853276843804, 8.412419482080421673, -1.027626812407915313 ) ) ;
#20072=CARTESIAN_POINT ( 'NONE',  ( -7.812550801365593323, 3.368539882008727115, 1.828967928396026954 ) ) ;
#20078=ORIENTED_EDGE ( 'NONE', *, *, #27716, .F. ) ;
#20079=EDGE_CURVE ( 'NONE', #14801, #13430, #19090, .T. ) ;
#20090=DIRECTION ( 'NONE',  ( -0.000000000000000000, -0.5735764363510496011, -0.8191520442889893561 ) ) ;
#20093=DIRECTION ( 'NONE',  ( -1.000000000000000000, -0.000000000000000000, -0.000000000000000000 ) ) ;
#20095=DIRECTION ( 'NONE',  ( 0.000000000000000000, 0.000000000000000000, 1.000000000000000000 ) ) ;
#20096=ORIENTED_EDGE ( 'NONE', *, *, #5273, .F. ) ;
#20097=EDGE_CURVE ( 'NONE', #4314, #32347, #3188, .T. ) ;
#20100=LINE ( 'NONE', #19591, #20461 ) ;
#20101=EDGE_CURVE ( 'NONE', #20892, #3605, #4591, .T. ) ;
#20116=CARTESIAN_POINT ( 'NONE',  ( 7.249760686538667009, 8.721381771256204729, 0.7071067811865429098 ) ) ;
#20123=DIRECTION ( 'NONE',  ( 0.000000000000000000, 0.9063077870366477162, 0.4226182617407044928 ) ) ;
#20124=FACE_OUTER_BOUND ( 'NONE', #22835, .T. ) ;
#20125=CARTESIAN_POINT ( 'NONE',  ( -6.087550801365593678, -2.752080473201636845, 2.228590825266444586 ) ) ;
#20126=ORIENTED_EDGE ( 'NONE', *, *, #2054, .F. ) ;
#20127=B_SPLINE_CURVE_WITH_KNOTS ( 'NONE', 3,
 ( #10934, #20968, #28654, #8413 ),
 .UNSPECIFIED., .F., .F.,
 ( 4, 4 ),
 ( 0.9237604347401378035, 1.000000000000000000 ),
 .UNSPECIFIED. ) ;
#20129=CARTESIAN_POINT ( 'NONE',  ( 5.377543748152548986, -7.530955069117495349, -2.741043480755002371 ) ) ;
#20130=CARTESIAN_POINT ( 'NONE',  ( 0.000000000000000000, 0.000000000000000000, 0.000000000000000000 ) ) ;
#20131=ORIENTED_EDGE ( 'NONE', *, *, #24722, .T. ) ;
#20133=ADVANCED_FACE ( 'NONE', ( #14109 ), #16942, .T. ) ;
#20137=EDGE_LOOP ( 'NONE', ( #12202, #22576, #27419 ) ) ;
#20146=ORIENTED_EDGE ( 'NONE', *, *, #5403, .T. ) ;
#20147=CARTESIAN_POINT ( 'NONE',  ( -5.550050800000001061, -3.113457007523259268, 0.9222479816126455399 ) ) ;
#20157=CARTESIAN_POINT ( 'NONE',  ( -3.450050802731187805, 1.887961173149511618, 2.331437884370912705 ) ) ;
#20158=VERTEX_POINT ( 'NONE', #12595 ) ;
#20159=CARTESIAN_POINT ( 'NONE',  ( -3.150050800000000262, -3.113457007523259268, 0.9222479816126455399 ) ) ;
#20162=DIRECTION ( 'NONE',  ( -1.000000000000000000, 0.000000000000000000, 0.000000000000000000 ) ) ;
#20164=CARTESIAN_POINT ( 'NONE',  ( 3.499999999999999556, -5.349675154362298457, -3.229702268444986757 ) ) ;
#20175=DIRECTION ( 'NONE',  ( -1.000000000000000000, 0.000000000000000000, 0.000000000000000000 ) ) ;
#20184=LINE ( 'NONE', #23199, #11764 ) ;
#20185=CARTESIAN_POINT ( 'NONE',  ( -4.162942409646514186, -5.022711880624455567E-15, 2.999999999999999556 ) ) ;
#20190=DIRECTION ( 'NONE',  ( -1.000000000000000000, 0.000000000000000000, 0.000000000000000000 ) ) ;
#20195=CARTESIAN_POINT ( 'NONE',  ( -5.862550801365593145, -3.521866450007987037, -0.3701630799359323931 ) ) ;
#20197=CARTESIAN_POINT ( 'NONE',  ( -5.604531657079157903, -2.325406398514293205, 1.883076972206379818 ) ) ;
#20208=CARTESIAN_POINT ( 'NONE',  ( 5.489343806296448136, -1.512045527216150598, -7.976812024616041441 ) ) ;
#20211=CARTESIAN_POINT ( 'NONE',  ( 5.377543748152549874, 4.007137495034909236, -6.940565734314555257 ) ) ;
#20213=CARTESIAN_POINT ( 'NONE',  ( 5.377543748152548098, 8.385837730238846314E-14, -8.014274990069656823 ) ) ;
#20215=CARTESIAN_POINT ( 'NONE',  ( -8.000050800000002127, -2.890068019510989572, 0.8529434025099479344 ) ) ;
#20222=CARTESIAN_POINT ( 'NONE',  ( -4.612550801365593145, 3.368539882008727115, 1.828967928396026954 ) ) ;
#20229=DIRECTION ( 'NONE',  ( -1.000000000000000000, -0.000000000000000000, -0.000000000000000000 ) ) ;
#20235=EDGE_CURVE ( 'NONE', #3680, #26986, #33004, .T. ) ;
#20238=ORIENTED_EDGE ( 'NONE', *, *, #8796, .T. ) ;
#20243=ORIENTED_EDGE ( 'NONE', *, *, #21351, .T. ) ;
#20245=CARTESIAN_POINT ( 'NONE',  ( 0.000000000000000000, -3.573533178329615367, 5.126388750707211450 ) ) ;
#20246=ORIENTED_EDGE ( 'NONE', *, *, #15349, .F. ) ;
#20252=CARTESIAN_POINT ( 'NONE',  ( -7.362550801365593145, -2.228590825266444586, -2.752080473201636401 ) ) ;
#20265=VERTEX_POINT ( 'NONE', #30182 ) ;
#20271=CARTESIAN_POINT ( 'NONE',  ( 6.037141752603385036, 8.462586328878536790, -0.4483113388088767470 ) ) ;
#20273=ORIENTED_EDGE ( 'NONE', *, *, #19652, .F. ) ;
#20276=CARTESIAN_POINT ( 'NONE',  ( -7.337550801365593678, 1.828967928396027398, -3.368539882008727115 ) ) ;
#20278=VECTOR ( 'NONE', #7100, 1000.000000000000000 ) ;
#20289=ORIENTED_EDGE ( 'NONE', *, *, #2436, .F. ) ;
#20311=DIRECTION ( 'NONE',  ( 0.000000000000000000, -0.4067366430757887730, -0.9135454576426058626 ) ) ;
#20314=VECTOR ( 'NONE', #30220, 999.9999999999998863 ) ;
#20315=CARTESIAN_POINT ( 'NONE',  ( 3.499999999999999556, -1.471047635026823786, -6.892461014225975013 ) ) ;
#20316=CARTESIAN_POINT ( 'NONE',  ( -2.950050802731187360, 0.3135853898029611342, -2.983565686104819648 ) ) ;
#20318=CARTESIAN_POINT ( 'NONE',  ( -4.387550801365594388, -3.521866450007987037, -0.3701630799359323931 ) ) ;
#20320=AXIS2_PLACEMENT_3D ( 'NONE', #21884, #6999, #16529 ) ;
#20324=CARTESIAN_POINT ( 'NONE',  ( 5.489321708267612898, -5.138670926724855370, -6.285661071314523340 ) ) ;
#20325=AXIS2_PLACEMENT_3D ( 'NONE', #27988, #15096, #25313 ) ;
#20333=ORIENTED_EDGE ( 'NONE', *, *, #3519, .F. ) ;
#20335=LINE ( 'NONE', #17642, #32590 ) ;
#20357=CARTESIAN_POINT ( 'NONE',  ( -7.412550801365592967, -3.368539882008727115, -1.828967928396028064 ) ) ;
#20359=CARTESIAN_POINT ( 'NONE',  ( -4.604531657079157014, -1.883076972206379818, -2.325406398514292761 ) ) ;
#20362=DIRECTION ( 'NONE',  ( 0.000000000000000000, 0.7071067811865507924, 0.7071067811865441310 ) ) ;
#20368=AXIS2_PLACEMENT_3D ( 'NONE', #14816, #28047, #20533 ) ;
#20371=ORIENTED_EDGE ( 'NONE', *, *, #41, .T. ) ;
#20372=CARTESIAN_POINT ( 'NONE',  ( 5.885541615502093649, 1.821712961073348014, 8.193643496140859739 ) ) ;
#20377=LINE ( 'NONE', #7482, #15498 ) ;
#20388=CARTESIAN_POINT ( 'NONE',  ( -6.712550801365593678, -3.675193018007246071, 1.088641768524163167 ) ) ;
#20394=ORIENTED_EDGE ( 'NONE', *, *, #8993, .T. ) ;
#20396=ORIENTED_EDGE ( 'NONE', *, *, #12628, .F. ) ;
#20397=VECTOR ( 'NONE', #27695, 1000.000000000000114 ) ;
#20398=CIRCLE ( 'NONE', #24639, 8.750000000000000000 ) ;
#20407=VECTOR ( 'NONE', #4518, 999.9999999999998863 ) ;
#20409=DIRECTION ( 'NONE',  ( 1.000000000000000000, -0.000000000000000000, 0.000000000000000000 ) ) ;
#20418=CIRCLE ( 'NONE', #10866, 8.500000000000000000 ) ;
#20419=VERTEX_POINT ( 'NONE', #18596 ) ;
#20429=CARTESIAN_POINT ( 'NONE',  ( -7.212550801365594566, 1.828967928396027398, -3.368539882008727115 ) ) ;
#20430=CARTESIAN_POINT ( 'NONE',  ( 7.064632918400242545, -8.437262856154175594, 2.318425219014201843 ) ) ;
#20434=ORIENTED_EDGE ( 'NONE', *, *, #9493, .F. ) ;
#20449=AXIS2_PLACEMENT_3D ( 'NONE', #3030, #2680, #15861 ) ;
#20450=FACE_OUTER_BOUND ( 'NONE', #3143, .T. ) ;
#20451=VECTOR ( 'NONE', #16050, 1000.000000000000000 ) ;
#20452=CARTESIAN_POINT ( 'NONE',  ( 5.377543748152548986, 8.014274990069656823, -8.669741416787380218E-17 ) ) ;
#20455=CARTESIAN_POINT ( 'NONE',  ( 7.249760686538667009, 7.892520144992453801, -1.391664247347147443 ) ) ;
#20457=CIRCLE ( 'NONE', #18850, 2.999999999999999556 ) ;
#20459=CARTESIAN_POINT ( 'NONE',  ( -5.837550801365592790, -1.088641768524163611, -3.675193018007245627 ) ) ;
#20461=VECTOR ( 'NONE', #32139, 1000.000000000000000 ) ;
#20468=ORIENTED_EDGE ( 'NONE', *, *, #10979, .F. ) ;
#20479=VECTOR ( 'NONE', #8347, 1000.000000000000114 ) ;
#20483=CARTESIAN_POINT ( 'NONE',  ( 5.885541806331895387, -7.076443837533989090, 4.514241479885522601 ) ) ;
#20486=CARTESIAN_POINT ( 'NONE',  ( -5.650050800000001594, -1.549418761218565255, 2.853674364686380471 ) ) ;
#20489=DIRECTION ( 'NONE',  ( 0.000000000000000000, -0.08715574274766962892, 0.9961946980917446570 ) ) ;
#20490=CARTESIAN_POINT ( 'NONE',  ( 0.000000000000000000, 0.000000000000000000, 6.000000000000000000 ) ) ;
#20491=CARTESIAN_POINT ( 'NONE',  ( 7.064632816082964339, 8.721381771256204729, 0.7071067811865412445 ) ) ;
#20499=VECTOR ( 'NONE', #14498, 1000.000000000000000 ) ;
#20501=CARTESIAN_POINT ( 'NONE',  ( -3.700050802731187805, 1.549418761218566143, -2.853674364686379583 ) ) ;
#20503=TOROIDAL_SURFACE ( 'NONE', #8739, 5.500000000000000000, 0.5000000000000000000 ) ;
#20504=CARTESIAN_POINT ( 'NONE',  ( -5.537550801365594744, 3.368539882008727115, 1.828967928396026954 ) ) ;
#20507=CARTESIAN_POINT ( 'NONE',  ( 6.749760686538667009, 6.735557395310442023E-16, -5.500000000000000000 ) ) ;
#20509=EDGE_LOOP ( 'NONE', ( #14160, #2940, #9060, #28097 ) ) ;
#20515=VERTEX_POINT ( 'NONE', #28486 ) ;
#20521=AXIS2_PLACEMENT_3D ( 'NONE', #6306, #1328, #8972 ) ;
#20532=CARTESIAN_POINT ( 'NONE',  ( 7.249760686538667009, -8.014274990069656823, 8.669741416787380218E-17 ) ) ;
#20533=DIRECTION ( 'NONE',  ( 0.000000000000000000, 0.9659258262890678681, 0.2588190451025219052 ) ) ;
#20536=CARTESIAN_POINT ( 'NONE',  ( -7.998722633285748174, -2.371517779863575370, 1.837526800715260533 ) ) ;
#20541=CARTESIAN_POINT ( 'NONE',  ( -7.662550801365593856, -0.3701630799359326152, 3.521866450007987037 ) ) ;
#20542=VERTEX_POINT ( 'NONE', #30052 ) ;
#20543=CARTESIAN_POINT ( 'NONE',  ( -3.054531657079158080, -2.846291840500172921, -1.545410377633947618 ) ) ;
#20552=ORIENTED_EDGE ( 'NONE', *, *, #1402, .T. ) ;
#20558=DIRECTION ( 'NONE',  ( 0.000000000000000000, 0.000000000000000000, 1.000000000000000000 ) ) ;
#20559=DIRECTION ( 'NONE',  ( 0.000000000000000000, -0.8660254037844433705, 0.4999999999999920064 ) ) ;
#20560=CARTESIAN_POINT ( 'NONE',  ( 6.880159329304569304, 7.110803091624058325, 5.066480354148957588 ) ) ;
#20561=ORIENTED_EDGE ( 'NONE', *, *, #21077, .F. ) ;
#20565=DIRECTION ( 'NONE',  ( 0.000000000000000000, 0.2079116908177532363, 0.9781476007338069101 ) ) ;
#20569=CARTESIAN_POINT ( 'NONE',  ( -6.062550801365593323, -0.3701630799359326152, 3.521866450007987037 ) ) ;
#20572=LINE ( 'NONE', #22387, #25145 ) ;
#20573=EDGE_LOOP ( 'NONE', ( #17240, #15548, #4854, #25575 ) ) ;
#20575=CARTESIAN_POINT ( 'NONE',  ( 7.249760686538667009, -6.139290821770289064, 5.151476664237455871 ) ) ;
#20595=EDGE_LOOP ( 'NONE', ( #15608, #30938, #7009 ) ) ;
#20596=EDGE_CURVE ( 'NONE', #9165, #14302, #5133, .T. ) ;
#20599=CARTESIAN_POINT ( 'NONE',  ( -7.912550801365592967, 3.675193018007246959, -1.088641768524161391 ) ) ;
#20601=DIRECTION ( 'NONE',  ( 0.000000000000000000, 0.8191520442889936859, -0.5735764363510434949 ) ) ;
#20602=CARTESIAN_POINT ( 'NONE',  ( 0.000000000000000000, -4.724769925181202979, 4.089810527897742354 ) ) ;
#20616=EDGE_CURVE ( 'NONE', #21332, #10245, #9601, .T. ) ;
#20618=CARTESIAN_POINT ( 'NONE',  ( 6.524594682510452159, 8.636529731786344755, -0.6222547417166852668 ) ) ;
#20621=DIRECTION ( 'NONE',  ( 0.000000000000000000, 0.9945218953682734009, 0.1045284632676534292 ) ) ;
#20623=LINE ( 'NONE', #15761, #17754 ) ;
#20626=CYLINDRICAL_SURFACE ( 'NONE', #29472, 8.500000000000000000 ) ;
#20627=LINE ( 'NONE', #7396, #5565 ) ;
#20631=EDGE_CURVE ( 'NONE', #12982, #15020, #20335, .T. ) ;
#20634=ORIENTED_EDGE ( 'NONE', *, *, #15787, .T. ) ;
#20640=EDGE_CURVE ( 'NONE', #28881, #6649, #11734, .T. ) ;
#20641=ORIENTED_EDGE ( 'NONE', *, *, #5236, .F. ) ;
#20647=CARTESIAN_POINT ( 'NONE',  ( 7.249760686538667009, 0.000000000000000000, 0.000000000000000000 ) ) ;
#20649=DIRECTION ( 'NONE',  ( 0.000000000000000000, 0.000000000000000000, 1.000000000000000000 ) ) ;
#20650=DIRECTION ( 'NONE',  ( -1.000000000000000000, -0.000000000000000000, -0.000000000000000000 ) ) ;
#20658=CYLINDRICAL_SURFACE ( 'NONE', #20970, 2.999999999999998224 ) ;
#20660=DIRECTION ( 'NONE',  ( 0.000000000000000000, -0.4226182617406868403, -0.9063077870366558209 ) ) ;
#20663=CARTESIAN_POINT ( 'NONE',  ( -7.287550801365593856, 2.752080473201636845, -2.228590825266444142 ) ) ;
#20666=EDGE_CURVE ( 'NONE', #30035, #16750, #19873, .T. ) ;
#20679=ORIENTED_EDGE ( 'NONE', *, *, #447, .F. ) ;
#20680=DIRECTION ( 'NONE',  ( -1.000000000000000000, -0.000000000000000000, -0.000000000000000000 ) ) ;
#20681=CARTESIAN_POINT ( 'NONE',  ( 3.499999999999999556, 0.000000000000000000, 0.000000000000000000 ) ) ;
#20685=DIRECTION ( 'NONE',  ( 0.000000000000000000, 0.000000000000000000, 1.000000000000000000 ) ) ;
#20687=EDGE_CURVE ( 'NONE', #4862, #14011, #26650, .T. ) ;
#20690=CARTESIAN_POINT ( 'NONE',  ( 5.885541838704149598, -6.185046950422357526, 5.674471607902420445 ) ) ;
#20697=CARTESIAN_POINT ( 'NONE',  ( 7.064423669210277978, -7.135485519863427051, -5.064320921489765759 ) ) ;
#20699=CARTESIAN_POINT ( 'NONE',  ( -6.562550801365594211, -2.228590825266444586, -2.752080473201636401 ) ) ;
#20701=ADVANCED_FACE ( 'NONE', ( #13770 ), #31703, .F. ) ;
#20702=CARTESIAN_POINT ( 'NONE',  ( -4.454531657079158435, 1.545410377633947174, -2.846291840500173365 ) ) ;
#20709=B_SPLINE_CURVE_WITH_KNOTS ( 'NONE', 3,
 ( #8876, #3403, #24265, #11219, #19084, #5730, #3559, #3224, #1030, #3883 ),
 .UNSPECIFIED., .F., .F.,
 ( 4, 2, 2, 2, 4 ),
 ( 3.032460776717885298E-07, 0.0005479053915603964179, 0.001095507537043121033, 0.001643109682525845322, 0.002190711828008569829 ),
 .UNSPECIFIED. ) ;
#20710=ORIENTED_EDGE ( 'NONE', *, *, #31204, .F. ) ;
#20715=LINE ( 'NONE', #25901, #22514 ) ;
#20718=CARTESIAN_POINT ( 'NONE',  ( -8.000050800000002127, -2.895451290119166021, -0.7990719894741236118 ) ) ;
#20724=CARTESIAN_POINT ( 'NONE',  ( -6.312550801365593323, 3.675193018007247403, -1.088641768524161391 ) ) ;
#20731=CYLINDRICAL_SURFACE ( 'NONE', #6382, 8.500000000000000000 ) ;
#20746=CARTESIAN_POINT ( 'NONE',  ( -4.962942409646514008, 3.284080845023683730E-15, 3.000000000000000000 ) ) ;
#20751=CARTESIAN_POINT ( 'NONE',  ( -6.012550801365594388, -1.828967928396026732, 3.368539882008728004 ) ) ;
#20752=CARTESIAN_POINT ( 'NONE',  ( 7.249760686538667009, 6.139290821770257089, 5.151476664237498504 ) ) ;
#20771=EDGE_LOOP ( 'NONE', ( #7090, #10099, #27164, #14550 ) ) ;
#20772=FACE_OUTER_BOUND ( 'NONE', #15726, .T. ) ;
#20786=ORIENTED_EDGE ( 'NONE', *, *, #31075, .T. ) ;
#20787=CARTESIAN_POINT ( 'NONE',  ( 5.885541806331895387, -4.514241479885499508, -7.076443837534005077 ) ) ;
#20796=CARTESIAN_POINT ( 'NONE',  ( 3.499999999999999556, 6.100541242131516384, -3.528937025535512362 ) ) ;
#20797=CARTESIAN_POINT ( 'NONE',  ( 0.000000000000000000, -2.861184399891040009, 6.440778198864103743 ) ) ;
#20805=CIRCLE ( 'NONE', #26657, 8.500000000000000000 ) ;
#20816=VECTOR ( 'NONE', #17048, 1000.000000000000227 ) ;
#20821=ORIENTED_EDGE ( 'NONE', *, *, #13035, .F. ) ;
#20830=LINE ( 'NONE', #25676, #28261 ) ;
#20833=ORIENTED_EDGE ( 'NONE', *, *, #10592, .T. ) ;
#20835=CARTESIAN_POINT ( 'NONE',  ( -4.050050800000001061, -1.549418761218565255, 2.853674364686380471 ) ) ;
#20838=CARTESIAN_POINT ( 'NONE',  ( 3.499999999999999556, -1.179494851233859887, -6.136676046192499179 ) ) ;
#20841=VECTOR ( 'NONE', #20035, 1000.000000000000000 ) ;
#20843=CARTESIAN_POINT ( 'NONE',  ( -7.050050802731187893, -1.887961173149512062, -2.331437884370912261 ) ) ;
#20844=DIRECTION ( 'NONE',  ( -1.000000000000000000, -0.000000000000000000, -0.000000000000000000 ) ) ;
#20847=CARTESIAN_POINT ( 'NONE',  ( -3.112550801365593145, 3.675193018007247403, -1.088641768524161391 ) ) ;
#20848=ORIENTED_EDGE ( 'NONE', *, *, #19701, .F. ) ;
#20849=CARTESIAN_POINT ( 'NONE',  ( -4.854531657079157903, -1.545410377633946286, 2.846291840500174697 ) ) ;
#20850=CIRCLE ( 'NONE', #19770, 6.000000000000000000 ) ;
#20852=CARTESIAN_POINT ( 'NONE',  ( -5.150050800000000706, 3.113457007523260156, -0.9222479816126439855 ) ) ;
#20856=EDGE_CURVE ( 'NONE', #14011, #19637, #5098, .T. ) ;
#20857=ORIENTED_EDGE ( 'NONE', *, *, #10999, .T. ) ;
#20861=AXIS2_PLACEMENT_3D ( 'NONE', #14020, #29593, #1167 ) ;
#20875=CARTESIAN_POINT ( 'NONE',  ( -7.362550801365593145, -2.228590825266444586, -2.752080473201636401 ) ) ;
#20877=DIRECTION ( 'NONE',  ( -0.000000000000000000, 0.9961946980917458783, -0.08715574274765452989 ) ) ;
#20880=EDGE_LOOP ( 'NONE', ( #16868, #8519, #18686, #15413, #3627, #18841, #15358, #6255 ) ) ;
#20882=CARTESIAN_POINT ( 'NONE',  ( 4.749760686538667009, -6.139290821770219786, -5.151476664237539360 ) ) ;
#20885=CIRCLE ( 'NONE', #13388, 2.999999999999999112 ) ;
#20892=VERTEX_POINT ( 'NONE', #25324 ) ;
#20903=ORIENTED_EDGE ( 'NONE', *, *, #33046, .T. ) ;
#20905=ORIENTED_EDGE ( 'NONE', *, *, #947, .F. ) ;
#20908=CARTESIAN_POINT ( 'NONE',  ( -5.812550801365592434, -3.368539882008727115, -1.828967928396027842 ) ) ;
#20915=CARTESIAN_POINT ( 'NONE',  ( 0.000000000000000000, -7.673322273190700926, -3.656518192455154637 ) ) ;
#20924=ORIENTED_EDGE ( 'NONE', *, *, #2182, .T. ) ;
#20927=CIRCLE ( 'NONE', #18247, 2.999999999999999112 ) ;
#20930=CARTESIAN_POINT ( 'NONE',  ( -8.000050800000000351, 0.05271045196100602320, -2.999989457909464363 ) ) ;
#20935=CARTESIAN_POINT ( 'NONE',  ( -7.906300802048391141, 0.3418742348694470690, -3.252716068056403564 ) ) ;
#20936=ORIENTED_EDGE ( 'NONE', *, *, #2080, .F. ) ;
#20937=AXIS2_PLACEMENT_3D ( 'NONE', #14671, #4147, #1638 ) ;
#20949=VERTEX_POINT ( 'NONE', #30697 ) ;
#20950=CARTESIAN_POINT ( 'NONE',  ( 7.249760686538667009, 6.226446564517917892, 6.147671362329242051 ) ) ;
#20954=EDGE_CURVE ( 'NONE', #32424, #11793, #10155, .T. ) ;
#20959=CARTESIAN_POINT ( 'NONE',  ( 5.612718761614565288, -3.934162523501283815, 7.212912035758797913 ) ) ;
#20964=AXIS2_PLACEMENT_3D ( 'NONE', #19280, #23952, #1063 ) ;
#20968=CARTESIAN_POINT ( 'NONE',  ( -2.484167557306937280, -0.3164610288023908535, 3.010925563584172515 ) ) ;
#20970=AXIS2_PLACEMENT_3D ( 'NONE', #30199, #22671, #25649 ) ;
#20974=LINE ( 'NONE', #7928, #7716 ) ;
#20984=CIRCLE ( 'NONE', #5530, 2.999999999999999556 ) ;
#20986=VECTOR ( 'NONE', #31801, 999.9999999999998863 ) ;
#20990=VERTEX_POINT ( 'NONE', #30994 ) ;
#20991=CARTESIAN_POINT ( 'NONE',  ( 3.499999999999999556, 0.000000000000000000, 0.000000000000000000 ) ) ;
#21002=AXIS2_PLACEMENT_3D ( 'NONE', #8808, #26534, #4123 ) ;
#21005=CARTESIAN_POINT ( 'NONE',  ( -1.757992424077718940, -0.3150232093026757996, 2.997245624844496081 ) ) ;
#21017=CARTESIAN_POINT ( 'NONE',  ( 3.499999999999999556, 7.008469740302810891, -0.7425307242147067832 ) ) ;
#21018=EDGE_CURVE ( 'NONE', #9606, #12581, #22831, .T. ) ;
#21020=CARTESIAN_POINT ( 'NONE',  ( -6.956376981307135665, 0.1572233378491243172, -2.999999999999999556 ) ) ;
#21025=CARTESIAN_POINT ( 'NONE',  ( -8.000050799999998574, -0.9398417724546661578, 2.990403141914843133 ) ) ;
#21030=CARTESIAN_POINT ( 'NONE',  ( -3.712550801365592790, 1.088641768524161613, 3.675193018007247403 ) ) ;
#21032=CARTESIAN_POINT ( 'NONE',  ( -4.904531657079156837, -0.3127741368606806738, 2.975847129947406522 ) ) ;
#21034=FACE_OUTER_BOUND ( 'NONE', #19554, .T. ) ;
#21038=CARTESIAN_POINT ( 'NONE',  ( 3.499999999999999556, -4.147285340411747789, -5.698247474649445365 ) ) ;
#21040=VECTOR ( 'NONE', #15847, 1000.000000000000000 ) ;
#21046=AXIS2_PLACEMENT_3D ( 'NONE', #5272, #2453, #15447 ) ;
#21049=CARTESIAN_POINT ( 'NONE',  ( 7.249760686538667009, 8.437262856154195134, -2.318425219014145444 ) ) ;
#21051=ORIENTED_EDGE ( 'NONE', *, *, #17322, .T. ) ;
#21057=B_SPLINE_CURVE_WITH_KNOTS ( 'NONE', 3,
 ( #6465, #32562, #31904, #32254, #9632, #24507, #32409, #29567, #14815, #29880 ),
 .UNSPECIFIED., .F., .F.,
 ( 4, 2, 2, 2, 4 ),
 ( 1.968338519013029732E-07, 0.0005467926395225683033, 0.001093388445193234533, 0.001639984250863900980, 0.002186580056534567426 ),
 .UNSPECIFIED. ) ;
#21060=CARTESIAN_POINT ( 'NONE',  ( -2.712550801365593234, -3.675193018007246071, 1.088641768524163167 ) ) ;
#21063=ORIENTED_EDGE ( 'NONE', *, *, #16663, .F. ) ;
#21064=VERTEX_POINT ( 'NONE', #5888 ) ;
#21068=CARTESIAN_POINT ( 'NONE',  ( 7.249760686538667009, 0.7071067811865129338, 8.721381771256208282 ) ) ;
#21070=CARTESIAN_POINT ( 'NONE',  ( 0.000000000000000000, 8.357095590591338663, 1.552080310331533486 ) ) ;
#21075=VERTEX_POINT ( 'NONE', #8557 ) ;
#21077=EDGE_CURVE ( 'NONE', #26082, #18185, #18769, .T. ) ;
#21085=EDGE_LOOP ( 'NONE', ( #21693, #32966, #13735, #1416 ) ) ;
#21086=DIRECTION ( 'NONE',  ( 0.000000000000000000, 0.000000000000000000, -1.000000000000000000 ) ) ;
#21091=CARTESIAN_POINT ( 'NONE',  ( -3.112550801365593145, 3.675193018007246959, -1.088641768524161391 ) ) ;
#21094=CARTESIAN_POINT ( 'NONE',  ( 6.880159540721329847, 7.943102264535301771, -3.624895993596787491 ) ) ;
#21096=CARTESIAN_POINT ( 'NONE',  ( -6.187550801365593323, -0.3701630799359326152, 3.521866450007987037 ) ) ;
#21111=DIRECTION ( 'NONE',  ( 0.000000000000000000, 0.000000000000000000, 1.000000000000000000 ) ) ;
#21113=ORIENTED_EDGE ( 'NONE', *, *, #14248, .F. ) ;
#21130=CARTESIAN_POINT ( 'NONE',  ( 5.377543748152548098, -6.940565734314625423, 4.007137495034787555 ) ) ;
#21133=ORIENTED_EDGE ( 'NONE', *, *, #17497, .F. ) ;
#21139=CARTESIAN_POINT ( 'NONE',  ( -6.912942406915326465, 7.727249047114547632E-16, -2.999999999999999556 ) ) ;
#21140=CARTESIAN_POINT ( 'NONE',  ( 1.750000000000000222, -8.497168642645963388, -0.2193742428685781509 ) ) ;
#21143=CARTESIAN_POINT ( 'NONE',  ( 6.356382477965132338, 5.080803740829814785, -6.947086032709882453 ) ) ;
#21146=( BOUNDED_CURVE ( )  B_SPLINE_CURVE ( 2, ( #10636, #18011, #22708, #23013, #15479, #28050, #9980, #455, #20843, #23205, #133 ),
 .UNSPECIFIED., .F., .F. ) 
 B_SPLINE_CURVE_WITH_KNOTS ( ( 3, 2, 2, 2, 2, 3 ),
 ( 0.06038226199343772749, 0.06250000000000000000, 0.07812500000000000000, 0.09375000000000000000, 0.1093750000000000000, 0.1228822619934377414 ),
 .UNSPECIFIED. ) 
 CURVE ( )  GEOMETRIC_REPRESENTATION_ITEM ( )  RATIONAL_B_SPLINE_CURVE ( ( 0.9821626249036858880, 0.9896829947469992783, 1.000000000000000000, 0.9238795325112867385, 1.000000000000000000, 0.9238795325112867385, 1.000000000000000000, 0.9238795325112867385, 1.000000000000000000, 0.9341965377642873491, 0.9821626249036861100 ) ) 
 REPRESENTATION_ITEM ( '' )  );
#21149=LINE ( 'NONE', #18618, #13497 ) ;
#21156=CARTESIAN_POINT ( 'NONE',  ( 6.038145268433178892, 6.771555838910925829, -5.096160642893582171 ) ) ;
#21158=VERTEX_POINT ( 'NONE', #3897 ) ;
#21164=EDGE_LOOP ( 'NONE', ( #14673, #14467, #6738 ) ) ;
#21167=CARTESIAN_POINT ( 'NONE',  ( -1.750050802731187405, -0.3135853898029607456, 2.983565686104819648 ) ) ;
#21168=CARTESIAN_POINT ( 'NONE',  ( -2.286883085291277595, 1.186209272513202517, 3.262832825226773092 ) ) ;
#21169=ORIENTED_EDGE ( 'NONE', *, *, #8616, .T. ) ;
#21170=CARTESIAN_POINT ( 'NONE',  ( 0.000000000000000000, 0.000000000000000000, 0.000000000000000000 ) ) ;
#21171=CARTESIAN_POINT ( 'NONE',  ( 5.887529311434773760, -0.3723788567093893609, 8.386653846779019261 ) ) ;
#21174=CARTESIAN_POINT ( 'NONE',  ( 0.000000000000000000, 6.745408891279611296, -5.171987904998036178 ) ) ;
#21180=DIRECTION ( 'NONE',  ( 0.000000000000000000, 0.8191520442889864695, 0.5735764363510537089 ) ) ;
#21182=CARTESIAN_POINT ( 'NONE',  ( 6.038145077921538650, 7.799182446117193912, 3.316258947000888302 ) ) ;
#21185=CARTESIAN_POINT ( 'NONE',  ( 7.249760686538667009, 7.906491560603716273, -3.748318449932209973 ) ) ;
#21187=CARTESIAN_POINT ( 'NONE',  ( -4.412550801365593856, -1.828967928396026510, 3.368539882008728004 ) ) ;
#21189=CARTESIAN_POINT ( 'NONE',  ( -5.650050800000000706, -1.549418761218565477, 2.853674364686380471 ) ) ;
#21209=CARTESIAN_POINT ( 'NONE',  ( -4.112550801365593145, -1.088641768524163389, -3.675193018007246071 ) ) ;
#21211=CARTESIAN_POINT ( 'NONE',  ( 3.499999999999999556, -8.497168642645966941, 0.2193742428684632428 ) ) ;
#21213=EDGE_LOOP ( 'NONE', ( #27291, #29279, #408 ) ) ;
#21219=FACE_OUTER_BOUND ( 'NONE', #18276, .T. ) ;
#21221=CARTESIAN_POINT ( 'NONE',  ( -1.928625734671288505, 0.6478360620448558871, 3.177561564833204066 ) ) ;
#21222=CARTESIAN_POINT ( 'NONE',  ( -3.137550801365593500, 3.368539882008727115, 1.828967928396027176 ) ) ;
#21228=VERTEX_POINT ( 'NONE', #7376 ) ;
#21230=CARTESIAN_POINT ( 'NONE',  ( 7.249760686538667009, 6.139290821770327256, -5.151476664237414127 ) ) ;
#21231=EDGE_CURVE ( 'NONE', #29357, #10953, #31535, .T. ) ;
#21232=FACE_OUTER_BOUND ( 'NONE', #15209, .T. ) ;
#21233=VERTEX_POINT ( 'NONE', #20602 ) ;
#21235=ORIENTED_EDGE ( 'NONE', *, *, #4305, .F. ) ;
#21239=CARTESIAN_POINT ( 'NONE',  ( -5.662550801365592967, 0.3701630799359330593, -3.521866450007987037 ) ) ;
#21244=CARTESIAN_POINT ( 'NONE',  ( -7.487550801365594033, -2.228590825266444586, -2.752080473201636401 ) ) ;
#21252=LINE ( 'NONE', #6523, #8803 ) ;
#21258=CARTESIAN_POINT ( 'NONE',  ( 3.499999999999999556, 4.137773741518377513, 5.705158055754806945 ) ) ;
#21260=CARTESIAN_POINT ( 'NONE',  ( -5.587550801365593678, 3.521866450007987037, 0.3701630799359328372 ) ) ;
#21264=CARTESIAN_POINT ( 'NONE',  ( 0.000000000000000000, -6.200809695932770538, -0.7745709230445805282 ) ) ;
#21265=DIRECTION ( 'NONE',  ( 0.000000000000000000, 0.9659258262890693114, -0.2588190451025167427 ) ) ;
#21274=VERTEX_POINT ( 'NONE', #12564 ) ;
#21286=B_SPLINE_CURVE_WITH_KNOTS ( 'NONE', 3,
 ( #14691, #17199, #4517, #32591, #30104, #7181, #14837, #12339, #23040, #7484 ),
 .UNSPECIFIED., .F., .F.,
 ( 4, 2, 2, 2, 4 ),
 ( 2.571685856657688708E-07, 0.0005478592107668815280, 0.001095461252948097194, 0.001643063295129312644, 0.002190665337310528961 ),
 .UNSPECIFIED. ) ;
#21289=CARTESIAN_POINT ( 'NONE',  ( -2.912942406915326909, 4.884725290497410777E-15, -2.999999999999999556 ) ) ;
#21291=ORIENTED_EDGE ( 'NONE', *, *, #24028, .F. ) ;
#21292=CARTESIAN_POINT ( 'NONE',  ( 7.249760686538667009, -3.647351267791519636, -7.953573330858250579 ) ) ;
#21293=FACE_OUTER_BOUND ( 'NONE', #3660, .T. ) ;
#21296=CYLINDRICAL_SURFACE ( 'NONE', #13550, 3.000000000000000444 ) ;
#21302=ORIENTED_EDGE ( 'NONE', *, *, #20631, .T. ) ;
#21309=ORIENTED_EDGE ( 'NONE', *, *, #3631, .F. ) ;
#21313=LINE ( 'NONE', #14120, #19359 ) ;
#21317=CARTESIAN_POINT ( 'NONE',  ( 5.612974441954673210, 5.126870824538761973, 6.420536856479951204 ) ) ;
#21322=DIRECTION ( 'NONE',  ( -1.000000000000000000, 0.000000000000000000, 0.000000000000000000 ) ) ;
#21327=DIRECTION ( 'NONE',  ( 1.000000000000000000, -0.000000000000000000, 0.000000000000000000 ) ) ;
#21331=CARTESIAN_POINT ( 'NONE',  ( -2.862550801365593145, -0.3701630799359326152, 3.521866450007987037 ) ) ;
#21332=VERTEX_POINT ( 'NONE', #16375 ) ;
#21333=CARTESIAN_POINT ( 'NONE',  ( -7.050050800000000173, -2.853674364686378695, -1.549418761218566809 ) ) ;
#21336=CARTESIAN_POINT ( 'NONE',  ( 7.249760686538667009, -4.007137495034861274, 6.940565734314584567 ) ) ;
#21337=CARTESIAN_POINT ( 'NONE',  ( 3.499999999999999556, -5.979767908488830663, -1.814490771706242622 ) ) ;
#21340=DIRECTION ( 'NONE',  ( 1.000000000000000000, -0.000000000000000000, -0.000000000000000000 ) ) ;
#21347=LINE ( 'NONE', #3498, #16565 ) ;
#21351=EDGE_CURVE ( 'NONE', #27551, #5304, #32012, .T. ) ;
#21354=DIRECTION ( 'NONE',  ( 1.000000000000000000, -0.000000000000000000, -0.000000000000000000 ) ) ;
#21359=CARTESIAN_POINT ( 'NONE',  ( -4.162550801365592967, -2.228590825266444586, -2.752080473201636401 ) ) ;
#21372=CARTESIAN_POINT ( 'NONE',  ( -8.404531657079157725, 2.325406398514293205, -1.883076972206379374 ) ) ;
#21373=DIRECTION ( 'NONE',  ( -1.000000000000000000, -0.000000000000000000, -0.000000000000000000 ) ) ;
#21374=CARTESIAN_POINT ( 'NONE',  ( -4.287550801365592967, -2.228590825266444586, -2.752080473201636401 ) ) ;
#21379=CARTESIAN_POINT ( 'NONE',  ( 7.064423637759000840, -2.318425219013664496, 8.437262856155488322 ) ) ;
#21387=CIRCLE ( 'NONE', #13349, 6.248999999999999666 ) ;
#21396=CARTESIAN_POINT ( 'NONE',  ( -4.112550801365593145, -1.088641768524163611, -3.675193018007245627 ) ) ;
#21400=VERTEX_POINT ( 'NONE', #20915 ) ;
#21401=CARTESIAN_POINT ( 'NONE',  ( -6.237550801365593145, 1.088641768524161613, 3.675193018007247403 ) ) ;
#21408=CARTESIAN_POINT ( 'NONE',  ( 3.499999999999999556, 0.000000000000000000, 0.000000000000000000 ) ) ;
#21409=VERTEX_POINT ( 'NONE', #11533 ) ;
#21410=AXIS2_PLACEMENT_3D ( 'NONE', #31263, #21696, #18533 ) ;
#21411=DIRECTION ( 'NONE',  ( -1.000000000000000000, -0.000000000000000000, -0.000000000000000000 ) ) ;
#21413=CARTESIAN_POINT ( 'NONE',  ( 5.887529755120530339, -1.089605374054316789, -8.323904922804405970 ) ) ;
#21414=EDGE_CURVE ( 'NONE', #24368, #12536, #10461, .T. ) ;
#21419=CARTESIAN_POINT ( 'NONE',  ( -4.537550801365592967, -1.828967928396026510, 3.368539882008728004 ) ) ;
#21436=EDGE_CURVE ( 'NONE', #10245, #22148, #26193, .T. ) ;
#21438=EDGE_CURVE ( 'NONE', #19582, #25459, #1630, .T. ) ;
#21439=VECTOR ( 'NONE', #32848, 1000.000000000000227 ) ;
#21440=CARTESIAN_POINT ( 'NONE',  ( -6.150050802731187538, 0.3135853898029611342, -2.983565686104819648 ) ) ;
#21443=VERTEX_POINT ( 'NONE', #27070 ) ;
#21454=VECTOR ( 'NONE', #11130, 1000.000000000000000 ) ;
#21456=CARTESIAN_POINT ( 'NONE',  ( 6.356382228872879736, 8.265862592379924934, 2.398350474621971706 ) ) ;
#21457=FACE_OUTER_BOUND ( 'NONE', #20573, .T. ) ;
#21465=CYLINDRICAL_SURFACE ( 'NONE', #18344, 3.000000000000000444 ) ;
#21466=VERTEX_POINT ( 'NONE', #24390 ) ;
#21468=VECTOR ( 'NONE', #14511, 1000.000000000000000 ) ;
#21471=ORIENTED_EDGE ( 'NONE', *, *, #31969, .T. ) ;
#21476=ORIENTED_EDGE ( 'NONE', *, *, #31969, .F. ) ;
#21479=AXIS2_PLACEMENT_3D ( 'NONE', #12950, #10279, #20660 ) ;
#21480=DIRECTION ( 'NONE',  ( -1.000000000000000000, -0.000000000000000000, 0.000000000000000000 ) ) ;
#21481=EDGE_LOOP ( 'NONE', ( #10612, #5458, #27862, #15299, #20023, #7972, #13126, #620, #23126, #23884, #3371, #7627, #22558, #16410, #4865, #29609, #6748, #10236, #20936, #19694, #16914 ) ) ;
#21491=CARTESIAN_POINT ( 'NONE',  ( 4.749760686538667009, 5.151476664237477188, 6.139290821770273077 ) ) ;
#21492=ORIENTED_EDGE ( 'NONE', *, *, #9439, .F. ) ;
#21502=EDGE_CURVE ( 'NONE', #30146, #2248, #2152, .T. ) ;
#21508=DIRECTION ( 'NONE',  ( 1.000000000000000000, -0.000000000000000000, -0.000000000000000000 ) ) ;
#21509=VECTOR ( 'NONE', #20090, 1000.000000000000000 ) ;
#21510=AXIS2_PLACEMENT_3D ( 'NONE', #22208, #9642, #4002 ) ;
#21512=CARTESIAN_POINT ( 'NONE',  ( -2.112550801365593145, 1.088641768524161613, 3.675193018007247403 ) ) ;
#21515=CARTESIAN_POINT ( 'NONE',  ( -5.450050799999999640, -2.853674364686378695, -1.549418761218566809 ) ) ;
#21516=LINE ( 'NONE', #31061, #25281 ) ;
#21517=CARTESIAN_POINT ( 'NONE',  ( -4.912942406915327354, -5.022711880624455567E-15, 2.999999999999999556 ) ) ;
#21520=ORIENTED_EDGE ( 'NONE', *, *, #31411, .T. ) ;
#21530=CIRCLE ( 'NONE', #1775, 6.248999999999999666 ) ;
#21532=DIRECTION ( 'NONE',  ( 0.000000000000000000, -0.5735764363510352792, -0.8191520442889993481 ) ) ;
#21535=EDGE_LOOP ( 'NONE', ( #30209, #22390, #28903 ) ) ;
#21538=LINE ( 'NONE', #26059, #9146 ) ;
#21543=CARTESIAN_POINT ( 'NONE',  ( -2.112550801365593145, 1.088641768524161613, 3.675193018007247403 ) ) ;
#21547=DIRECTION ( 'NONE',  ( -0.000000000000000000, -0.4226182617407035491, 0.9063077870366480493 ) ) ;
#21551=CARTESIAN_POINT ( 'NONE',  ( 0.000000000000000000, 0.000000000000000000, 0.000000000000000000 ) ) ;
#21552=ORIENTED_EDGE ( 'NONE', *, *, #27516, .T. ) ;
#21555=CARTESIAN_POINT ( 'NONE',  ( -4.037550801365593856, 3.675193018007246959, -1.088641768524161391 ) ) ;
#21575=CARTESIAN_POINT ( 'NONE',  ( -5.212550801365593678, -1.828967928396026732, 3.368539882008728004 ) ) ;
#21581=CARTESIAN_POINT ( 'NONE',  ( -7.687550801365593323, -2.752080473201636845, 2.228590825266444586 ) ) ;
#21595=DIRECTION ( 'NONE',  ( 1.000000000000000000, -0.000000000000000000, -0.000000000000000000 ) ) ;
#21604=CARTESIAN_POINT ( 'NONE',  ( 3.499999999999999556, -2.861184399890954300, -6.440778198864141935 ) ) ;
#21606=CARTESIAN_POINT ( 'NONE',  ( -7.712942406915323623, 7.727249047114547632E-16, -2.999999999999999556 ) ) ;
#21608=ORIENTED_EDGE ( 'NONE', *, *, #9768, .T. ) ;
#21611=CARTESIAN_POINT ( 'NONE',  ( -8.000050800000000351, 3.400452463515772461, -1.145969202744355542 ) ) ;
#21612=CARTESIAN_POINT ( 'NONE',  ( -6.100050802731187716, 1.549418761218566143, -2.853674364686379583 ) ) ;
#21617=EDGE_CURVE ( 'NONE', #11109, #12129, #12540, .T. ) ;
#21618=CYLINDRICAL_SURFACE ( 'NONE', #31583, 2.999999999999999112 ) ;
#21621=CARTESIAN_POINT ( 'NONE',  ( 6.356382228872879736, 3.475951004017332924, 7.873648075250509137 ) ) ;
#21625=CARTESIAN_POINT ( 'NONE',  ( -3.250050800000000795, -1.549418761218565255, 2.853674364686380471 ) ) ;
#21632=LINE ( 'NONE', #26978, #9783 ) ;
#21634=DIRECTION ( 'NONE',  ( 0.000000000000000000, 0.000000000000000000, -1.000000000000000000 ) ) ;
#21638=VERTEX_POINT ( 'NONE', #3331 ) ;
#21652=ORIENTED_EDGE ( 'NONE', *, *, #19652, .T. ) ;
#21665=FACE_OUTER_BOUND ( 'NONE', #2697, .T. ) ;
#21669=CARTESIAN_POINT ( 'NONE',  ( -5.100050802731186828, 2.853674364686379583, 1.549418761218565921 ) ) ;
#21671=CARTESIAN_POINT ( 'NONE',  ( -6.900050800000000706, 0.3135853898029611342, -2.983565686104819648 ) ) ;
#21692=DIRECTION ( 'NONE',  ( 0.000000000000000000, 0.2588190451025172423, 0.9659258262890692004 ) ) ;
#21693=ORIENTED_EDGE ( 'NONE', *, *, #23075, .F. ) ;
#21694=CARTESIAN_POINT ( 'NONE',  ( -3.112550801365593145, 3.675193018007247403, -1.088641768524161391 ) ) ;
#21696=DIRECTION ( 'NONE',  ( 0.000000000000000000, -0.4226182617407066022, 0.9063077870366466060 ) ) ;
#21698=DIRECTION ( 'NONE',  ( 1.000000000000000000, -0.000000000000000000, -0.000000000000000000 ) ) ;
#21701=DIRECTION ( 'NONE',  ( -1.000000000000000000, 0.000000000000000000, 0.000000000000000000 ) ) ;
#21708=CARTESIAN_POINT ( 'NONE',  ( -1.913028242501583209, 0.5824277790515788311, 3.167204378891976813 ) ) ;
#21709=CARTESIAN_POINT ( 'NONE',  ( -3.837550801365593234, 1.088641768524161613, 3.675193018007246959 ) ) ;
#21713=DIRECTION ( 'NONE',  ( -1.000000000000000000, -0.000000000000000000, 0.000000000000000000 ) ) ;
#21715=EDGE_LOOP ( 'NONE', ( #32574, #31505, #8078 ) ) ;
#21720=ORIENTED_EDGE ( 'NONE', *, *, #29930, .T. ) ;
#21725=DIRECTION ( 'NONE',  ( 1.000000000000000000, -0.000000000000000000, -0.000000000000000000 ) ) ;
#21728=CARTESIAN_POINT ( 'NONE',  ( 5.612718761614564400, 3.934162523501332220, -7.212912035758772156 ) ) ;
#21730=CARTESIAN_POINT ( 'NONE',  ( -7.737550801365593145, -1.828967928396026510, 3.368539882008728004 ) ) ;
#21732=CARTESIAN_POINT ( 'NONE',  ( 5.489321486716458587, 1.512021494499692809, -7.976795196726671477 ) ) ;
#21738=EDGE_CURVE ( 'NONE', #29013, #5075, #1626, .T. ) ;
#21742=CARTESIAN_POINT ( 'NONE',  ( 7.249760686538667009, -0.8180878109961253752, -8.711672189281435053 ) ) ;
#21748=CARTESIAN_POINT ( 'NONE',  ( -3.287550801365593856, 2.752080473201636845, -2.228590825266444142 ) ) ;
#21753=CARTESIAN_POINT ( 'NONE',  ( 6.037141812302425414, -1.911013226338353688, -8.256172215043598328 ) ) ;
#21761=ORIENTED_EDGE ( 'NONE', *, *, #12942, .T. ) ;
#21762=CARTESIAN_POINT ( 'NONE',  ( -6.162942409646512409, 7.727249047114547632E-16, -2.999999999999999556 ) ) ;
#21767=DIRECTION ( 'NONE',  ( 0.000000000000000000, 0.000000000000000000, -1.000000000000000000 ) ) ;
#21774=FACE_OUTER_BOUND ( 'NONE', #29779, .T. ) ;
#21781=CYLINDRICAL_SURFACE ( 'NONE', #20964, 8.500000000000000000 ) ;
#21782=DIRECTION ( 'NONE',  ( 0.000000000000000000, 0.000000000000000000, -1.000000000000000000 ) ) ;
#21785=CARTESIAN_POINT ( 'NONE',  ( 6.749760686538667009, 0.000000000000000000, 5.500000000000000000 ) ) ;
#21788=ADVANCED_FACE ( 'NONE', ( #19357 ), #21843, .F. ) ;
#21789=ORIENTED_EDGE ( 'NONE', *, *, #16232, .F. ) ;
#21796=ORIENTED_EDGE ( 'NONE', *, *, #8031, .T. ) ;
#21804=CARTESIAN_POINT ( 'NONE',  ( 6.356381935169119757, 0.9265622495396906855, -8.556754636093199196 ) ) ;
#21807=EDGE_CURVE ( 'NONE', #8819, #16362, #21897, .T. ) ;
#21808=CARTESIAN_POINT ( 'NONE',  ( 6.883866621640341243, 5.066432324612723193, 7.111352071735041136 ) ) ;
#21811=DIRECTION ( 'NONE',  ( 0.000000000000000000, 0.000000000000000000, 1.000000000000000000 ) ) ;
#21815=DIRECTION ( 'NONE',  ( 0.000000000000000000, 0.000000000000000000, 1.000000000000000000 ) ) ;
#21818=CARTESIAN_POINT ( 'NONE',  ( -7.250050802731188071, -2.331437884370912705, 1.887961173149512062 ) ) ;
#21820=ADVANCED_FACE ( 'NONE', ( #1816 ), #9129, .T. ) ;
#21821=CARTESIAN_POINT ( 'NONE',  ( -5.900050800000000706, 2.983565686104819648, 0.3135853898029609677 ) ) ;
#21823=DIRECTION ( 'NONE',  ( 0.000000000000000000, -0.8660254037844432595, 0.4999999999999918954 ) ) ;
#21824=CARTESIAN_POINT ( 'NONE',  ( 4.749760686538667009, -1.391664247347281780, 7.892520144992429820 ) ) ;
#21825=ORIENTED_EDGE ( 'NONE', *, *, #9172, .F. ) ;
#21828=ORIENTED_EDGE ( 'NONE', *, *, #26592, .F. ) ;
#21831=CARTESIAN_POINT ( 'NONE',  ( 6.880159329304571081, 6.122988934091276647, 6.224287131858821986 ) ) ;
#21832=ORIENTED_EDGE ( 'NONE', *, *, #24301, .T. ) ;
#21835=LINE ( 'NONE', #29361, #5407 ) ;
#21840=ADVANCED_FACE ( 'NONE', ( #16664 ), #26549, .F. ) ;
#21843=PLANE ( 'NONE',  #27774 ) ;
#21844=ORIENTED_EDGE ( 'NONE', *, *, #21018, .F. ) ;
#21847=CARTESIAN_POINT ( 'NONE',  ( -4.562942409646513653, -3.366872799099910998E-15, -3.000000000000000000 ) ) ;
#21850=ADVANCED_FACE ( 'NONE', ( #13806 ), #13980, .F. ) ;
#21852=DIRECTION ( 'NONE',  ( 1.000000000000000000, -0.000000000000000000, -0.000000000000000000 ) ) ;
#21854=VECTOR ( 'NONE', #4092, 1000.000000000000000 ) ;
#21856=CARTESIAN_POINT ( 'NONE',  ( 5.612974259723589654, 2.621729824970383760, 7.786824029658776070 ) ) ;
#21858=ADVANCED_FACE ( 'NONE', ( #14661 ), #27538, .T. ) ;
#21859=CARTESIAN_POINT ( 'NONE',  ( 3.499999999999999556, 5.904264776415098837, 2.046865518294726183 ) ) ;
#21862=FACE_OUTER_BOUND ( 'NONE', #16370, .T. ) ;
#21871=EDGE_CURVE ( 'NONE', #19072, #20419, #14405, .T. ) ;
#21872=AXIS2_PLACEMENT_3D ( 'NONE', #22327, #32539, #22498 ) ;
#21880=DIRECTION ( 'NONE',  ( 0.000000000000000000, 0.9659258262890660918, 0.2588190451025291772 ) ) ;
#21883=AXIS2_PLACEMENT_3D ( 'NONE', #24784, #32644, #27279 ) ;
#21884=CARTESIAN_POINT ( 'NONE',  ( 0.000000000000000000, 0.000000000000000000, 0.000000000000000000 ) ) ;
#21886=CARTESIAN_POINT ( 'NONE',  ( -3.137550801365593500, 3.368539882008727115, 1.828967928396026954 ) ) ;
#21892=ORIENTED_EDGE ( 'NONE', *, *, #24442, .F. ) ;
#21893=CARTESIAN_POINT ( 'NONE',  ( -6.700050800000000528, 2.983565686104819648, 0.3135853898029609677 ) ) ;
#21897=CIRCLE ( 'NONE', #24561, 2.999999999999999112 ) ;
#21898=ADVANCED_FACE ( 'NONE', ( #9465 ), #25830, .T. ) ;
#21901=CARTESIAN_POINT ( 'NONE',  ( 1.750000000000000222, -2.417132211460010005, -8.149077976821821778 ) ) ;
#21904=CARTESIAN_POINT ( 'NONE',  ( -3.637550801365593944, -3.675193018007246071, 1.088641768524163167 ) ) ;
#21905=ORIENTED_EDGE ( 'NONE', *, *, #5165, .T. ) ;
#21911=CARTESIAN_POINT ( 'NONE',  ( 7.064423600674403225, 2.210816291637418551, 8.466096581344331184 ) ) ;
#21915=DIRECTION ( 'NONE',  ( -1.000000000000000000, 0.000000000000000000, 0.000000000000000000 ) ) ;
#21919=EDGE_CURVE ( 'NONE', #11908, #32312, #4635, .T. ) ;
#21921=VERTEX_POINT ( 'NONE', #28154 ) ;
#21924=CARTESIAN_POINT ( 'NONE',  ( 7.064632951172269415, 6.147671362329299782, -6.226446564517853943 ) ) ;
#21929=PLANE ( 'NONE',  #32199 ) ;
#21932=CARTESIAN_POINT ( 'NONE',  ( 7.249760686538667009, 0.000000000000000000, 0.000000000000000000 ) ) ;
#21947=ORIENTED_EDGE ( 'NONE', *, *, #22054, .T. ) ;
#21950=CARTESIAN_POINT ( 'NONE',  ( -8.000050800000009232, 1.732502019020233597, -3.080952105985496292 ) ) ;
#21956=EDGE_CURVE ( 'NONE', #19600, #4093, #11207, .T. ) ;
#21969=ORIENTED_EDGE ( 'NONE', *, *, #11171, .F. ) ;
#21971=CARTESIAN_POINT ( 'NONE',  ( -1.750050802731187405, -0.3135853898029607456, 2.983565686104819648 ) ) ;
#21972=AXIS2_PLACEMENT_3D ( 'NONE', #1730, #1555, #32341 ) ;
#21977=CIRCLE ( 'NONE', #17731, 2.999999999999998668 ) ;
#21981=VECTOR ( 'NONE', #15512, 1000.000000000000000 ) ;
#21988=CARTESIAN_POINT ( 'NONE',  ( -5.700050802731187360, -1.549418761218565477, 2.853674364686380471 ) ) ;
#21990=CARTESIAN_POINT ( 'NONE',  ( -4.200050800000000528, 1.887961173149511618, 2.331437884370912705 ) ) ;
#21993=AXIS2_PLACEMENT_3D ( 'NONE', #29152, #11095, #3587 ) ;
#21998=ORIENTED_EDGE ( 'NONE', *, *, #16922, .T. ) ;
#21999=CARTESIAN_POINT ( 'NONE',  ( -1.950050802731187138, 2.983565686104819648, 0.3135853898029609677 ) ) ;
#22001=EDGE_CURVE ( 'NONE', #23179, #1670, #3098, .T. ) ;
#22002=AXIS2_PLACEMENT_3D ( 'NONE', #18122, #18783, #10761 ) ;
#22005=VERTEX_POINT ( 'NONE', #268 ) ;
#22013=CIRCLE ( 'NONE', #32176, 8.750000000000000000 ) ;
#22015=CARTESIAN_POINT ( 'NONE',  ( -5.712942406915326288, 3.284080845023683730E-15, 3.000000000000000000 ) ) ;
#22023=AXIS2_PLACEMENT_3D ( 'NONE', #30738, #15160, #2121 ) ;
#22031=DIRECTION ( 'NONE',  ( 1.000000000000000000, 0.000000000000000000, -0.000000000000000000 ) ) ;
#22032=ADVANCED_FACE ( 'NONE', ( #4487 ), #1975, .T. ) ;
#22038=CARTESIAN_POINT ( 'NONE',  ( 6.883866621640341243, -6.224335161394975557, -6.123537914202305643 ) ) ;
#22042=EDGE_CURVE ( 'NONE', #23417, #18225, #29027, .T. ) ;
#22043=CARTESIAN_POINT ( 'NONE',  ( -2.962942409646513564, 4.884725290497410777E-15, -2.999999999999999556 ) ) ;
#22054=EDGE_CURVE ( 'NONE', #30035, #572, #20127, .T. ) ;
#22056=ORIENTED_EDGE ( 'NONE', *, *, #19522, .T. ) ;
#22069=DIRECTION ( 'NONE',  ( 0.000000000000000000, 0.000000000000000000, 1.000000000000000000 ) ) ;
#22073=CARTESIAN_POINT ( 'NONE',  ( 5.377543748152549874, 4.007137495034909236, -6.940565734314555257 ) ) ;
#22075=CARTESIAN_POINT ( 'NONE',  ( -7.762550801365593500, 2.228590825266444142, 2.752080473201636845 ) ) ;
#22076=PLANE ( 'NONE',  #11772 ) ;
#22084=AXIS2_PLACEMENT_3D ( 'NONE', #3657, #26702, #8660 ) ;
#22085=CARTESIAN_POINT ( 'NONE',  ( 6.357667697713668353, 8.357963647880076508, 2.056386458247302595 ) ) ;
#22088=VECTOR ( 'NONE', #10570, 1000.000000000000000 ) ;
#22091=CARTESIAN_POINT ( 'NONE',  ( -6.450050802731187360, -2.331437884370912705, 1.887961173149512062 ) ) ;
#22093=CARTESIAN_POINT ( 'NONE',  ( 7.064632940817594076, 7.199384779417120406, 4.973063321323900610 ) ) ;
#22097=CARTESIAN_POINT ( 'NONE',  ( -2.837550801365592790, -3.675193018007246071, 1.088641768524163167 ) ) ;
#22099=CARTESIAN_POINT ( 'NONE',  ( 3.499999999999999556, -2.861184399891040009, 6.440778198864103743 ) ) ;
#22102=CARTESIAN_POINT ( 'NONE',  ( 7.249760686538667009, 7.530955069117513112, 2.741043480754951744 ) ) ;
#22104=VERTEX_POINT ( 'NONE', #18954 ) ;
#22106=CARTESIAN_POINT ( 'NONE',  ( 7.249760686538667009, 2.741043480755029016, -7.530955069117485579 ) ) ;
#22107=CIRCLE ( 'NONE', #26897, 8.500000000000000000 ) ;
#22112=ORIENTED_EDGE ( 'NONE', *, *, #1379, .T. ) ;
#22113=AXIS2_PLACEMENT_3D ( 'NONE', #4738, #15407, #24955 ) ;
#22125=CARTESIAN_POINT ( 'NONE',  ( 7.249760686538667009, -2.741043480754977946, 7.530955069117504230 ) ) ;
#22130=CARTESIAN_POINT ( 'NONE',  ( 3.499999999999999556, -2.861184399890954300, -6.440778198864141935 ) ) ;
#22144=ORIENTED_EDGE ( 'NONE', *, *, #19773, .T. ) ;
#22148=VERTEX_POINT ( 'NONE', #17750 ) ;
#22151=CARTESIAN_POINT ( 'NONE',  ( 3.499999999999999556, 7.008469740302810891, 2.257469275785292329 ) ) ;
#22158=DIRECTION ( 'NONE',  ( 1.000000000000000000, 0.000000000000000000, -0.000000000000000000 ) ) ;
#22162=DIRECTION ( 'NONE',  ( -1.000000000000000000, 0.000000000000000000, -0.000000000000000000 ) ) ;
#22167=DIRECTION ( 'NONE',  ( -1.000000000000000000, 0.000000000000000000, 0.000000000000000000 ) ) ;
#22170=DIRECTION ( 'NONE',  ( 0.000000000000000000, -0.9659258262890689783, -0.2588190451025185190 ) ) ;
#22171=CARTESIAN_POINT ( 'NONE',  ( -4.450050802731187360, 2.331437884370912705, -1.887961173149511618 ) ) ;
#22173=CARTESIAN_POINT ( 'NONE',  ( -3.800050800000000617, -1.887961173149512062, -2.331437884370912261 ) ) ;
#22174=FACE_OUTER_BOUND ( 'NONE', #25270, .T. ) ;
#22177=CARTESIAN_POINT ( 'NONE',  ( 7.249760686538667009, 1.391664247347228045, 7.892520144992438702 ) ) ;
#22186=CARTESIAN_POINT ( 'NONE',  ( -5.850050800000001772, 2.853674364686379583, 1.549418761218565921 ) ) ;
#22190=B_SPLINE_CURVE_WITH_KNOTS ( 'NONE', 3,
 ( #31015, #17977, #15795, #23168, #30864, #7934, #28319, #23320, #26001, #422 ),
 .UNSPECIFIED., .F., .F.,
 ( 4, 2, 2, 2, 4 ),
 ( 3.032460776734494555E-07, 0.0005479053915603975021, 0.001095507537043121683, 0.001643109682525845539, 0.002190711828008569395 ),
 .UNSPECIFIED. ) ;
#22198=CARTESIAN_POINT ( 'NONE',  ( 0.000000000000000000, -5.349675154362342866, 3.229702268444914370 ) ) ;
#22202=LINE ( 'NONE', #24206, #18912 ) ;
#22203=CARTESIAN_POINT ( 'NONE',  ( 6.524594682510452159, 0.6222547417166542916, 8.636529731786346531 ) ) ;
#22208=CARTESIAN_POINT ( 'NONE',  ( 3.499999999999999556, -4.147285340411824173, 5.698247474649390298 ) ) ;
#22210=CARTESIAN_POINT ( 'NONE',  ( -6.054531657079158080, 1.545410377633947174, -2.846291840500173365 ) ) ;
#22212=LINE ( 'NONE', #9649, #20499 ) ;
#22227=LINE ( 'NONE', #4338, #11357 ) ;
#22228=FACE_OUTER_BOUND ( 'NONE', #12069, .T. ) ;
#22233=CARTESIAN_POINT ( 'NONE',  ( -2.737550801365594477, -3.368539882008727115, -1.828967928396028064 ) ) ;
#22235=CARTESIAN_POINT ( 'NONE',  ( 7.249760686538667009, 0.000000000000000000, 0.000000000000000000 ) ) ;
#22250=CARTESIAN_POINT ( 'NONE',  ( -3.537550801365593411, -3.368539882008727115, -1.828967928396028064 ) ) ;
#22257=DIRECTION ( 'NONE',  ( -1.000000000000000000, -0.000000000000000000, 0.000000000000000000 ) ) ;
#22259=ORIENTED_EDGE ( 'NONE', *, *, #7592, .F. ) ;
#22261=ORIENTED_EDGE ( 'NONE', *, *, #21738, .T. ) ;
#22265=EDGE_LOOP ( 'NONE', ( #5231, #18597, #9537, #4777 ) ) ;
#22272=DIRECTION ( 'NONE',  ( -1.000000000000000000, -0.000000000000000000, -0.000000000000000000 ) ) ;
#22273=EDGE_CURVE ( 'NONE', #9461, #24987, #14969, .T. ) ;
#22277=EDGE_CURVE ( 'NONE', #4152, #19569, #26211, .T. ) ;
#22279=PLANE ( 'NONE',  #15554 ) ;
#22282=CARTESIAN_POINT ( 'NONE',  ( 3.499999999999999556, 0.000000000000000000, 0.000000000000000000 ) ) ;
#22285=CARTESIAN_POINT ( 'NONE',  ( 5.887530180601101115, -4.515817126386058256, 7.076866030741298275 ) ) ;
#22287=CARTESIAN_POINT ( 'NONE',  ( -7.887550801365593500, 2.228590825266444142, 2.752080473201636845 ) ) ;
#22297=LINE ( 'NONE', #27802, #10246 ) ;
#22299=CARTESIAN_POINT ( 'NONE',  ( -10.00000000000000000, 0.000000000000000000, 0.000000000000000000 ) ) ;
#22300=VERTEX_POINT ( 'NONE', #3060 ) ;
#22301=ORIENTED_EDGE ( 'NONE', *, *, #1635, .F. ) ;
#22305=FACE_OUTER_BOUND ( 'NONE', #30923, .T. ) ;
#22311=DIRECTION ( 'NONE',  ( 0.000000000000000000, 0.000000000000000000, 1.000000000000000000 ) ) ;
#22321=CARTESIAN_POINT ( 'NONE',  ( -4.750050802731187183, -2.983565686104819648, -0.3135853898029605791 ) ) ;
#22323=CARTESIAN_POINT ( 'NONE',  ( -2.850050800000000439, 1.549418761218566143, -2.853674364686379583 ) ) ;
#22324=PLANE ( 'NONE',  #31686 ) ;
#22325=CARTESIAN_POINT ( 'NONE',  ( -4.156376981307135843, -0.1572233378491262878, 2.999999999999999556 ) ) ;
#22327=CARTESIAN_POINT ( 'NONE',  ( 3.499999999999999556, 0.000000000000000000, 0.000000000000000000 ) ) ;
#22328=CARTESIAN_POINT ( 'NONE',  ( 6.880159329304570193, -6.122988934091237567, -6.224287131858866395 ) ) ;
#22332=CARTESIAN_POINT ( 'NONE',  ( -2.600050800000000883, 1.887961173149511618, 2.331437884370912705 ) ) ;
#22337=ORIENTED_EDGE ( 'NONE', *, *, #26381, .T. ) ;
#22338=LINE ( 'NONE', #7140, #20314 ) ;
#22341=DIRECTION ( 'NONE',  ( 0.000000000000000000, 0.4226182617406901154, 0.9063077870366543776 ) ) ;
#22346=DIRECTION ( 'NONE',  ( -1.000000000000000000, 0.000000000000000000, 0.000000000000000000 ) ) ;
#22347=VERTEX_POINT ( 'NONE', #31303 ) ;
#22353=CARTESIAN_POINT ( 'NONE',  ( -8.000050800000000351, 3.273954799371778801, 1.157949676854548526 ) ) ;
#22354=CARTESIAN_POINT ( 'NONE',  ( 5.887530252753765403, -6.185189124321781584, -5.676096663009868593 ) ) ;
#22360=CARTESIAN_POINT ( 'NONE',  ( -5.254531657079158258, 1.545410377633947174, -2.846291840500173365 ) ) ;
#22366=DIRECTION ( 'NONE',  ( -1.000000000000000000, -0.000000000000000000, -0.000000000000000000 ) ) ;
#22378=CARTESIAN_POINT ( 'NONE',  ( 4.749760686538667009, -2.741043480754977946, 7.530955069117504230 ) ) ;
#22379=CARTESIAN_POINT ( 'NONE',  ( 6.524595551582240915, -7.790581746767706761, -3.779376390944553243 ) ) ;
#22384=CARTESIAN_POINT ( 'NONE',  ( -4.737550801365593145, 3.368539882008727115, 1.828967928396026954 ) ) ;
#22387=CARTESIAN_POINT ( 'NONE',  ( 7.249760686538667009, 5.151476664237558900, -6.139290821770204687 ) ) ;
#22389=DIRECTION ( 'NONE',  ( 0.000000000000000000, -0.08715574274766618723, 0.9961946980917448791 ) ) ;
#22390=ORIENTED_EDGE ( 'NONE', *, *, #29581, .T. ) ;
#22391=CIRCLE ( 'NONE', #26148, 3.000000000000000444 ) ;
#22392=DIRECTION ( 'NONE',  ( 0.000000000000000000, 0.000000000000000000, 1.000000000000000000 ) ) ;
#22393=( BOUNDED_CURVE ( )  B_SPLINE_CURVE ( 2, ( #19332, #30323, #27017, #6436, #4120, #16640, #27167, #14287, #17587, #11791, #12586 ),
 .UNSPECIFIED., .F., .F. ) 
 B_SPLINE_CURVE_WITH_KNOTS ( ( 3, 2, 2, 2, 2, 3 ),
 ( 0.3103822619934377136, 0.3125000000000000000, 0.3281250000000000000, 0.3437500000000000000, 0.3593750000000000000, 0.3728822619934377136 ),
 .UNSPECIFIED. ) 
 CURVE ( )  GEOMETRIC_REPRESENTATION_ITEM ( )  RATIONAL_B_SPLINE_CURVE ( ( 0.9821626249036857770, 0.9896829947469991673, 1.000000000000000000, 0.9238795325112867385, 1.000000000000000000, 0.9238795325112867385, 1.000000000000000000, 0.9238795325112867385, 1.000000000000000000, 0.9341965377642874602, 0.9821626249036857770 ) ) 
 REPRESENTATION_ITEM ( '' )  );
#22398=CARTESIAN_POINT ( 'NONE',  ( 0.000000000000000000, 2.429606751577043422, 5.757344182232919216 ) ) ;
#22399=EDGE_CURVE ( 'NONE', #33011, #4959, #19278, .T. ) ;
#22406=ADVANCED_FACE ( 'NONE', ( #29423 ), #9509, .F. ) ;
#22407=AXIS2_PLACEMENT_3D ( 'NONE', #18322, #21480, #10615 ) ;
#22412=ADVANCED_FACE ( 'NONE', ( #24904 ), #2017, .F. ) ;
#22415=CARTESIAN_POINT ( 'NONE',  ( 0.000000000000000000, -5.233522515400055752, -4.720195129223329289 ) ) ;
#22416=ORIENTED_EDGE ( 'NONE', *, *, #5727, .F. ) ;
#22419=ORIENTED_EDGE ( 'NONE', *, *, #13829, .F. ) ;
#22425=CARTESIAN_POINT ( 'NONE',  ( 6.037141869538512395, 4.619542287584905260, 7.104659103919362728 ) ) ;
#22428=DIRECTION ( 'NONE',  ( -1.000000000000000000, -0.000000000000000000, -0.000000000000000000 ) ) ;
#22434=VECTOR ( 'NONE', #26356, 1000.000000000000000 ) ;
#22446=CARTESIAN_POINT ( 'NONE',  ( -5.637550801365594388, 3.675193018007246959, -1.088641768524161391 ) ) ;
#22447=ORIENTED_EDGE ( 'NONE', *, *, #32311, .F. ) ;
#22449=CARTESIAN_POINT ( 'NONE',  ( 7.249760686538667009, 0.000000000000000000, 0.000000000000000000 ) ) ;
#22451=DIRECTION ( 'NONE',  ( -1.000000000000000000, 0.000000000000000000, -0.000000000000000000 ) ) ;
#22452=ORIENTED_EDGE ( 'NONE', *, *, #1242, .T. ) ;
#22454=EDGE_CURVE ( 'NONE', #1352, #9705, #23524, .T. ) ;
#22455=VERTEX_POINT ( 'NONE', #30424 ) ;
#22467=AXIS2_PLACEMENT_3D ( 'NONE', #9530, #21915, #24270 ) ;
#22470=DIRECTION ( 'NONE',  ( 0.000000000000000000, 0.000000000000000000, 1.000000000000000000 ) ) ;
#22473=DIRECTION ( 'NONE',  ( 0.000000000000000000, 0.7071067811865455743, 0.7071067811865495711 ) ) ;
#22482=AXIS2_PLACEMENT_3D ( 'NONE', #32255, #16344, #19686 ) ;
#22489=EDGE_CURVE ( 'NONE', #26613, #26504, #4902, .T. ) ;
#22490=CARTESIAN_POINT ( 'NONE',  ( -3.500050802731187627, 2.853674364686379583, 1.549418761218565921 ) ) ;
#22492=CARTESIAN_POINT ( 'NONE',  ( -3.550050800000000173, 3.113457007523260156, -0.9222479816126439855 ) ) ;
#22496=CARTESIAN_POINT ( 'NONE',  ( -4.350050800000000883, 3.113457007523260156, -0.9222479816126439855 ) ) ;
#22498=DIRECTION ( 'NONE',  ( 0.000000000000000000, 0.7431448254773954654, -0.6691306063588569053 ) ) ;
#22499=ORIENTED_EDGE ( 'NONE', *, *, #12186, .T. ) ;
#22503=CARTESIAN_POINT ( 'NONE',  ( 7.249760686538667009, 7.906491560603665647, 3.748318449932320107 ) ) ;
#22507=EDGE_LOOP ( 'NONE', ( #9077, #17221, #20468 ) ) ;
#22508=CARTESIAN_POINT ( 'NONE',  ( 3.499999999999999556, -3.573533178329542537, -5.126388750707260300 ) ) ;
#22514=VECTOR ( 'NONE', #26055, 1000.000000000000114 ) ;
#22519=VECTOR ( 'NONE', #21532, 999.9999999999998863 ) ;
#22520=CARTESIAN_POINT ( 'NONE',  ( -3.362942409646513031, -5.022711880624455567E-15, 2.999999999999999556 ) ) ;
#22527=CARTESIAN_POINT ( 'NONE',  ( -8.000050800000055418, 2.257600361463367289, 2.491616663310649127 ) ) ;
#22531=ORIENTED_EDGE ( 'NONE', *, *, #20640, .T. ) ;
#22533=CARTESIAN_POINT ( 'NONE',  ( -7.962550801365594566, 2.752080473201636845, -2.228590825266444142 ) ) ;
#22535=EDGE_CURVE ( 'NONE', #1082, #7709, #29931, .T. ) ;
#22538=CARTESIAN_POINT ( 'NONE',  ( -7.204531657079157547, -2.325406398514293205, 1.883076972206379818 ) ) ;
#22550=CARTESIAN_POINT ( 'NONE',  ( -3.712942406915326288, 4.884725290497410777E-15, -2.999999999999999556 ) ) ;
#22556=DIRECTION ( 'NONE',  ( 1.000000000000000000, -0.000000000000000000, -0.000000000000000000 ) ) ;
#22558=ORIENTED_EDGE ( 'NONE', *, *, #30763, .F. ) ;
#22559=CIRCLE ( 'NONE', #12931, 2.999999999999999112 ) ;
#22560=CARTESIAN_POINT ( 'NONE',  ( -8.000050800000002127, -2.133806103461856729, -2.113321545700467041 ) ) ;
#22568=CARTESIAN_POINT ( 'NONE',  ( -8.012550801365593500, 1.828967928396027176, -3.368539882008727115 ) ) ;
#22573=CIRCLE ( 'NONE', #13454, 8.500000000000000000 ) ;
#22574=VERTEX_POINT ( 'NONE', #4624 ) ;
#22576=ORIENTED_EDGE ( 'NONE', *, *, #41, .F. ) ;
#22593=CARTESIAN_POINT ( 'NONE',  ( 3.499999999999999556, 0.000000000000000000, 0.000000000000000000 ) ) ;
#22609=VERTEX_POINT ( 'NONE', #14148 ) ;
#22610=VECTOR ( 'NONE', #7105, 1000.000000000000000 ) ;
#22613=( BOUNDED_CURVE ( )  B_SPLINE_CURVE ( 2, ( #8455, #21020, #18009, #12988, #8307, #28845, #23202, #3295, #13462, #611, #18648 ),
 .UNSPECIFIED., .F., .F. ) 
 B_SPLINE_CURVE_WITH_KNOTS ( ( 3, 2, 2, 2, 2, 3 ),
 ( 0.1228822619934377414, 0.1250000000000000000, 0.1406250000000000000, 0.1562500000000000000, 0.1718750000000000000, 0.1853822619934377414 ),
 .UNSPECIFIED. ) 
 CURVE ( )  GEOMETRIC_REPRESENTATION_ITEM ( )  RATIONAL_B_SPLINE_CURVE ( ( 0.9821626249036861100, 0.9896829947469993893, 1.000000000000000000, 0.9238795325112867385, 1.000000000000000000, 0.9238795325112867385, 1.000000000000000000, 0.9238795325112867385, 1.000000000000000000, 0.9341965377642873491, 0.9821626249036861100 ) ) 
 REPRESENTATION_ITEM ( '' )  );
#22614=VECTOR ( 'NONE', #28559, 1000.000000000000000 ) ;
#22620=AXIS2_PLACEMENT_3D ( 'NONE', #31922, #29741, #19384 ) ;
#22627=CYLINDRICAL_SURFACE ( 'NONE', #2225, 2.999999999999999112 ) ;
#22633=CARTESIAN_POINT ( 'NONE',  ( -7.187550801365593323, 3.521866450007987037, 0.3701630799359328372 ) ) ;
#22634=VERTEX_POINT ( 'NONE', #22503 ) ;
#22637=PLANE ( 'NONE',  #26868 ) ;
#22641=AXIS2_PLACEMENT_3D ( 'NONE', #16427, #3743, #21634 ) ;
#22651=EDGE_CURVE ( 'NONE', #4862, #19637, #1362, .T. ) ;
#22656=DIRECTION ( 'NONE',  ( 1.000000000000000000, -0.000000000000000000, -0.000000000000000000 ) ) ;
#22660=EDGE_CURVE ( 'NONE', #10072, #481, #20572, .T. ) ;
#22663=CIRCLE ( 'NONE', #7191, 8.500000000000000000 ) ;
#22671=DIRECTION ( 'NONE',  ( -1.000000000000000000, 0.000000000000000000, 0.000000000000000000 ) ) ;
#22675=CARTESIAN_POINT ( 'NONE',  ( -3.350050802731187272, -0.3135853898029607456, 2.983565686104819648 ) ) ;
#22676=ORIENTED_EDGE ( 'NONE', *, *, #12498, .F. ) ;
#22677=CARTESIAN_POINT ( 'NONE',  ( -4.050050800000001061, -1.549418761218565477, 2.853674364686380471 ) ) ;
#22682=CARTESIAN_POINT ( 'NONE',  ( 7.249760686538667009, 7.530955069117513112, 2.741043480754951744 ) ) ;
#22684=ADVANCED_FACE ( 'NONE', ( #27728 ), #7850, .T. ) ;
#22695=CARTESIAN_POINT ( 'NONE',  ( 6.883866482134012976, -2.190971798910002377, 8.452201317944597392 ) ) ;
#22703=DIRECTION ( 'NONE',  ( 1.000000000000000000, 0.000000000000000000, -0.000000000000000000 ) ) ;
#22708=CARTESIAN_POINT ( 'NONE',  ( -7.350050802731187716, -0.3135853898029607456, 2.983565686104819648 ) ) ;
#22712=CARTESIAN_POINT ( 'NONE',  ( -6.412550801365592967, 1.828967928396027176, -3.368539882008727115 ) ) ;
#22714=CARTESIAN_POINT ( 'NONE',  ( -6.754531657079159146, 3.105402419394639235, -0.9198621039125850496 ) ) ;
#22717=ORIENTED_EDGE ( 'NONE', *, *, #29044, .T. ) ;
#22719=EDGE_CURVE ( 'NONE', #1670, #19072, #2517, .T. ) ;
#22728=CARTESIAN_POINT ( 'NONE',  ( 4.749760686538667009, 7.892520144992453801, -1.391664247347147443 ) ) ;
#22730=CARTESIAN_POINT ( 'NONE',  ( -7.650050802731187538, 2.331437884370912705, -1.887961173149511618 ) ) ;
#22734=CARTESIAN_POINT ( 'NONE',  ( 4.749760686538667009, -7.892520144992443143, 1.391664247347202288 ) ) ;
#22736=VERTEX_POINT ( 'NONE', #12188 ) ;
#22737=CARTESIAN_POINT ( 'NONE',  ( -6.212550801365593678, 3.368539882008727115, 1.828967928396026954 ) ) ;
#22741=ORIENTED_EDGE ( 'NONE', *, *, #15093, .F. ) ;
#22744=CARTESIAN_POINT ( 'NONE',  ( -2.124956573341760357, 1.323625320507108460, 3.284597389080124774 ) ) ;
#22756=ORIENTED_EDGE ( 'NONE', *, *, #8415, .F. ) ;
#22758=ORIENTED_EDGE ( 'NONE', *, *, #17710, .T. ) ;
#22765=CARTESIAN_POINT ( 'NONE',  ( -7.062550801365593323, 3.521866450007987037, 0.3701630799359328372 ) ) ;
#22773=EDGE_CURVE ( 'NONE', #2513, #10376, #31570, .T. ) ;
#22778=LINE ( 'NONE', #17752, #29053 ) ;
#22779=B_SPLINE_CURVE_WITH_KNOTS ( 'NONE', 3,
 ( #23317, #26328, #1060, #8275, #419, #21143, #13419, #571, #18468, #16094 ),
 .UNSPECIFIED., .F., .F.,
 ( 4, 2, 2, 2, 4 ),
 ( 2.493548413911061648E-07, 0.0005478513795029415741, 0.001095453404164492160, 0.001643055428826042637, 0.002190657453487592898 ),
 .UNSPECIFIED. ) ;
#22780=DIRECTION ( 'NONE',  ( 0.000000000000000000, -0.5735764363510496011, -0.8191520442889893561 ) ) ;
#22784=ORIENTED_EDGE ( 'NONE', *, *, #29343, .T. ) ;
#22787=CARTESIAN_POINT ( 'NONE',  ( -5.787550801365593856, 0.3701630799359330593, -3.521866450007987037 ) ) ;
#22790=DIRECTION ( 'NONE',  ( 0.000000000000000000, -0.9945218953682744001, 0.1045284632676437286 ) ) ;
#22791=CARTESIAN_POINT ( 'NONE',  ( 3.499999999999999556, -3.573533178329542537, -5.126388750707260300 ) ) ;
#22796=CARTESIAN_POINT ( 'NONE',  ( 4.749760686538667009, 8.014274990069656823, -8.669741416787380218E-17 ) ) ;
#22801=ORIENTED_EDGE ( 'NONE', *, *, #17139, .T. ) ;
#22802=CARTESIAN_POINT ( 'NONE',  ( 6.524595551582241804, -4.857153507487898203, -7.168326838404991186 ) ) ;
#22820=CARTESIAN_POINT ( 'NONE',  ( -3.550050802731187005, 2.983565686104819648, 0.3135853898029609677 ) ) ;
#22822=CARTESIAN_POINT ( 'NONE',  ( -4.587550801365592790, -0.3701630799359326152, 3.521866450007987037 ) ) ;
#22824=EDGE_CURVE ( 'NONE', #24760, #4026, #18685, .T. ) ;
#22828=CARTESIAN_POINT ( 'NONE',  ( 6.883866621640341243, -5.066432324612676119, -7.111352071735073110 ) ) ;
#22831=B_SPLINE_CURVE_WITH_KNOTS ( 'NONE', 3,
 ( #26307, #11418, #20959, #18454, #16078, #13401, #8077, #23618, #31330, #8407 ),
 .UNSPECIFIED., .F., .F.,
 ( 4, 2, 2, 2, 4 ),
 ( 2.571685856657688708E-07, 0.0005478592107668808775, 0.001095461252948095893, 0.001643063295129310692, 0.002190665337310525058 ),
 .UNSPECIFIED. ) ;
#22835=EDGE_LOOP ( 'NONE', ( #23219, #16422, #23954, #22261 ) ) ;
#22838=CARTESIAN_POINT ( 'NONE',  ( -8.000050800000000351, 0.000000000000000000, 0.000000000000000000 ) ) ;
#22839=EDGE_LOOP ( 'NONE', ( #9830, #32654, #32904 ) ) ;
#22846=EDGE_CURVE ( 'NONE', #19569, #12106, #13909, .T. ) ;
#22859=CARTESIAN_POINT ( 'NONE',  ( -6.062550801365593323, -0.3701630799359326152, 3.521866450007987037 ) ) ;
#22861=CARTESIAN_POINT ( 'NONE',  ( -2.904531657079157725, 0.3127741368606810068, -2.975847129947406522 ) ) ;
#22867=FACE_OUTER_BOUND ( 'NONE', #25110, .T. ) ;
#22869=ORIENTED_EDGE ( 'NONE', *, *, #16506, .F. ) ;
#22870=CARTESIAN_POINT ( 'NONE',  ( 4.499760686538666121, 7.347880794884119736E-16, -6.000000000000000000 ) ) ;
#22877=LINE ( 'NONE', #33080, #21468 ) ;
#22878=VERTEX_POINT ( 'NONE', #3997 ) ;
#22886=CARTESIAN_POINT ( 'NONE',  ( -5.962550801365593678, -2.752080473201636845, 2.228590825266444586 ) ) ;
#22888=CARTESIAN_POINT ( 'NONE',  ( 5.489321708267612898, -6.285661071314506465, 5.138670926724877575 ) ) ;
#22892=ORIENTED_EDGE ( 'NONE', *, *, #7592, .T. ) ;
#22914=CARTESIAN_POINT ( 'NONE',  ( -1.738758153310166144, -0.3178988483021044087, 3.024605502323848949 ) ) ;
#22915=CARTESIAN_POINT ( 'NONE',  ( -6.662550801365592967, -3.521866450007987037, -0.3701630799359323931 ) ) ;
#22916=CARTESIAN_POINT ( 'NONE',  ( 7.249760686538667009, -8.437262856154180923, 2.318425219014200511 ) ) ;
#22923=PLANE ( 'NONE',  #12287 ) ;
#22929=DIRECTION ( 'NONE',  ( 0.000000000000000000, 0.7071067811865520136, -0.7071067811865431318 ) ) ;
#22933=DIRECTION ( 'NONE',  ( -1.000000000000000000, -0.000000000000000000, -0.000000000000000000 ) ) ;
#22935=DIRECTION ( 'NONE',  ( 1.000000000000000000, -0.000000000000000000, -0.000000000000000000 ) ) ;
#22936=CARTESIAN_POINT ( 'NONE',  ( -5.987550801365593145, -3.521866450007987037, -0.3701630799359323931 ) ) ;
#22939=VECTOR ( 'NONE', #16301, 1000.000000000000000 ) ;
#22951=ORIENTED_EDGE ( 'NONE', *, *, #32704, .F. ) ;
#22961=CARTESIAN_POINT ( 'NONE',  ( 5.377543748152549874, 2.741043480754926875, 7.530955069117522882 ) ) ;
#22962=CIRCLE ( 'NONE', #29916, 8.500000000000000000 ) ;
#22968=CARTESIAN_POINT ( 'NONE',  ( 7.249760686538667009, 8.711672189281426171, 0.8180878109962165246 ) ) ;
#22973=CARTESIAN_POINT ( 'NONE',  ( -3.800050802731187005, -0.9222479816126459840, -3.113457007523259268 ) ) ;
#22975=ADVANCED_FACE ( 'NONE', ( #24508 ), #9471, .T. ) ;
#22976=CARTESIAN_POINT ( 'NONE',  ( -6.137550801365595277, -1.828967928396026510, 3.368539882008728004 ) ) ;
#22981=DIRECTION ( 'NONE',  ( -1.000000000000000000, 0.000000000000000000, 0.000000000000000000 ) ) ;
#22984=AXIS2_PLACEMENT_3D ( 'NONE', #22796, #12914, #23134 ) ;
#23000=DIRECTION ( 'NONE',  ( 0.000000000000000000, -0.4226182617407076014, 0.9063077870366461619 ) ) ;
#23008=CARTESIAN_POINT ( 'NONE',  ( 1.750000000000000000, -2.834406817834851378, -8.013497238472808704 ) ) ;
#23012=CARTESIAN_POINT ( 'NONE',  ( -8.000050800000011009, -0.4525887372486252502, 3.137152558661513435 ) ) ;
#23013=CARTESIAN_POINT ( 'NONE',  ( -7.300050802731188782, -1.549418761218565255, 2.853674364686380471 ) ) ;
#23016=EDGE_LOOP ( 'NONE', ( #27939, #16651, #1388, #3189 ) ) ;
#23017=CARTESIAN_POINT ( 'NONE',  ( -6.112550801365593145, 1.088641768524161613, 3.675193018007247403 ) ) ;
#23020=CARTESIAN_POINT ( 'NONE',  ( -4.004531657079157370, -2.325406398514293205, 1.883076972206379818 ) ) ;
#23031=ORIENTED_EDGE ( 'NONE', *, *, #33000, .F. ) ;
#23038=AXIS2_PLACEMENT_3D ( 'NONE', #30500, #66, #13101 ) ;
#23040=CARTESIAN_POINT ( 'NONE',  ( 7.064423659272766720, 7.906491560605081403, 3.748318449931938634 ) ) ;
#23044=CARTESIAN_POINT ( 'NONE',  ( -7.407304909706597051, 1.062355717592094573, 2.999999999999999556 ) ) ;
#23047=DIRECTION ( 'NONE',  ( 0.000000000000000000, 0.5735764363510474917, -0.8191520442889909104 ) ) ;
#23050=CARTESIAN_POINT ( 'NONE',  ( -6.362550801365593145, 2.752080473201636845, -2.228590825266444142 ) ) ;
#23052=ADVANCED_FACE ( 'NONE', ( #25015 ), #17350, .F. ) ;
#23058=CIRCLE ( 'NONE', #20937, 8.750000000000000000 ) ;
#23064=ADVANCED_FACE ( 'NONE', ( #7156 ), #12795, .F. ) ;
#23073=CARTESIAN_POINT ( 'NONE',  ( 3.499999999999999556, -7.009698679648292519, 3.730838147389666126 ) ) ;
#23075=EDGE_CURVE ( 'NONE', #12879, #11105, #4980, .T. ) ;
#23080=DIRECTION ( 'NONE',  ( 1.000000000000000000, 0.000000000000000000, 0.000000000000000000 ) ) ;
#23081=AXIS2_PLACEMENT_3D ( 'NONE', #8140, #804, #10808 ) ;
#23086=AXIS2_PLACEMENT_3D ( 'NONE', #29519, #6612, #4108 ) ;
#23088=CARTESIAN_POINT ( 'NONE',  ( -5.100050802731186828, 2.853674364686379583, 1.549418761218565921 ) ) ;
#23094=CARTESIAN_POINT ( 'NONE',  ( -6.862550801365594033, -0.3701630799359326152, 3.521866450007987037 ) ) ;
#23099=DIRECTION ( 'NONE',  ( 0.000000000000000000, 0.5735764363510406083, 0.8191520442889955733 ) ) ;
#23116=DIRECTION ( 'NONE',  ( -1.000000000000000000, -0.000000000000000000, -0.000000000000000000 ) ) ;
#23118=CARTESIAN_POINT ( 'NONE',  ( 5.885541416630534428, 8.385500676968931089, -0.3712256868992730441 ) ) ;
#23123=AXIS2_PLACEMENT_3D ( 'NONE', #21038, #28562, #10824 ) ;
#23125=CARTESIAN_POINT ( 'NONE',  ( -4.637550801365592612, 1.088641768524161613, 3.675193018007246959 ) ) ;
#23126=ORIENTED_EDGE ( 'NONE', *, *, #826, .F. ) ;
#23133=CIRCLE ( 'NONE', #24715, 3.000000000000000444 ) ;
#23134=DIRECTION ( 'NONE',  ( 0.000000000000000000, -0.7071067811865507924, -0.7071067811865441310 ) ) ;
#23140=ORIENTED_EDGE ( 'NONE', *, *, #8961, .F. ) ;
#23141=ORIENTED_EDGE ( 'NONE', *, *, #3149, .F. ) ;
#23147=CYLINDRICAL_SURFACE ( 'NONE', #16627, 8.500000000000000000 ) ;
#23150=DIRECTION ( 'NONE',  ( 1.000000000000000000, -0.000000000000000000, -0.000000000000000000 ) ) ;
#23157=ADVANCED_FACE ( 'NONE', ( #5143 ), #19857, .F. ) ;
#23160=LINE ( 'NONE', #21140, #10238 ) ;
#23168=CARTESIAN_POINT ( 'NONE',  ( 5.885541615502097201, -8.322568858718549123, -1.090540896198895160 ) ) ;
#23169=CARTESIAN_POINT ( 'NONE',  ( -2.700050802731186916, 2.853674364686379583, 1.549418761218565921 ) ) ;
#23172=CARTESIAN_POINT ( 'NONE',  ( -4.887550801365593500, 2.752080473201636845, -2.228590825266444142 ) ) ;
#23174=DIRECTION ( 'NONE',  ( 0.000000000000000000, -1.224646799147351482E-16, 1.000000000000000000 ) ) ;
#23177=CARTESIAN_POINT ( 'NONE',  ( 6.038145268433179780, -5.096160642893607040, -6.771555838910908065 ) ) ;
#23179=VERTEX_POINT ( 'NONE', #308 ) ;
#23183=ORIENTED_EDGE ( 'NONE', *, *, #19419, .F. ) ;
#23187=CARTESIAN_POINT ( 'NONE',  ( -7.700050800000000528, 0.3135853898029611342, -2.983565686104819648 ) ) ;
#23190=ORIENTED_EDGE ( 'NONE', *, *, #1944, .T. ) ;
#23199=CARTESIAN_POINT ( 'NONE',  ( 3.499999999999999556, 5.904264776415128146, -2.046865518294647579 ) ) ;
#23202=CARTESIAN_POINT ( 'NONE',  ( -6.750050802731187183, 2.983565686104819648, 0.3135853898029609677 ) ) ;
#23203=EDGE_LOOP ( 'NONE', ( #15659, #211, #26928, #18815 ) ) ;
#23205=CARTESIAN_POINT ( 'NONE',  ( -7.007304909706599361, -1.062355717592095017, -2.999999999999999556 ) ) ;
#23209=EDGE_LOOP ( 'NONE', ( #6338, #13488, #7370, #26176 ) ) ;
#23210=CARTESIAN_POINT ( 'NONE',  ( -6.912550801365593856, 1.088641768524161613, 3.675193018007247403 ) ) ;
#23211=ORIENTED_EDGE ( 'NONE', *, *, #12116, .F. ) ;
#23212=CARTESIAN_POINT ( 'NONE',  ( -3.654531657079158169, 1.545410377633947174, -2.846291840500173365 ) ) ;
#23219=ORIENTED_EDGE ( 'NONE', *, *, #10565, .T. ) ;
#23226=CARTESIAN_POINT ( 'NONE',  ( 5.489344087273877903, 6.285690376021097592, 5.138668362895301378 ) ) ;
#23235=CARTESIAN_POINT ( 'NONE',  ( -7.612550801365593145, -1.828967928396026510, 3.368539882008728004 ) ) ;
#23236=DIRECTION ( 'NONE',  ( 0.000000000000000000, 0.000000000000000000, 1.000000000000000000 ) ) ;
#23253=EDGE_LOOP ( 'NONE', ( #30541, #314, #9680, #14952 ) ) ;
#23263=CARTESIAN_POINT ( 'NONE',  ( -6.062550801365593323, -0.3701630799359326152, 3.521866450007987037 ) ) ;
#23274=ORIENTED_EDGE ( 'NONE', *, *, #12610, .F. ) ;
#23275=ADVANCED_FACE ( 'NONE', ( #14127 ), #11615, .T. ) ;
#23277=B_SPLINE_CURVE_WITH_KNOTS ( 'NONE', 3,
 ( #24893, #1664, #26733, #17018, #1854, #14694, #1503, #3850, #29598, #2005 ),
 .UNSPECIFIED., .F., .F.,
 ( 4, 2, 2, 2, 4 ),
 ( 1.968338519002218415E-07, 0.0005467926089500440819, 0.001093388384048187825, 0.001639984159146331676, 0.002186579934244475745 ),
 .UNSPECIFIED. ) ;
#23280=CARTESIAN_POINT ( 'NONE',  ( -8.000050800000000351, 0.3135937863663861291, -2.983645574069408557 ) ) ;
#23299=ORIENTED_EDGE ( 'NONE', *, *, #5299, .F. ) ;
#23301=ADVANCED_FACE ( 'NONE', ( #8935 ), #6613, .T. ) ;
#23303=CARTESIAN_POINT ( 'NONE',  ( 5.489344046532323773, -6.978601450725515853, 4.149088721182507378 ) ) ;
#23316=FACE_OUTER_BOUND ( 'NONE', #23966, .T. ) ;
#23317=CARTESIAN_POINT ( 'NONE',  ( 5.377543748152549874, 5.151476664237558900, -6.139290821770204687 ) ) ;
#23319=CARTESIAN_POINT ( 'NONE',  ( 5.612974441954674987, -5.432722698947198836, 6.163896661468954541 ) ) ;
#23320=CARTESIAN_POINT ( 'NONE',  ( 6.880159790065805581, -8.691376398188692676, -0.8322990769133310485 ) ) ;
#23323=CARTESIAN_POINT ( 'NONE',  ( -2.450050802731187360, -2.331437884370912705, 1.887961173149512062 ) ) ;
#23335=ORIENTED_EDGE ( 'NONE', *, *, #21956, .T. ) ;
#23337=CARTESIAN_POINT ( 'NONE',  ( -2.429479563265797726, 0.4428684773465039748, 3.145100343978137758 ) ) ;
#23343=ORIENTED_EDGE ( 'NONE', *, *, #31232, .F. ) ;
#23353=CARTESIAN_POINT ( 'NONE',  ( -3.662550801365593411, -0.3701630799359326152, 3.521866450007987037 ) ) ;
#23355=CARTESIAN_POINT ( 'NONE',  ( -8.150050800000000706, 0.9222479816126443186, 3.113457007523260156 ) ) ;
#23363=ORIENTED_EDGE ( 'NONE', *, *, #29795, .F. ) ;
#23378=CARTESIAN_POINT ( 'NONE',  ( -5.712550801365594566, -1.088641768524163389, -3.675193018007246071 ) ) ;
#23379=CARTESIAN_POINT ( 'NONE',  ( 4.499760686538666121, 0.000000000000000000, 6.000000000000000000 ) ) ;
#23382=ORIENTED_EDGE ( 'NONE', *, *, #25936, .F. ) ;
#23393=DIRECTION ( 'NONE',  ( 0.000000000000000000, 0.000000000000000000, 1.000000000000000000 ) ) ;
#23403=EDGE_LOOP ( 'NONE', ( #27184, #23721, #21051, #1003 ) ) ;
#23406=CARTESIAN_POINT ( 'NONE',  ( -7.512550801365593500, -3.675193018007245627, 1.088641768524163389 ) ) ;
#23409=CARTESIAN_POINT ( 'NONE',  ( 5.885541736258998569, 7.752826540560551649, -3.216848386727986675 ) ) ;
#23411=CARTESIAN_POINT ( 'NONE',  ( 7.249760686538667009, 2.318425219014346172, -8.437262856154140067 ) ) ;
#23415=FACE_OUTER_BOUND ( 'NONE', #32992, .T. ) ;
#23417=VERTEX_POINT ( 'NONE', #12449 ) ;
#23422=FACE_OUTER_BOUND ( 'NONE', #30186, .T. ) ;
#23427=CARTESIAN_POINT ( 'NONE',  ( -3.762942409646513386, 4.884725290497410777E-15, -2.999999999999999556 ) ) ;
#23430=ORIENTED_EDGE ( 'NONE', *, *, #8929, .T. ) ;
#23433=ADVANCED_FACE ( 'NONE', ( #12611, #2441 ), #11966, .F. ) ;
#23438=CARTESIAN_POINT ( 'NONE',  ( -4.557304906975410574, -1.062355717592093463, -3.000000000000000888 ) ) ;
#23442=ORIENTED_EDGE ( 'NONE', *, *, #21919, .T. ) ;
#23446=LINE ( 'NONE', #261, #5946 ) ;
#23456=CIRCLE ( 'NONE', #5837, 8.750000000000000000 ) ;
#23463=ORIENTED_EDGE ( 'NONE', *, *, #27516, .F. ) ;
#23466=EDGE_CURVE ( 'NONE', #27801, #13878, #6481, .T. ) ;
#23467=DIRECTION ( 'NONE',  ( 0.000000000000000000, 0.7071067811865431318, 0.7071067811865520136 ) ) ;
#23472=CARTESIAN_POINT ( 'NONE',  ( -8.000050800000000351, 0.000000000000000000, 0.000000000000000000 ) ) ;
#23477=AXIS2_PLACEMENT_3D ( 'NONE', #5584, #25804, #13232 ) ;
#23479=ORIENTED_EDGE ( 'NONE', *, *, #2190, .F. ) ;
#23484=EDGE_LOOP ( 'NONE', ( #23183, #31854, #26915, #29666 ) ) ;
#23487=ORIENTED_EDGE ( 'NONE', *, *, #5236, .T. ) ;
#23489=DIRECTION ( 'NONE',  ( 0.000000000000000000, -0.9510565162951502005, -0.3090169943749573322 ) ) ;
#23490=CARTESIAN_POINT ( 'NONE',  ( -2.249956573341760357, 1.323625320507108460, 3.284597389080124774 ) ) ;
#23497=CARTESIAN_POINT ( 'NONE',  ( -3.850050799999999995, -2.853674364686378695, -1.549418761218566809 ) ) ;
#23501=EDGE_CURVE ( 'NONE', #30729, #4093, #23160, .T. ) ;
#23502=DIRECTION ( 'NONE',  ( 0.000000000000000000, -0.9063077870366526012, 0.4226182617406936126 ) ) ;
#23508=CARTESIAN_POINT ( 'NONE',  ( -3.762550801365593500, 2.228590825266444142, 2.752080473201636845 ) ) ;
#23510=CARTESIAN_POINT ( 'NONE',  ( -4.754531657079158258, -3.105402419394638791, 0.9198621039125867149 ) ) ;
#23516=CARTESIAN_POINT ( 'NONE',  ( 3.499999999999999556, 6.704570150426983233, 2.172265885002680808 ) ) ;
#23522=VECTOR ( 'NONE', #26398, 1000.000000000000000 ) ;
#23524=CIRCLE ( 'NONE', #11232, 2.999999999999998668 ) ;
#23528=CARTESIAN_POINT ( 'NONE',  ( 6.038145077921539539, 8.106170535363485641, -2.472816103755169248 ) ) ;
#23535=ORIENTED_EDGE ( 'NONE', *, *, #8929, .F. ) ;
#23536=CARTESIAN_POINT ( 'NONE',  ( -3.562550801365592879, -2.752080473201636845, 2.228590825266444586 ) ) ;
#23539=ORIENTED_EDGE ( 'NONE', *, *, #15787, .F. ) ;
#23545=CIRCLE ( 'NONE', #32656, 8.750000000000000000 ) ;
#23550=CIRCLE ( 'NONE', #19817, 2.999999999999998668 ) ;
#23567=CARTESIAN_POINT ( 'NONE',  ( -5.712550801365593678, -1.088641768524163611, -3.675193018007245627 ) ) ;
#23570=AXIS2_PLACEMENT_3D ( 'NONE', #19650, #17117, #27330 ) ;
#23578=DIRECTION ( 'NONE',  ( -1.000000000000000000, -0.000000000000000000, -0.000000000000000000 ) ) ;
#23586=VECTOR ( 'NONE', #13489, 1000.000000000000114 ) ;
#23590=CARTESIAN_POINT ( 'NONE',  ( 7.064632879756603145, -0.8180878109961264855, -8.711672189281433276 ) ) ;
#23597=CARTESIAN_POINT ( 'NONE',  ( 7.249760686538667009, -7.530955069117533540, 2.741043480754901118 ) ) ;
#23600=AXIS2_PLACEMENT_3D ( 'NONE', #7691, #20877, #7498 ) ;
#23603=CARTESIAN_POINT ( 'NONE',  ( 6.880160201030087741, -8.703862158141008720, 0.6895871680713464569 ) ) ;
#23616=CARTESIAN_POINT ( 'NONE',  ( 4.749760686538667009, 2.741043480754926875, 7.530955069117522882 ) ) ;
#23617=EDGE_CURVE ( 'NONE', #25632, #4026, #4074, .T. ) ;
#23618=CARTESIAN_POINT ( 'NONE',  ( 6.880159396099836400, -3.754731129947842749, 7.882559112973148707 ) ) ;
#23630=AXIS2_PLACEMENT_3D ( 'NONE', #24796, #17764, #27972 ) ;
#23634=VECTOR ( 'NONE', #21340, 1000.000000000000000 ) ;
#23636=CARTESIAN_POINT ( 'NONE',  ( -3.100050800000000439, -2.983565686104819648, -0.3135853898029605791 ) ) ;
#23639=CARTESIAN_POINT ( 'NONE',  ( 7.064423637759001728, -3.647351267792851903, -7.953573330858871415 ) ) ;
#23642=CYLINDRICAL_SURFACE ( 'NONE', #30626, 2.999999999999999112 ) ;
#23643=VERTEX_POINT ( 'NONE', #31488 ) ;
#23655=VECTOR ( 'NONE', #33097, 1000.000000000000000 ) ;
#23656=VERTEX_POINT ( 'NONE', #19459 ) ;
#23668=CARTESIAN_POINT ( 'NONE',  ( 5.885541615502091872, 1.090540896198919585, -8.322568858718543794 ) ) ;
#23673=FACE_OUTER_BOUND ( 'NONE', #22265, .T. ) ;
#23690=CARTESIAN_POINT ( 'NONE',  ( -4.812550801365592434, 1.828967928396027176, -3.368539882008727115 ) ) ;
#23692=EDGE_CURVE ( 'NONE', #23643, #299, #20398, .T. ) ;
#23693=CARTESIAN_POINT ( 'NONE',  ( -5.700050800000000528, -0.3135853898029607456, 2.983565686104819648 ) ) ;
#23695=CARTESIAN_POINT ( 'NONE',  ( 5.377543748152549874, -4.007137495034861274, 6.940565734314584567 ) ) ;
#23698=DIRECTION ( 'NONE',  ( -1.000000000000000000, 0.000000000000000000, -0.000000000000000000 ) ) ;
#23718=CARTESIAN_POINT ( 'NONE',  ( -4.012550801365593500, 1.828967928396027176, -3.368539882008727115 ) ) ;
#23721=ORIENTED_EDGE ( 'NONE', *, *, #9604, .F. ) ;
#23723=AXIS2_PLACEMENT_3D ( 'NONE', #15665, #25874, #2994 ) ;
#23728=ADVANCED_FACE ( 'NONE', ( #1909 ), #14587, .F. ) ;
#23732=CARTESIAN_POINT ( 'NONE',  ( -3.687550801365593323, -2.752080473201636845, 2.228590825266444586 ) ) ;
#23734=DIRECTION ( 'NONE',  ( -1.000000000000000000, 0.000000000000000000, 0.000000000000000000 ) ) ;
#23737=CARTESIAN_POINT ( 'NONE',  ( 3.499999999999999556, 0.005878491403554959860, -7.047692205288322853 ) ) ;
#23747=VERTEX_POINT ( 'NONE', #12576 ) ;
#23749=CARTESIAN_POINT ( 'NONE',  ( -4.662550801365592967, 3.521866450007987037, 0.3701630799359328372 ) ) ;
#23750=DIRECTION ( 'NONE',  ( -0.000000000000000000, -0.08715574274766135776, -0.9961946980917452121 ) ) ;
#23754=CARTESIAN_POINT ( 'NONE',  ( -5.437550801365592434, 1.088641768524161613, 3.675193018007247403 ) ) ;
#23756=CARTESIAN_POINT ( 'NONE',  ( 0.000000000000000000, 0.000000000000000000, 0.000000000000000000 ) ) ;
#23759=DIRECTION ( 'NONE',  ( -1.000000000000000000, -0.000000000000000000, -0.000000000000000000 ) ) ;
#23766=DIRECTION ( 'NONE',  ( 0.000000000000000000, 0.000000000000000000, -1.000000000000000000 ) ) ;
#23769=CARTESIAN_POINT ( 'NONE',  ( -5.687550801365593323, 2.752080473201636845, -2.228590825266444142 ) ) ;
#23776=EDGE_CURVE ( 'NONE', #21228, #10967, #11212, .T. ) ;
#23779=CARTESIAN_POINT ( 'NONE',  ( 0.000000000000000000, 7.008469740302810891, -0.7425307242147067832 ) ) ;
#23789=ORIENTED_EDGE ( 'NONE', *, *, #9647, .T. ) ;
#23802=CARTESIAN_POINT ( 'NONE',  ( 6.356382228872879736, -3.475951004017282298, -7.873648075250535783 ) ) ;
#23805=ORIENTED_EDGE ( 'NONE', *, *, #31552, .T. ) ;
#23815=ORIENTED_EDGE ( 'NONE', *, *, #447, .T. ) ;
#23819=ORIENTED_EDGE ( 'NONE', *, *, #23617, .F. ) ;
#23820=ORIENTED_EDGE ( 'NONE', *, *, #9962, .T. ) ;
#23829=DIRECTION ( 'NONE',  ( -1.000000000000000000, 0.000000000000000000, 0.000000000000000000 ) ) ;
#23842=CARTESIAN_POINT ( 'NONE',  ( -2.712550801365593234, -3.675193018007246071, 1.088641768524163167 ) ) ;
#23844=CARTESIAN_POINT ( 'NONE',  ( -6.850050799999999995, 1.549418761218566143, -2.853674364686379583 ) ) ;
#23845=ADVANCED_FACE ( 'NONE', ( #6882 ), #22279, .F. ) ;
#23846=DIRECTION ( 'NONE',  ( 1.000000000000000000, -0.000000000000000000, -0.000000000000000000 ) ) ;
#23850=ORIENTED_EDGE ( 'NONE', *, *, #30625, .F. ) ;
#23852=ORIENTED_EDGE ( 'NONE', *, *, #31884, .T. ) ;
#23858=CARTESIAN_POINT ( 'NONE',  ( 6.883866482134013864, -8.452201317944586734, -2.190971798910030799 ) ) ;
#23860=LINE ( 'NONE', #11491, #13427 ) ;
#23861=ORIENTED_EDGE ( 'NONE', *, *, #13019, .T. ) ;
#23879=CARTESIAN_POINT ( 'NONE',  ( 0.000000000000000000, 0.000000000000000000, 0.000000000000000000 ) ) ;
#23880=CARTESIAN_POINT ( 'NONE',  ( -3.437550801365593767, -1.088641768524163611, -3.675193018007245627 ) ) ;
#23884=ORIENTED_EDGE ( 'NONE', *, *, #19060, .F. ) ;
#23891=DIRECTION ( 'NONE',  ( 0.000000000000000000, 0.000000000000000000, -1.000000000000000000 ) ) ;
#23897=CARTESIAN_POINT ( 'NONE',  ( -5.012550801365594388, -3.368539882008727115, -1.828967928396027842 ) ) ;
#23903=CARTESIAN_POINT ( 'NONE',  ( -6.287550801365593856, 2.228590825266444142, 2.752080473201636845 ) ) ;
#23905=DIRECTION ( 'NONE',  ( 0.000000000000000000, 0.000000000000000000, 1.000000000000000000 ) ) ;
#23913=CARTESIAN_POINT ( 'NONE',  ( 3.499999999999999556, 0.000000000000000000, 0.000000000000000000 ) ) ;
#23917=LINE ( 'NONE', #6053, #18310 ) ;
#23918=CARTESIAN_POINT ( 'NONE',  ( -5.837550801365594566, -1.088641768524163389, -3.675193018007246071 ) ) ;
#23922=CARTESIAN_POINT ( 'NONE',  ( 7.249760686538667009, -6.940565734314570356, -4.007137495034885255 ) ) ;
#23926=CARTESIAN_POINT ( 'NONE',  ( -4.512942406915326998, 4.884725290497410777E-15, -2.999999999999999556 ) ) ;
#23927=ORIENTED_EDGE ( 'NONE', *, *, #21077, .T. ) ;
#23931=VERTEX_POINT ( 'NONE', #379 ) ;
#23934=CARTESIAN_POINT ( 'NONE',  ( 0.000000000000000000, -2.861184399890954300, -6.440778198864141935 ) ) ;
#23943=CARTESIAN_POINT ( 'NONE',  ( 0.000000000000000000, 6.100541242131516384, 3.528937025535512362 ) ) ;
#23952=DIRECTION ( 'NONE',  ( -1.000000000000000000, -0.000000000000000000, -0.000000000000000000 ) ) ;
#23954=ORIENTED_EDGE ( 'NONE', *, *, #19634, .F. ) ;
#23964=PLANE ( 'NONE',  #11182 ) ;
#23966=EDGE_LOOP ( 'NONE', ( #21520, #11954, #3738 ) ) ;
#23972=VERTEX_POINT ( 'NONE', #26275 ) ;
#23980=DIRECTION ( 'NONE',  ( -1.000000000000000000, 0.000000000000000000, 0.000000000000000000 ) ) ;
#23983=CARTESIAN_POINT ( 'NONE',  ( 5.612974259723585213, 7.650268724902057116, 2.996912441296202267 ) ) ;
#23987=CARTESIAN_POINT ( 'NONE',  ( -2.662550801365593411, -3.521866450007987037, -0.3701630799359323931 ) ) ;
#23989=CARTESIAN_POINT ( 'NONE',  ( -8.000050800000000351, -2.331437884370912705, 1.887961173149512062 ) ) ;
#23993=CARTESIAN_POINT ( 'NONE',  ( -5.200050800000000528, 2.331437884370912705, -1.887961173149511618 ) ) ;
#24009=CARTESIAN_POINT ( 'NONE',  ( 0.000000000000000000, -5.522688772756352726, -6.461416928141300531 ) ) ;
#24014=CARTESIAN_POINT ( 'NONE',  ( -3.812550801365593323, 3.368539882008727115, 1.828967928396026954 ) ) ;
#24019=CARTESIAN_POINT ( 'NONE',  ( 7.249760686538667009, -2.741043480754877582, -7.530955069117540646 ) ) ;
#24020=CARTESIAN_POINT ( 'NONE',  ( 1.750000000000000222, 8.265874651078018331, 1.981241088980808751 ) ) ;
#24023=ADVANCED_FACE ( 'NONE', ( #16998 ), #4499, .F. ) ;
#24026=DIRECTION ( 'NONE',  ( 0.000000000000000000, 0.9961946980917451011, 0.08715574274766293983 ) ) ;
#24028=EDGE_CURVE ( 'NONE', #15458, #29777, #5456, .T. ) ;
#24029=CARTESIAN_POINT ( 'NONE',  ( -3.787550801365593411, -0.3701630799359326152, 3.521866450007987037 ) ) ;
#24037=ORIENTED_EDGE ( 'NONE', *, *, #25551, .F. ) ;
#24043=CARTESIAN_POINT ( 'NONE',  ( -8.000050800000000351, 0.000000000000000000, 0.000000000000000000 ) ) ;
#24044=VERTEX_POINT ( 'NONE', #27199 ) ;
#24047=ORIENTED_EDGE ( 'NONE', *, *, #5403, .F. ) ;
#24050=CARTESIAN_POINT ( 'NONE',  ( -5.062550801365593323, -3.521866450007987037, -0.3701630799359323931 ) ) ;
#24055=CARTESIAN_POINT ( 'NONE',  ( -7.987550801365593145, 3.521866450007987037, 0.3701630799359328372 ) ) ;
#24061=AXIS2_PLACEMENT_3D ( 'NONE', #15955, #13447, #23489 ) ;
#24063=VERTEX_POINT ( 'NONE', #17174 ) ;
#24071=AXIS2_PLACEMENT_3D ( 'NONE', #10032, #7215, #20095 ) ;
#24074=CARTESIAN_POINT ( 'NONE',  ( -2.987550801365593145, -0.3701630799359326152, 3.521866450007987037 ) ) ;
#24075=EDGE_LOOP ( 'NONE', ( #20046, #25824 ) ) ;
#24086=DIRECTION ( 'NONE',  ( 0.000000000000000000, 0.000000000000000000, 1.000000000000000000 ) ) ;
#24092=ORIENTED_EDGE ( 'NONE', *, *, #10950, .T. ) ;
#24093=CARTESIAN_POINT ( 'NONE',  ( -8.000050800000018114, 1.979734913925816908, -2.936190332390367086 ) ) ;
#24094=VECTOR ( 'NONE', #30339, 1000.000000000000000 ) ;
#24104=ADVANCED_FACE ( 'NONE', ( #30568 ), #135, .F. ) ;
#24108=CARTESIAN_POINT ( 'NONE',  ( 3.499999999999999556, -5.979767908488830663, -1.814490771706242622 ) ) ;
#24111=CARTESIAN_POINT ( 'NONE',  ( 5.377543748152549874, -7.892520144992443143, 1.391664247347202288 ) ) ;
#24112=CIRCLE ( 'NONE', #32134, 6.248999999999998778 ) ;
#24113=AXIS2_PLACEMENT_3D ( 'NONE', #12158, #31306, #3389 ) ;
#24117=VERTEX_POINT ( 'NONE', #9640 ) ;
#24119=AXIS2_PLACEMENT_3D ( 'NONE', #23756, #11537, #23905 ) ;
#24128=CARTESIAN_POINT ( 'NONE',  ( -2.207304909706596874, -1.062355717592093463, -3.000000000000000888 ) ) ;
#24132=ORIENTED_EDGE ( 'NONE', *, *, #27562, .T. ) ;
#24133=VECTOR ( 'NONE', #20042, 1000.000000000000000 ) ;
#24147=CARTESIAN_POINT ( 'NONE',  ( 5.377543748152550762, -7.530955069117533540, 2.741043480754901118 ) ) ;
#24156=PLANE ( 'NONE',  #28481 ) ;
#24157=AXIS2_PLACEMENT_3D ( 'NONE', #6553, #26127, #3230 ) ;
#24164=AXIS2_PLACEMENT_3D ( 'NONE', #3132, #25680, #304 ) ;
#24165=LINE ( 'NONE', #31381, #19869 ) ;
#24166=CARTESIAN_POINT ( 'NONE',  ( -4.562942409646513653, -3.366872799099910998E-15, -3.000000000000000000 ) ) ;
#24167=CARTESIAN_POINT ( 'NONE',  ( 4.749760686538667009, -6.940565734314625423, 4.007137495034787555 ) ) ;
#24171=CARTESIAN_POINT ( 'NONE',  ( -4.700050802731189137, -2.853674364686378695, -1.549418761218566809 ) ) ;
#24174=CARTESIAN_POINT ( 'NONE',  ( -4.950050800000000528, 0.9222479816126443186, 3.113457007523260156 ) ) ;
#24179=CARTESIAN_POINT ( 'NONE',  ( -6.957304906975410042, -1.062355717592095017, -2.999999999999999556 ) ) ;
#24180=ORIENTED_EDGE ( 'NONE', *, *, #22454, .F. ) ;
#24187=DIRECTION ( 'NONE',  ( -1.000000000000000000, -0.000000000000000000, 0.000000000000000000 ) ) ;
#24197=VECTOR ( 'NONE', #21595, 1000.000000000000000 ) ;
#24200=CARTESIAN_POINT ( 'NONE',  ( 4.749760686538667009, -6.940565734314570356, -4.007137495034885255 ) ) ;
#24201=VERTEX_POINT ( 'NONE', #21185 ) ;
#24202=CARTESIAN_POINT ( 'NONE',  ( -3.412550801365593411, -3.368539882008727115, -1.828967928396028064 ) ) ;
#24206=CARTESIAN_POINT ( 'NONE',  ( 4.749760686538667009, -5.151476664237518044, 6.139290821770238438 ) ) ;
#24209=CYLINDRICAL_SURFACE ( 'NONE', #18780, 2.999999999999999112 ) ;
#24210=CYLINDRICAL_SURFACE ( 'NONE', #24695, 2.999999999999999112 ) ;
#24219=CARTESIAN_POINT ( 'NONE',  ( -2.387550801365593056, 3.521866450007987037, 0.3701630799359328372 ) ) ;
#24221=CARTESIAN_POINT ( 'NONE',  ( 4.749760686538667009, 6.139290821770257089, 5.151476664237498504 ) ) ;
#24223=EDGE_LOOP ( 'NONE', ( #25931, #27723, #9520, #260 ) ) ;
#24227=ORIENTED_EDGE ( 'NONE', *, *, #6923, .F. ) ;
#24237=CARTESIAN_POINT ( 'NONE',  ( -4.212550801365593678, -3.368539882008727115, -1.828967928396027842 ) ) ;
#24243=CARTESIAN_POINT ( 'NONE',  ( -5.337550801365593678, -1.828967928396026510, 3.368539882008728004 ) ) ;
#24258=DIRECTION ( 'NONE',  ( -0.000000000000000000, 0.08715574274765452989, 0.9961946980917458783 ) ) ;
#24259=CARTESIAN_POINT ( 'NONE',  ( -2.737550801365594477, -3.368539882008727115, -1.828967928396028064 ) ) ;
#24265=CARTESIAN_POINT ( 'NONE',  ( 5.612718383992088889, 8.054241895195652035, -1.622626842546680104 ) ) ;
#24266=CYLINDRICAL_SURFACE ( 'NONE', #25183, 2.999999999999999112 ) ;
#24270=DIRECTION ( 'NONE',  ( 0.000000000000000000, 0.8660254037844362651, 0.5000000000000039968 ) ) ;
#24276=EDGE_CURVE ( 'NONE', #27732, #7771, #16147, .T. ) ;
#24286=LINE ( 'NONE', #24108, #17283 ) ;
#24294=DIRECTION ( 'NONE',  ( -1.000000000000000000, -0.000000000000000000, -0.000000000000000000 ) ) ;
#24298=PLANE ( 'NONE',  #26371 ) ;
#24301=EDGE_CURVE ( 'NONE', #9041, #533, #28742, .T. ) ;
#24303=ORIENTED_EDGE ( 'NONE', *, *, #13683, .F. ) ;
#24311=VERTEX_POINT ( 'NONE', #18161 ) ;
#24317=LINE ( 'NONE', #32194, #32634 ) ;
#24323=DIRECTION ( 'NONE',  ( 0.000000000000000000, 0.000000000000000000, 1.000000000000000000 ) ) ;
#24334=CARTESIAN_POINT ( 'NONE',  ( -5.350050802731187716, 0.3135853898029611342, -2.983565686104819648 ) ) ;
#24337=CARTESIAN_POINT ( 'NONE',  ( -6.750050800000001239, 3.113457007523260156, -0.9222479816126439855 ) ) ;
#24353=ORIENTED_EDGE ( 'NONE', *, *, #9103, .F. ) ;
#24355=CARTESIAN_POINT ( 'NONE',  ( 6.037141848526922594, -7.798898458906302622, 3.315649934461692983 ) ) ;
#24358=DIRECTION ( 'NONE',  ( -1.000000000000000000, -0.000000000000000000, 0.000000000000000000 ) ) ;
#24363=CARTESIAN_POINT ( 'NONE',  ( 5.489343806296446360, -1.307372367723691919, 8.012901424861405886 ) ) ;
#24364=LINE ( 'NONE', #17499, #12903 ) ;
#24366=ORIENTED_EDGE ( 'NONE', *, *, #15105, .T. ) ;
#24368=VERTEX_POINT ( 'NONE', #19002 ) ;
#24369=ADVANCED_FACE ( 'NONE', ( #21665 ), #11781, .F. ) ;
#24390=CARTESIAN_POINT ( 'NONE',  ( 3.499999999999999556, -2.417132211460010005, -8.149077976821821778 ) ) ;
#24391=ORIENTED_EDGE ( 'NONE', *, *, #16506, .T. ) ;
#24392=CARTESIAN_POINT ( 'NONE',  ( -6.487550801365593145, 2.752080473201636845, -2.228590825266444142 ) ) ;
#24397=CARTESIAN_POINT ( 'NONE',  ( 5.612974384376780534, -7.013635602076178976, -4.279837954023545166 ) ) ;
#24399=CARTESIAN_POINT ( 'NONE',  ( 7.249760686538667009, -4.007137495034861274, 6.940565734314584567 ) ) ;
#24409=CARTESIAN_POINT ( 'NONE',  ( -4.087550801365593678, 2.752080473201636845, -2.228590825266444142 ) ) ;
#24415=CARTESIAN_POINT ( 'NONE',  ( 7.249760686538667009, -2.210816291636156006, -8.466096581343503402 ) ) ;
#24416=DIRECTION ( 'NONE',  ( 1.000000000000000000, -0.000000000000000000, -0.000000000000000000 ) ) ;
#24417=VERTEX_POINT ( 'NONE', #13948 ) ;
#24418=DIRECTION ( 'NONE',  ( -0.000000000000000000, 0.4226182617406968323, 0.9063077870366511579 ) ) ;
#24434=CARTESIAN_POINT ( 'NONE',  ( 3.499999999999999556, 1.106368468154540263, -8.427689411260562480 ) ) ;
#24435=EDGE_CURVE ( 'NONE', #20064, #13402, #6927, .T. ) ;
#24437=CARTESIAN_POINT ( 'NONE',  ( 4.749760686538667009, 8.385837730238846314E-14, -8.014274990069656823 ) ) ;
#24442=EDGE_CURVE ( 'NONE', #9082, #26824, #1292, .T. ) ;
#24446=CARTESIAN_POINT ( 'NONE',  ( -8.000050800000000351, 1.467282277383798572, -3.195100177104094552 ) ) ;
#24454=DIRECTION ( 'NONE',  ( -1.000000000000000000, -0.000000000000000000, -0.000000000000000000 ) ) ;
#24459=DIRECTION ( 'NONE',  ( -1.000000000000000000, -0.000000000000000000, -0.000000000000000000 ) ) ;
#24466=CARTESIAN_POINT ( 'NONE',  ( 5.887529755120530339, 1.089605374054371856, 8.323904922804400641 ) ) ;
#24478=CARTESIAN_POINT ( 'NONE',  ( -5.200050802731187360, 3.113457007523260156, -0.9222479816126439855 ) ) ;
#24480=CARTESIAN_POINT ( 'NONE',  ( -7.737550801365593145, -1.828967928396026510, 3.368539882008728004 ) ) ;
#24488=VERTEX_POINT ( 'NONE', #9941 ) ;
#24492=ORIENTED_EDGE ( 'NONE', *, *, #12657, .T. ) ;
#24495=DIRECTION ( 'NONE',  ( -1.000000000000000000, 0.000000000000000000, 0.000000000000000000 ) ) ;
#24503=CARTESIAN_POINT ( 'NONE',  ( 6.356382228872880624, -7.873648075250523348, 3.475951004017304946 ) ) ;
#24507=CARTESIAN_POINT ( 'NONE',  ( 6.038145208238973716, -3.842870190353647075, -7.553619661406949959 ) ) ;
#24508=FACE_OUTER_BOUND ( 'NONE', #3118, .T. ) ;
#24510=EDGE_CURVE ( 'NONE', #3811, #13648, #14554, .T. ) ;
#24515=AXIS2_PLACEMENT_3D ( 'NONE', #4780, #25169, #12967 ) ;
#24517=CARTESIAN_POINT ( 'NONE',  ( -2.800050802731187005, 3.113457007523260156, -0.9222479816126439855 ) ) ;
#24518=EDGE_LOOP ( 'NONE', ( #28487, #30985, #20096, #1508 ) ) ;
#24519=CARTESIAN_POINT ( 'NONE',  ( 4.749760686538667009, 5.151476664237477188, 6.139290821770273077 ) ) ;
#24525=CARTESIAN_POINT ( 'NONE',  ( 3.499999999999999556, 0.000000000000000000, 0.000000000000000000 ) ) ;
#24528=CARTESIAN_POINT ( 'NONE',  ( 0.000000000000000000, 0.000000000000000000, 0.000000000000000000 ) ) ;
#24538=ORIENTED_EDGE ( 'NONE', *, *, #10999, .F. ) ;
#24542=EDGE_CURVE ( 'NONE', #10302, #280, #15616, .T. ) ;
#24545=B_SPLINE_CURVE_WITH_KNOTS ( 'NONE', 3,
 ( #20129, #28777, #3077, #15907, #5397, #30979, #10568, #16058, #30835, #28285 ),
 .UNSPECIFIED., .F., .F.,
 ( 4, 2, 2, 2, 4 ),
 ( 2.740849916237977078E-07, 0.0005478761651001723409, 0.001095478245208722241, 0.001643080325317271924, 0.002190682405425822040 ),
 .UNSPECIFIED. ) ;
#24549=CARTESIAN_POINT ( 'NONE',  ( -8.062550801365594211, 0.3701630799359330593, -3.521866450007987037 ) ) ;
#24553=LINE ( 'NONE', #27423, #10344 ) ;
#24558=CARTESIAN_POINT ( 'NONE',  ( 7.249760686538667009, -5.064320921489867899, 7.135485519861982873 ) ) ;
#24561=AXIS2_PLACEMENT_3D ( 'NONE', #1472, #6801, #4139 ) ;
#24562=CARTESIAN_POINT ( 'NONE',  ( -6.550050802731187005, -0.3135853898029607456, 2.983565686104819648 ) ) ;
#24567=CARTESIAN_POINT ( 'NONE',  ( -3.137550801365593500, 3.368539882008727115, 1.828967928396026954 ) ) ;
#24570=ORIENTED_EDGE ( 'NONE', *, *, #10798, .T. ) ;
#24577=ORIENTED_EDGE ( 'NONE', *, *, #6005, .F. ) ;
#24582=ORIENTED_EDGE ( 'NONE', *, *, #15769, .T. ) ;
#24589=EDGE_LOOP ( 'NONE', ( #6185, #1419, #8481, #29742, #24615, #1612 ) ) ;
#24605=CARTESIAN_POINT ( 'NONE',  ( -2.476225935960405966, -0.3178988483021057410, 3.024605502323848949 ) ) ;
#24608=CIRCLE ( 'NONE', #83, 2.999999999999999112 ) ;
#24610=CARTESIAN_POINT ( 'NONE',  ( -8.000050800000018114, 1.979734913925816908, -2.936190332390367086 ) ) ;
#24614=CARTESIAN_POINT ( 'NONE',  ( 7.249760686538667009, 6.940565734314597002, 4.007137495034836405 ) ) ;
#24615=ORIENTED_EDGE ( 'NONE', *, *, #28428, .F. ) ;
#24617=VECTOR ( 'NONE', #30048, 1000.000000000000000 ) ;
#24619=VERTEX_POINT ( 'NONE', #3108 ) ;
#24620=LINE ( 'NONE', #17097, #15595 ) ;
#24629=CARTESIAN_POINT ( 'NONE',  ( 5.489321606599601999, -7.593050043411094130, -2.874206582856486669 ) ) ;
#24638=CIRCLE ( 'NONE', #28920, 6.248999999999999666 ) ;
#24639=AXIS2_PLACEMENT_3D ( 'NONE', #6087, #1056, #13741 ) ;
#24644=CIRCLE ( 'NONE', #30020, 2.999999999999999112 ) ;
#24646=AXIS2_PLACEMENT_3D ( 'NONE', #17521, #22556, #27899 ) ;
#24651=DIRECTION ( 'NONE',  ( 0.000000000000000000, 0.000000000000000000, -1.000000000000000000 ) ) ;
#24652=CARTESIAN_POINT ( 'NONE',  ( -6.150050802731187538, 0.3135853898029611342, -2.983565686104819648 ) ) ;
#24654=CARTESIAN_POINT ( 'NONE',  ( -4.800050800000000173, -2.331437884370912705, 1.887961173149512062 ) ) ;
#24656=EDGE_CURVE ( 'NONE', #10967, #5620, #2056, .T. ) ;
#24657=AXIS2_PLACEMENT_3D ( 'NONE', #15253, #15403, #10062 ) ;
#24659=CARTESIAN_POINT ( 'NONE',  ( 7.249760686538667009, 7.135485519861997972, 5.064320921489847471 ) ) ;
#24662=CARTESIAN_POINT ( 'NONE',  ( -1.807304909706596519, 1.062355717592091686, 3.000000000000001332 ) ) ;
#24664=CIRCLE ( 'NONE', #5486, 2.999999999999999556 ) ;
#24666=VECTOR ( 'NONE', #5788, 1000.000000000000000 ) ;
#24667=ORIENTED_EDGE ( 'NONE', *, *, #13079, .T. ) ;
#24676=AXIS2_PLACEMENT_3D ( 'NONE', #31811, #16069, #8882 ) ;
#24679=CARTESIAN_POINT ( 'NONE',  ( 5.612974044843318744, -1.622927203279397101, 8.054452210044754423 ) ) ;
#24689=CARTESIAN_POINT ( 'NONE',  ( 6.883866357751288412, -8.704251636488463006, -0.6899766464187978565 ) ) ;
#24692=FACE_OUTER_BOUND ( 'NONE', #23016, .T. ) ;
#24695=AXIS2_PLACEMENT_3D ( 'NONE', #19372, #19186, #29886 ) ;
#24697=EDGE_CURVE ( 'NONE', #299, #26246, #19147, .T. ) ;
#24698=CARTESIAN_POINT ( 'NONE',  ( -4.962942409646514008, 3.284080845023683730E-15, 3.000000000000000000 ) ) ;
#24705=VERTEX_POINT ( 'NONE', #28511 ) ;
#24707=CARTESIAN_POINT ( 'NONE',  ( -6.254531657079159146, -2.846291840500172921, -1.545410377633947618 ) ) ;
#24715=AXIS2_PLACEMENT_3D ( 'NONE', #26691, #9127, #6800 ) ;
#24722=EDGE_CURVE ( 'NONE', #20542, #7771, #29895, .T. ) ;
#24726=CARTESIAN_POINT ( 'NONE',  ( 5.612717990268488499, -0.1993707932845431574, -8.213645783354287744 ) ) ;
#24731=CARTESIAN_POINT ( 'NONE',  ( -2.412550801365592967, 1.828967928396027398, -3.368539882008727115 ) ) ;
#24736=CARTESIAN_POINT ( 'NONE',  ( -3.937550801365593323, 3.368539882008727115, 1.828967928396026954 ) ) ;
#24745=AXIS2_PLACEMENT_3D ( 'NONE', #14777, #7266, #22311 ) ;
#24759=CARTESIAN_POINT ( 'NONE',  ( -3.087550801365593234, 2.228590825266444142, 2.752080473201636845 ) ) ;
#24760=VERTEX_POINT ( 'NONE', #8575 ) ;
#24770=DIRECTION ( 'NONE',  ( -1.000000000000000000, -0.000000000000000000, -0.000000000000000000 ) ) ;
#24771=ORIENTED_EDGE ( 'NONE', *, *, #6697, .F. ) ;
#24775=ORIENTED_EDGE ( 'NONE', *, *, #29211, .T. ) ;
#24782=CARTESIAN_POINT ( 'NONE',  ( 5.612974259723586989, -2.996912441296229801, 7.650268724902049122 ) ) ;
#24784=CARTESIAN_POINT ( 'NONE',  ( 0.000000000000000000, -6.106419733534973027, -3.518755179752868223 ) ) ;
#24786=ORIENTED_EDGE ( 'NONE', *, *, #16281, .F. ) ;
#24796=CARTESIAN_POINT ( 'NONE',  ( 3.499999999999999556, 0.000000000000000000, 0.000000000000000000 ) ) ;
#24799=CARTESIAN_POINT ( 'NONE',  ( -5.487550801365593145, 2.228590825266444142, 2.752080473201636845 ) ) ;
#24808=ORIENTED_EDGE ( 'NONE', *, *, #23466, .T. ) ;
#24811=ORIENTED_EDGE ( 'NONE', *, *, #6044, .T. ) ;
#24823=B_SPLINE_CURVE_WITH_KNOTS ( 'NONE', 3,
 ( #5974, #31078, #23858, #15502, #31253, #965, #642, #25719, #15989, #823 ),
 .UNSPECIFIED., .F., .F.,
 ( 4, 2, 2, 2, 4 ),
 ( 1.968338519003762927E-07, 0.0005467928198071716301, 0.001093388805762442921, 0.001639984791717713887, 0.002186580777672985070 ),
 .UNSPECIFIED. ) ;
#24830=CARTESIAN_POINT ( 'NONE',  ( 3.499999999999999556, 0.000000000000000000, 0.000000000000000000 ) ) ;
#24832=ADVANCED_FACE ( 'NONE', ( #27123 ), #17242, .T. ) ;
#24833=CARTESIAN_POINT ( 'NONE',  ( -7.200050802731187360, -3.113457007523259268, 0.9222479816126455399 ) ) ;
#24836=CARTESIAN_POINT ( 'NONE',  ( -3.250050800000000795, -1.549418761218565477, 2.853674364686380471 ) ) ;
#24838=DIRECTION ( 'NONE',  ( -1.000000000000000000, 0.000000000000000000, 0.000000000000000000 ) ) ;
#24846=CARTESIAN_POINT ( 'NONE',  ( -2.700050800000000084, 2.983565686104819648, 0.3135853898029609677 ) ) ;
#24847=ORIENTED_EDGE ( 'NONE', *, *, #3865, .T. ) ;
#24856=CARTESIAN_POINT ( 'NONE',  ( 0.000000000000000000, 7.347880794884119736E-16, -6.000000000000000000 ) ) ;
#24858=EDGE_LOOP ( 'NONE', ( #18558, #33095, #11012, #4089 ) ) ;
#24859=CARTESIAN_POINT ( 'NONE',  ( 3.499999999999999556, 3.771202944355777298, -4.982773259188332027 ) ) ;
#24860=EDGE_CURVE ( 'NONE', #6329, #21228, #31667, .T. ) ;
#24864=CARTESIAN_POINT ( 'NONE',  ( 0.000000000000000000, -2.834406817834851378, -8.013497238472808704 ) ) ;
#24865=B_SPLINE_CURVE_WITH_KNOTS ( 'NONE', 3,
 ( #5162, #20208, #9207, #4050, #21753, #31960, #9025, #16744, #14217, #24415 ),
 .UNSPECIFIED., .F., .F.,
 ( 4, 2, 2, 2, 4 ),
 ( 3.032460776717885298E-07, 0.0005479053915603963095, 0.001095507537043120816, 0.001643109682525845322, 0.002190711828008569829 ),
 .UNSPECIFIED. ) ;
#24867=CARTESIAN_POINT ( 'NONE',  ( 5.489343555808769537, 0.1039150536218459431, 8.118190043691528857 ) ) ;
#24868=CARTESIAN_POINT ( 'NONE',  ( 5.489321708267612898, -6.152096559282798083, -5.297846913781757650 ) ) ;
#24874=EDGE_CURVE ( 'NONE', #17188, #24705, #6238, .T. ) ;
#24875=CARTESIAN_POINT ( 'NONE',  ( -2.950050802731187360, 0.3135853898029611342, -2.983565686104819648 ) ) ;
#24876=ORIENTED_EDGE ( 'NONE', *, *, #27688, .T. ) ;
#24877=CARTESIAN_POINT ( 'NONE',  ( -5.404531657079157725, -1.883076972206379818, -2.325406398514292761 ) ) ;
#24893=CARTESIAN_POINT ( 'NONE',  ( 7.249760686538667009, 6.226446564517917892, 6.147671362329242051 ) ) ;
#24899=CARTESIAN_POINT ( 'NONE',  ( -7.912550801365592967, 3.675193018007247403, -1.088641768524161391 ) ) ;
#24900=DIRECTION ( 'NONE',  ( 0.000000000000000000, 0.2079116908177532919, 0.9781476007338069101 ) ) ;
#24904=FACE_OUTER_BOUND ( 'NONE', #28917, .T. ) ;
#24908=EDGE_CURVE ( 'NONE', #22300, #9606, #31536, .T. ) ;
#24916=VERTEX_POINT ( 'NONE', #25297 ) ;
#24923=EDGE_CURVE ( 'NONE', #16362, #20158, #7094, .T. ) ;
#24924=CARTESIAN_POINT ( 'NONE',  ( 0.000000000000000000, -8.497168642645963388, -0.2193742428685781509 ) ) ;
#24925=VERTEX_POINT ( 'NONE', #15252 ) ;
#24941=VERTEX_POINT ( 'NONE', #25456 ) ;
#24946=DIRECTION ( 'NONE',  ( 1.000000000000000000, 0.000000000000000000, 0.000000000000000000 ) ) ;
#24950=CARTESIAN_POINT ( 'NONE',  ( 4.749760686538667009, -7.530955069117495349, -2.741043480755002371 ) ) ;
#24952=CARTESIAN_POINT ( 'NONE',  ( -7.737550801365593145, -1.828967928396026732, 3.368539882008728004 ) ) ;
#24955=DIRECTION ( 'NONE',  ( 0.000000000000000000, -0.2079116908177664480, 0.9781476007338041345 ) ) ;
#24957=ORIENTED_EDGE ( 'NONE', *, *, #11670, .T. ) ;
#24962=ORIENTED_EDGE ( 'NONE', *, *, #31521, .T. ) ;
#24964=CARTESIAN_POINT ( 'NONE',  ( 4.749760686538667009, 6.139290821770257089, 5.151476664237498504 ) ) ;
#24968=ORIENTED_EDGE ( 'NONE', *, *, #28424, .T. ) ;
#24971=VERTEX_POINT ( 'NONE', #17082 ) ;
#24973=PLANE ( 'NONE',  #11217 ) ;
#24976=EDGE_CURVE ( 'NONE', #30996, #16442, #27292, .T. ) ;
#24983=CYLINDRICAL_SURFACE ( 'NONE', #10237, 6.248999999999999666 ) ;
#24986=CARTESIAN_POINT ( 'NONE',  ( -2.600050802731188160, 0.9222479816126443186, 3.113457007523260156 ) ) ;
#24987=VERTEX_POINT ( 'NONE', #19772 ) ;
#24988=CARTESIAN_POINT ( 'NONE',  ( -3.000050799999999906, -1.887961173149512062, -2.331437884370912261 ) ) ;
#24990=CARTESIAN_POINT ( 'NONE',  ( -4.450050800000000528, 1.549418761218566143, -2.853674364686379583 ) ) ;
#24993=CARTESIAN_POINT ( 'NONE',  ( 5.885541838704148709, -5.674471607902398240, -6.185046950422377066 ) ) ;
#25010=DIRECTION ( 'NONE',  ( 0.000000000000000000, 0.000000000000000000, 1.000000000000000000 ) ) ;
#25012=CARTESIAN_POINT ( 'NONE',  ( 6.356382477965130562, -6.209963745178052719, 5.959271875177131861 ) ) ;
#25015=FACE_OUTER_BOUND ( 'NONE', #8437, .T. ) ;
#25017=CARTESIAN_POINT ( 'NONE',  ( 6.880159790065807357, -0.8322990769132998512, 8.691376398188698005 ) ) ;
#25021=VERTEX_POINT ( 'NONE', #8054 ) ;
#25022=CARTESIAN_POINT ( 'NONE',  ( -7.012550801365593500, 3.368539882008727115, 1.828967928396026954 ) ) ;
#25024=CARTESIAN_POINT ( 'NONE',  ( -8.254531657079157370, 2.846291840500173365, 1.545410377633946952 ) ) ;
#25032=CARTESIAN_POINT ( 'NONE',  ( 4.749760686538667009, 6.139290821770327256, -5.151476664237414127 ) ) ;
#25035=EDGE_CURVE ( 'NONE', #11109, #10411, #2923, .T. ) ;
#25037=FACE_OUTER_BOUND ( 'NONE', #28915, .T. ) ;
#25046=CARTESIAN_POINT ( 'NONE',  ( -3.637550801365593944, -3.675193018007246071, 1.088641768524163167 ) ) ;
#25049=CARTESIAN_POINT ( 'NONE',  ( 7.064632951172269415, -7.135485519862033499, 5.064320921489798621 ) ) ;
#25050=DIRECTION ( 'NONE',  ( 0.000000000000000000, 0.000000000000000000, 1.000000000000000000 ) ) ;
#25054=CARTESIAN_POINT ( 'NONE',  ( 3.499999999999999556, 7.008469740302810891, -0.7425307242147067832 ) ) ;
#25058=ADVANCED_FACE ( 'NONE', ( #20772 ), #3396, .F. ) ;
#25066=LINE ( 'NONE', #3, #7122 ) ;
#25073=EDGE_CURVE ( 'NONE', #12812, #10072, #8148, .T. ) ;
#25076=VERTEX_POINT ( 'NONE', #23427 ) ;
#25106=ORIENTED_EDGE ( 'NONE', *, *, #16487, .T. ) ;
#25109=CARTESIAN_POINT ( 'NONE',  ( -7.587550801365593678, -3.521866450007987037, -0.3701630799359323931 ) ) ;
#25110=EDGE_LOOP ( 'NONE', ( #29301, #31962, #25783, #23852 ) ) ;
#25113=CARTESIAN_POINT ( 'NONE',  ( 7.249760686538667009, 8.385837730238846314E-14, -8.014274990069656823 ) ) ;
#25136=DIRECTION ( 'NONE',  ( 0.000000000000000000, 0.000000000000000000, 1.000000000000000000 ) ) ;
#25143=AXIS2_PLACEMENT_3D ( 'NONE', #32364, #29835, #31130 ) ;
#25145=VECTOR ( 'NONE', #17700, 1000.000000000000114 ) ;
#25151=CARTESIAN_POINT ( 'NONE',  ( 0.000000000000000000, 0.000000000000000000, 0.000000000000000000 ) ) ;
#25153=CARTESIAN_POINT ( 'NONE',  ( 0.000000000000000000, -5.848742439617878652, -6.167836887841045446 ) ) ;
#25154=CARTESIAN_POINT ( 'NONE',  ( -4.100050802731187716, -1.549418761218565477, 2.853674364686380471 ) ) ;
#25156=CARTESIAN_POINT ( 'NONE',  ( -7.837550801365593678, 1.088641768524161613, 3.675193018007247403 ) ) ;
#25163=ADVANCED_FACE ( 'NONE', ( #5864 ), #240, .F. ) ;
#25169=DIRECTION ( 'NONE',  ( 1.000000000000000000, 0.000000000000000000, 0.000000000000000000 ) ) ;
#25170=ORIENTED_EDGE ( 'NONE', *, *, #12628, .T. ) ;
#25182=LINE ( 'NONE', #24856, #16694 ) ;
#25183=AXIS2_PLACEMENT_3D ( 'NONE', #18590, #5874, #16061 ) ;
#25191=CARTESIAN_POINT ( 'NONE',  ( 7.064423600674403225, -0.8180878109953999555, 8.711672189282626988 ) ) ;
#25198=CARTESIAN_POINT ( 'NONE',  ( -6.612550801365593145, -3.368539882008727115, -1.828967928396028064 ) ) ;
#25202=CARTESIAN_POINT ( 'NONE',  ( -6.554531657079158080, 0.9198621039125853827, 3.105402419394639235 ) ) ;
#25205=AXIS2_PLACEMENT_3D ( 'NONE', #22235, #7194, #4680 ) ;
#25209=AXIS2_PLACEMENT_3D ( 'NONE', #22099, #14719, #32621 ) ;
#25214=VECTOR ( 'NONE', #12430, 1000.000000000000000 ) ;
#25216=CARTESIAN_POINT ( 'NONE',  ( -3.400050800000000262, 1.887961173149511618, 2.331437884370912705 ) ) ;
#25222=DIRECTION ( 'NONE',  ( -0.000000000000000000, 0.9961946980917455452, -0.08715574274765797158 ) ) ;
#25223=CARTESIAN_POINT ( 'NONE',  ( 3.499999999999999556, -7.673322273190700926, -3.656518192455154193 ) ) ;
#25235=CARTESIAN_POINT ( 'NONE',  ( -4.237550801365593145, -1.088641768524163389, -3.675193018007246071 ) ) ;
#25238=CARTESIAN_POINT ( 'NONE',  ( 7.249760686538667009, 6.139290821770257089, 5.151476664237498504 ) ) ;
#25240=AXIS2_PLACEMENT_3D ( 'NONE', #13308, #13485, #10647 ) ;
#25243=ORIENTED_EDGE ( 'NONE', *, *, #8383, .T. ) ;
#25246=LINE ( 'NONE', #345, #32031 ) ;
#25258=ORIENTED_EDGE ( 'NONE', *, *, #11475, .F. ) ;
#25266=ORIENTED_EDGE ( 'NONE', *, *, #12254, .F. ) ;
#25269=ORIENTED_EDGE ( 'NONE', *, *, #5186, .T. ) ;
#25270=EDGE_LOOP ( 'NONE', ( #19100, #28792, #21844 ) ) ;
#25272=CARTESIAN_POINT ( 'NONE',  ( -7.812550801365593323, 3.368539882008727115, 1.828967928396027176 ) ) ;
#25273=DIRECTION ( 'NONE',  ( 0.000000000000000000, 0.000000000000000000, 1.000000000000000000 ) ) ;
#25279=AXIS2_PLACEMENT_3D ( 'NONE', #3632, #25891, #3309 ) ;
#25280=CARTESIAN_POINT ( 'NONE',  ( 6.357667873252799140, -3.476490553296904373, 7.873899671211479045 ) ) ;
#25281=VECTOR ( 'NONE', #23846, 1000.000000000000000 ) ;
#25283=EDGE_CURVE ( 'NONE', #21466, #21064, #3872, .T. ) ;
#25286=CARTESIAN_POINT ( 'NONE',  ( 5.377543748152551650, -7.892520144992426268, -1.391664247347309535 ) ) ;
#25288=AXIS2_PLACEMENT_3D ( 'NONE', #20882, #18879, #29078 ) ;
#25296=ORIENTED_EDGE ( 'NONE', *, *, #32790, .T. ) ;
#25297=CARTESIAN_POINT ( 'NONE',  ( 0.000000000000000000, -1.179494851233859887, -6.136676046192499179 ) ) ;
#25301=CARTESIAN_POINT ( 'NONE',  ( -7.087550801365593678, 2.228590825266444142, 2.752080473201636845 ) ) ;
#25305=CARTESIAN_POINT ( 'NONE',  ( 3.499999999999999556, 0.000000000000000000, 0.000000000000000000 ) ) ;
#25306=DIRECTION ( 'NONE',  ( -1.000000000000000000, 0.000000000000000000, 0.000000000000000000 ) ) ;
#25313=DIRECTION ( 'NONE',  ( 0.000000000000000000, -0.2588190451025252914, 0.9659258262890669799 ) ) ;
#25317=VERTEX_POINT ( 'NONE', #11210 ) ;
#25319=CARTESIAN_POINT ( 'NONE',  ( 5.612718761614564400, -4.279483796478976920, -7.013540705848223311 ) ) ;
#25321=EDGE_CURVE ( 'NONE', #24925, #19839, #13502, .T. ) ;
#25324=CARTESIAN_POINT ( 'NONE',  ( 3.499999999999999556, -4.724769925181146135, -4.089810527897805414 ) ) ;
#25341=CARTESIAN_POINT ( 'NONE',  ( -4.300050802731186117, 2.853674364686379583, 1.549418761218565921 ) ) ;
#25343=CARTESIAN_POINT ( 'NONE',  ( -4.937550801365593323, 1.828967928396027176, -3.368539882008727115 ) ) ;
#25345=LINE ( 'NONE', #4465, #9231 ) ;
#25355=ORIENTED_EDGE ( 'NONE', *, *, #25035, .T. ) ;
#25362=CARTESIAN_POINT ( 'NONE',  ( -2.476225935960405966, -0.3178988483021057410, 3.024605502323848949 ) ) ;
#25368=ORIENTED_EDGE ( 'NONE', *, *, #32657, .T. ) ;
#25379=CARTESIAN_POINT ( 'NONE',  ( -6.862550801365594033, -0.3701630799359326152, 3.521866450007987037 ) ) ;
#25381=CARTESIAN_POINT ( 'NONE',  ( -7.654531657079158613, 1.545410377633947174, -2.846291840500173365 ) ) ;
#25393=EDGE_CURVE ( 'NONE', #31349, #25757, #18337, .T. ) ;
#25395=FACE_OUTER_BOUND ( 'NONE', #29661, .T. ) ;
#25396=CARTESIAN_POINT ( 'NONE',  ( 6.524594682510450383, -0.6222547417165948946, -8.636529731786351860 ) ) ;
#25399=CARTESIAN_POINT ( 'NONE',  ( 7.249760686538667009, 4.007137495034909236, -6.940565734314555257 ) ) ;
#25403=ORIENTED_EDGE ( 'NONE', *, *, #29041, .T. ) ;
#25404=CARTESIAN_POINT ( 'NONE',  ( -7.062550801365593323, 3.521866450007987037, 0.3701630799359328372 ) ) ;
#25422=ORIENTED_EDGE ( 'NONE', *, *, #8961, .T. ) ;
#25433=VERTEX_POINT ( 'NONE', #2026 ) ;
#25435=CARTESIAN_POINT ( 'NONE',  ( -6.312550801365593323, 3.675193018007246959, -1.088641768524161391 ) ) ;
#25436=CARTESIAN_POINT ( 'NONE',  ( 0.000000000000000000, 3.771202944355777298, -4.982773259188332027 ) ) ;
#25437=CARTESIAN_POINT ( 'NONE',  ( 0.000000000000000000, -6.106419733535023653, 3.518755179752782958 ) ) ;
#25452=PLANE ( 'NONE',  #6016 ) ;
#25453=CARTESIAN_POINT ( 'NONE',  ( 7.249760686538667009, 7.199384779417189684, -4.973063321323801134 ) ) ;
#25456=CARTESIAN_POINT ( 'NONE',  ( 3.499999999999999556, 7.003298780661491918, -4.817032923780495857 ) ) ;
#25458=CARTESIAN_POINT ( 'NONE',  ( -6.287550801365593856, 2.228590825266444142, 2.752080473201636845 ) ) ;
#25459=VERTEX_POINT ( 'NONE', #22398 ) ;
#25461=CARTESIAN_POINT ( 'NONE',  ( 6.883866601413089370, 7.883091392499370187, -3.754588506078523569 ) ) ;
#25463=EDGE_LOOP ( 'NONE', ( #6355, #14413, #835 ) ) ;
#25479=FACE_OUTER_BOUND ( 'NONE', #30061, .T. ) ;
#25492=FACE_OUTER_BOUND ( 'NONE', #18087, .T. ) ;
#25495=CARTESIAN_POINT ( 'NONE',  ( -6.387550801365593500, 3.521866450007987037, 0.3701630799359328372 ) ) ;
#25497=EDGE_CURVE ( 'NONE', #24488, #10254, #12052, .T. ) ;
#25500=CARTESIAN_POINT ( 'NONE',  ( 1.750000000000000222, -5.848742439617962141, 6.167836887840968174 ) ) ;
#25502=EDGE_LOOP ( 'NONE', ( #32174, #23382, #11661, #16518 ) ) ;
#25504=EDGE_CURVE ( 'NONE', #14880, #17821, #5348, .T. ) ;
#25507=ORIENTED_EDGE ( 'NONE', *, *, #16049, .T. ) ;
#25508=ORIENTED_EDGE ( 'NONE', *, *, #30669, .F. ) ;
#25512=DIRECTION ( 'NONE',  ( 1.000000000000000000, -0.000000000000000000, -0.000000000000000000 ) ) ;
#25520=EDGE_LOOP ( 'NONE', ( #17360, #21608 ) ) ;
#25521=PRODUCT_DEFINITION_SHAPE ( 'NONE', 'NONE',  #1036 ) ;
#25522=CARTESIAN_POINT ( 'NONE',  ( 4.499760686538666121, 0.000000000000000000, 0.000000000000000000 ) ) ;
#25532=CARTESIAN_POINT ( 'NONE',  ( -5.512550801365595277, 3.675193018007247403, -1.088641768524161391 ) ) ;
#25533=ORIENTED_EDGE ( 'NONE', *, *, #32867, .F. ) ;
#25535=CARTESIAN_POINT ( 'NONE',  ( -8.250050800000000351, 2.853674364686379583, 1.549418761218565921 ) ) ;
#25551=EDGE_CURVE ( 'NONE', #24705, #32504, #8712, .T. ) ;
#25556=PLANE ( 'NONE',  #14501 ) ;
#25557=CARTESIAN_POINT ( 'NONE',  ( 5.887529755120530339, 8.323904922804413076, -1.089605374054287701 ) ) ;
#25559=CARTESIAN_POINT ( 'NONE',  ( -7.412550801365592967, -3.368539882008727115, -1.828967928396028064 ) ) ;
#25566=LINE ( 'NONE', #18200, #1679 ) ;
#25575=ORIENTED_EDGE ( 'NONE', *, *, #19097, .T. ) ;
#25576=CARTESIAN_POINT ( 'NONE',  ( 3.499999999999999556, -0.1221666339524086348, 6.247805719894683918 ) ) ;
#25579=ORIENTED_EDGE ( 'NONE', *, *, #24923, .F. ) ;
#25582=ORIENTED_EDGE ( 'NONE', *, *, #6078, .T. ) ;
#25584=EDGE_CURVE ( 'NONE', #30847, #13402, #17901, .T. ) ;
#25589=CARTESIAN_POINT ( 'NONE',  ( -7.162550801365593856, 2.752080473201636845, -2.228590825266444142 ) ) ;
#25590=DIRECTION ( 'NONE',  ( -1.000000000000000000, -0.000000000000000000, -0.000000000000000000 ) ) ;
#25591=CARTESIAN_POINT ( 'NONE',  ( 4.749760686538667009, 7.892520144992435149, 1.391664247347255134 ) ) ;
#25593=( BOUNDED_CURVE ( )  B_SPLINE_CURVE ( 2, ( #13907, #17281, #7393, #27975, #22287, #15254, #17583, #24952, #30319, #27478, #25109, #2566, #30172, #27786, #12416, #20276, #7244, #9557, #22633, #4734, #25301, #19968, #4898, #30479, #12091, #14756, #7562, #2227, #9743, #2412, #14903, #27634, #32841, #9912, #49, #5079, #25458, #12733, #29981, #4580, #20125, #15084, #22936, #12584, #10235, #20459, #22787, #32991, #19776, #22446, #2065, #30675, #24799, #32498, #10063, #12237, #1919, #17434, #7076, #17767, #32660, #7751, #17943, #28131, #5230, #8672, #13678, #31766, #990, #23125, #13824, #18696, #11172, #29390, #19042, #3665, #21374, #31585, #18890, #14004, #3354, #21555, #11352, #26714, #26241, #21709, #24029, #16505, #23732, #13520, #25614, #29085, #3523, #23880, #1156, #26421, #846, #6006, #11022, #21222, #31421, #6171, #28899, #28736, #16357, #26565, #16009, #8838, #29234, #3831, #7897, #242, #6317, #10414, #24219, #31919, #1339, #11515, #8497 ),
 .UNSPECIFIED., .F., .F. ) 
 B_SPLINE_CURVE_WITH_KNOTS ( ( 3, 2, 2, 2, 2, 2, 2, 2, 2, 2, 2, 2, 2, 2, 2, 2, 2, 2, 2, 2, 2, 2, 2, 2, 2, 2, 2, 2, 2, 2, 2, 2, 2, 2, 2, 2, 2, 2, 2, 2, 2, 2, 2, 2, 2, 2, 2, 2, 2, 2, 2, 2, 2, 2, 2, 2, 2, 2, 2, 3 ),
 ( 0.02919498387531501912, 0.03125000000000000000, 0.04687500000000000000, 0.06250000000000000000, 0.07812499999999998612, 0.09375000000000000000, 0.1093749999999999861, 0.1250000000000000000, 0.1406250000000000000, 0.1562500000000000000, 0.1718749999999999722, 0.1875000000000000000, 0.2031250000000000000, 0.2187500000000000000, 0.2343750000000000000, 0.2500000000000000000, 0.2656250000000000000, 0.2812500000000000000, 0.2968750000000000000, 0.3125000000000000000, 0.3281250000000000000, 0.3437500000000000000, 0.3593750000000000000, 0.3750000000000000555, 0.3906250000000000000, 0.4062500000000000000, 0.4218750000000000000, 0.4375000000000000000, 0.4531250000000000000, 0.4687500000000000000, 0.4843750000000000000, 0.5000000000000000000, 0.5156250000000000000, 0.5312500000000000000, 0.5468750000000000000, 0.5625000000000000000, 0.5781250000000000000, 0.5937500000000000000, 0.6093750000000000000, 0.6250000000000000000, 0.6406250000000000000, 0.6562500000000000000, 0.6718750000000000000, 0.6875000000000000000, 0.7031250000000000000, 0.7187500000000000000, 0.7343750000000000000, 0.7500000000000000000, 0.7656250000000000000, 0.7812500000000000000, 0.7968750000000001110, 0.8125000000000000000, 0.8281250000000000000, 0.8437500000000000000, 0.8593750000000000000, 0.8750000000000000000, 0.8906250000000000000, 0.9062500000000000000, 0.9218750000000000000, 0.9278186525000968743 ),
 .UNSPECIFIED. ) 
 CURVE ( )  GEOMETRIC_REPRESENTATION_ITEM ( )  RATIONAL_B_SPLINE_CURVE ( ( 0.9826105456045359787, 0.9899885575610967159, 1.000000000000000000, 0.9238795325112867385, 1.000000000000000000, 0.9238795325112867385, 1.000000000000000000, 0.9238795325112867385, 1.000000000000000000, 0.9238795325112867385, 1.000000000000000000, 0.9238795325112867385, 1.000000000000000000, 0.9238795325112867385, 1.000000000000000000, 0.9238795325112867385, 1.000000000000000000, 0.9238795325112867385, 1.000000000000000000, 0.9238795325112867385, 1.000000000000000000, 0.9238795325112867385, 1.000000000000000000, 0.9238795325112867385, 1.000000000000000000, 0.9238795325112867385, 1.000000000000000000, 0.9238795325112867385, 1.000000000000000000, 0.9238795325112867385, 1.000000000000000000, 0.9238795325112867385, 1.000000000000000000, 0.9238795325112867385, 1.000000000000000000, 0.9238795325112867385, 1.000000000000000000, 0.9238795325112867385, 1.000000000000000000, 0.9238795325112867385, 1.000000000000000000, 0.9238795325112867385, 1.000000000000000000, 0.9238795325112867385, 1.000000000000000000, 0.9238795325112867385, 1.000000000000000000, 0.9238795325112867385, 1.000000000000000000, 0.9238795325112867385, 1.000000000000000000, 0.9238795325112867385, 1.000000000000000000, 0.9238795325112867385, 1.000000000000000000, 0.9238795325112867385, 1.000000000000000000, 0.9238795325112867385, 1.000000000000000000, 0.9238795325112867385, 1.000000000000000000, 0.9238795325112867385, 1.000000000000000000, 0.9238795325112867385, 1.000000000000000000, 0.9238795325112867385, 1.000000000000000000, 0.9238795325112867385, 1.000000000000000000, 0.9238795325112867385, 1.000000000000000000, 0.9238795325112867385, 1.000000000000000000, 0.9238795325112867385, 1.000000000000000000, 0.9238795325112867385, 1.000000000000000000, 0.9238795325112867385, 1.000000000000000000, 0.9238795325112867385, 1.000000000000000000, 0.9238795325112867385, 1.000000000000000000, 0.9238795325112867385, 1.000000000000000000, 0.9238795325112867385, 1.000000000000000000, 0.9238795325112867385, 1.000000000000000000, 0.9238795325112867385, 1.000000000000000000, 0.9238795325112867385, 1.000000000000000000, 0.9238795325112867385, 1.000000000000000000, 0.9238795325112867385, 1.000000000000000000, 0.9238795325112867385, 1.000000000000000000, 0.9238795325112867385, 1.000000000000000000, 0.9238795325112867385, 1.000000000000000000, 0.9238795325112867385, 1.000000000000000000, 0.9238795325112867385, 1.000000000000000000, 0.9238795325112867385, 1.000000000000000000, 0.9238795325112867385, 1.000000000000000000, 0.9238795325112867385, 1.000000000000000000, 0.9238795325112867385, 1.000000000000000000, 0.9238795325112867385, 1.000000000000000000, 0.9710442491585387081, 0.9641176721898496726 ) ) 
 REPRESENTATION_ITEM ( '' )  );
#25608=FACE_OUTER_BOUND ( 'NONE', #23203, .T. ) ;
#25609=CARTESIAN_POINT ( 'NONE',  ( 0.000000000000000000, 0.000000000000000000, 0.000000000000000000 ) ) ;
#25614=CARTESIAN_POINT ( 'NONE',  ( -3.587550801365593678, -3.521866450007987037, -0.3701630799359323931 ) ) ;
#25618=DIRECTION ( 'NONE',  ( -1.000000000000000000, 0.000000000000000000, -0.000000000000000000 ) ) ;
#25624=DIRECTION ( 'NONE',  ( -1.000000000000000000, -0.000000000000000000, -0.000000000000000000 ) ) ;
#25631=CARTESIAN_POINT ( 'NONE',  ( 5.377543748152549874, 5.151476664237477188, 6.139290821770273077 ) ) ;
#25632=VERTEX_POINT ( 'NONE', #13043 ) ;
#25636=LINE ( 'NONE', #2752, #14528 ) ;
#25642=CARTESIAN_POINT ( 'NONE',  ( 5.612718622971679672, 2.996580135471525796, 7.650113768151185489 ) ) ;
#25649=DIRECTION ( 'NONE',  ( 0.000000000000000000, 0.000000000000000000, 1.000000000000000000 ) ) ;
#25655=CARTESIAN_POINT ( 'NONE',  ( -5.487550801365593145, 2.228590825266444142, 2.752080473201636845 ) ) ;
#25658=AXIS2_PLACEMENT_3D ( 'NONE', #10394, #27951, #12219 ) ;
#25660=EDGE_LOOP ( 'NONE', ( #2196, #28282, #2463, #18974, #20146, #12959, #11278, #4742, #9719, #6900, #27049, #21235, #30839, #2979, #1501, #28368, #23211, #3934, #20394, #2518, #10684, #23815, #19868, #11029, #10693, #28542, #17952, #9047, #5726, #21720, #18980, #6560, #20821, #5371, #32284, #25368, #17879, #31601, #28181, #26618, #28055, #22144, #10312, #25269, #31459, #32847, #23335, #24570, #19891, #13278, #11872, #17009, #32080, #1817, #1961, #16825, #19, #2114, #1068, #31597, #12654, #15730, #12136, #28027 ) ) ;
#25661=CARTESIAN_POINT ( 'NONE',  ( 7.249760686538667009, -5.064320921489771976, -7.135485519862050374 ) ) ;
#25669=ORIENTED_EDGE ( 'NONE', *, *, #17611, .F. ) ;
#25676=CARTESIAN_POINT ( 'NONE',  ( 1.750000000000000000, -2.417132211460119251, 8.149077976821791580 ) ) ;
#25680=DIRECTION ( 'NONE',  ( 0.000000000000000000, -0.9063077870366433864, -0.4226182617407134856 ) ) ;
#25685=CARTESIAN_POINT ( 'NONE',  ( 7.064423669210280643, -6.226446564518083093, 6.147671362330662248 ) ) ;
#25689=CARTESIAN_POINT ( 'NONE',  ( 4.749760686538667009, -7.892520144992443143, 1.391664247347202288 ) ) ;
#25693=DIRECTION ( 'NONE',  ( 0.000000000000000000, 0.000000000000000000, -1.000000000000000000 ) ) ;
#25698=CARTESIAN_POINT ( 'NONE',  ( -6.662550801365592967, -3.521866450007987037, -0.3701630799359323931 ) ) ;
#25700=CARTESIAN_POINT ( 'NONE',  ( -4.204531657079157547, 1.883076972206379374, 2.325406398514293205 ) ) ;
#25703=EDGE_CURVE ( 'NONE', #11175, #8263, #5012, .T. ) ;
#25707=CARTESIAN_POINT ( 'NONE',  ( 0.000000000000000000, 4.058600654062949786, -7.468451026206159860 ) ) ;
#25718=VECTOR ( 'NONE', #21265, 1000.000000000000114 ) ;
#25719=CARTESIAN_POINT ( 'NONE',  ( 5.612974044843318744, -8.054452210044752647, -1.622927203279425967 ) ) ;
#25723=CARTESIAN_POINT ( 'NONE',  ( -7.450050802731187360, 1.887961173149511618, 2.331437884370912705 ) ) ;
#25728=ORIENTED_EDGE ( 'NONE', *, *, #7611, .F. ) ;
#25729=CARTESIAN_POINT ( 'NONE',  ( -4.812550801365592434, 1.828967928396027176, -3.368539882008727115 ) ) ;
#25732=CYLINDRICAL_SURFACE ( 'NONE', #3858, 2.999999999999999112 ) ;
#25744=CIRCLE ( 'NONE', #18793, 2.999999999999999556 ) ;
#25745=EDGE_CURVE ( 'NONE', #16397, #16840, #2423, .T. ) ;
#25746=CARTESIAN_POINT ( 'NONE',  ( 7.249760686538667009, -6.940565734314625423, 4.007137495034787555 ) ) ;
#25747=EDGE_CURVE ( 'NONE', #16362, #21274, #16199, .T. ) ;
#25752=EDGE_CURVE ( 'NONE', #19839, #18491, #2342, .T. ) ;
#25757=VERTEX_POINT ( 'NONE', #12509 ) ;
#25776=VERTEX_POINT ( 'NONE', #27051 ) ;
#25781=CARTESIAN_POINT ( 'NONE',  ( 3.499999999999999556, -2.652816298622462376, 5.657964889053574531 ) ) ;
#25783=ORIENTED_EDGE ( 'NONE', *, *, #13201, .T. ) ;
#25784=CARTESIAN_POINT ( 'NONE',  ( 7.249760686538667009, 7.892520144992453801, -1.391664247347147443 ) ) ;
#25786=VECTOR ( 'NONE', #18908, 1000.000000000000000 ) ;
#25798=DIRECTION ( 'NONE',  ( 0.000000000000000000, 0.9063077870366497146, -0.4226182617406997744 ) ) ;
#25804=DIRECTION ( 'NONE',  ( -1.000000000000000000, 0.000000000000000000, -0.000000000000000000 ) ) ;
#25817=CARTESIAN_POINT ( 'NONE',  ( 3.499999999999999556, 0.000000000000000000, 0.000000000000000000 ) ) ;
#25819=ADVANCED_FACE ( 'NONE', ( #4155 ), #1647, .F. ) ;
#25822=DIRECTION ( 'NONE',  ( 0.000000000000000000, 0.000000000000000000, 1.000000000000000000 ) ) ;
#25824=ORIENTED_EDGE ( 'NONE', *, *, #19911, .T. ) ;
#25830=CYLINDRICAL_SURFACE ( 'NONE', #3748, 6.000000000000000000 ) ;
#25832=CARTESIAN_POINT ( 'NONE',  ( 5.377543748152550762, -1.391664247347281780, 7.892520144992429820 ) ) ;
#25846=ORIENTED_EDGE ( 'NONE', *, *, #489, .F. ) ;
#25848=CARTESIAN_POINT ( 'NONE',  ( -4.737550801365593145, 3.368539882008727115, 1.828967928396026954 ) ) ;
#25849=CARTESIAN_POINT ( 'NONE',  ( -2.562942409646512321, -5.022711880624455567E-15, 2.999999999999999556 ) ) ;
#25852=ORIENTED_EDGE ( 'NONE', *, *, #32909, .F. ) ;
#25860=CARTESIAN_POINT ( 'NONE',  ( 7.249760686538667009, -6.147671362329178102, -6.226446564517978288 ) ) ;
#25864=CARTESIAN_POINT ( 'NONE',  ( -2.452970694446401811, 0.2355604519343507952, 3.112266013026773859 ) ) ;
#25874=DIRECTION ( 'NONE',  ( 0.000000000000000000, 0.5735764363510413855, 0.8191520442889951292 ) ) ;
#25876=EDGE_CURVE ( 'NONE', #27844, #11829, #16855, .T. ) ;
#25884=B_SPLINE_CURVE_WITH_KNOTS ( 'NONE', 3,
 ( #9869, #17032, #2021, #32609, #22085, #4537, #9188, #7016, #29614, #12361 ),
 .UNSPECIFIED., .F., .F.,
 ( 4, 2, 2, 2, 4 ),
 ( 1.968338519003762927E-07, 0.0005467928198071721722, 0.001093388805762444006, 0.001639984791717715839, 0.002186580777672987672 ),
 .UNSPECIFIED. ) ;
#25886=CARTESIAN_POINT ( 'NONE',  ( -3.362550801365593589, -2.228590825266444586, -2.752080473201636401 ) ) ;
#25888=CARTESIAN_POINT ( 'NONE',  ( -8.500050800000000351, 0.3135853898029611342, -2.983565686104819648 ) ) ;
#25889=VECTOR ( 'NONE', #946, 1000.000000000000000 ) ;
#25890=CARTESIAN_POINT ( 'NONE',  ( 7.249760686538667009, 0.000000000000000000, 0.000000000000000000 ) ) ;
#25891=DIRECTION ( 'NONE',  ( -1.000000000000000000, 0.000000000000000000, -0.000000000000000000 ) ) ;
#25901=CARTESIAN_POINT ( 'NONE',  ( 7.249760686538667009, -6.139290821770289064, 5.151476664237455871 ) ) ;
#25902=CARTESIAN_POINT ( 'NONE',  ( 6.524595623740806261, 7.015943501182391628, 5.074779492939314629 ) ) ;
#25904=ORIENTED_EDGE ( 'NONE', *, *, #9029, .F. ) ;
#25907=CARTESIAN_POINT ( 'NONE',  ( 3.499999999999999556, -2.834406817834851378, -8.013497238472808704 ) ) ;
#25911=AXIS2_PLACEMENT_3D ( 'NONE', #19610, #7552, #12083 ) ;
#25912=CARTESIAN_POINT ( 'NONE',  ( -5.412550801365593856, 3.368539882008727115, 1.828967928396026954 ) ) ;
#25913=DIRECTION ( 'NONE',  ( -0.000000000000000000, -0.9063077870366467170, -0.4226182617407066577 ) ) ;
#25916=ORIENTED_EDGE ( 'NONE', *, *, #23692, .T. ) ;
#25918=CARTESIAN_POINT ( 'NONE',  ( 7.249760686538667009, -6.940565734314625423, 4.007137495034787555 ) ) ;
#25920=EDGE_CURVE ( 'NONE', #19637, #30369, #30571, .T. ) ;
#25925=EDGE_CURVE ( 'NONE', #22609, #19221, #9166, .T. ) ;
#25931=ORIENTED_EDGE ( 'NONE', *, *, #6222, .F. ) ;
#25936=EDGE_CURVE ( 'NONE', #32347, #19255, #20418, .T. ) ;
#25941=CARTESIAN_POINT ( 'NONE',  ( 5.377543748152550762, -7.530955069117533540, 2.741043480754901118 ) ) ;
#25955=B_SPLINE_CURVE_WITH_KNOTS ( 'NONE', 3,
 ( #20213, #2002, #24726, #30409, #9851, #5015, #25396, #2505, #14692, #27410 ),
 .UNSPECIFIED., .F., .F.,
 ( 4, 2, 2, 2, 4 ),
 ( 3.512955446118267852E-07, 0.0005479535487287104769, 0.001095555801912809170, 0.001643158055096907971, 0.002190760308281006555 ),
 .UNSPECIFIED. ) ;
#25970=CARTESIAN_POINT ( 'NONE',  ( 5.489343555808772201, -8.118190043691528857, 0.1039150536218743925 ) ) ;
#25973=ORIENTED_EDGE ( 'NONE', *, *, #21231, .F. ) ;
#25974=CARTESIAN_POINT ( 'NONE',  ( 4.749760686538667009, 4.007137495034812424, 6.940565734314612101 ) ) ;
#25975=ORIENTED_EDGE ( 'NONE', *, *, #22719, .F. ) ;
#25979=ORIENTED_EDGE ( 'NONE', *, *, #3941, .T. ) ;
#25982=CARTESIAN_POINT ( 'NONE',  ( 7.249760686538667009, -7.892520144992443143, 1.391664247347202288 ) ) ;
#25991=CARTESIAN_POINT ( 'NONE',  ( 0.000000000000000000, -6.700937042937072263, 2.183447440113167826 ) ) ;
#25993=CARTESIAN_POINT ( 'NONE',  ( -8.000050800000000351, 0.3588475416126519768, -3.414206294404568798 ) ) ;
#26001=CARTESIAN_POINT ( 'NONE',  ( 7.064423600674403225, -8.711672189282625212, -0.8180878109954319299 ) ) ;
#26007=CARTESIAN_POINT ( 'NONE',  ( -2.400050802731187094, -3.113457007523259268, 0.9222479816126455399 ) ) ;
#26019=VERTEX_POINT ( 'NONE', #17219 ) ;
#26029=( BOUNDED_CURVE ( )  B_SPLINE_CURVE ( 2, ( #5878, #3408, #3082, #6063, #8880, #3228, #16066, #16253, #28782, #23438, #23926 ),
 .UNSPECIFIED., .F., .F. ) 
 B_SPLINE_CURVE_WITH_KNOTS ( ( 3, 2, 2, 2, 2, 3 ),
 ( 0.5603822619934377691, 0.5625000000000000000, 0.5781250000000000000, 0.5937500000000000000, 0.6093750000000000000, 0.6228822619934377691 ),
 .UNSPECIFIED. ) 
 CURVE ( )  GEOMETRIC_REPRESENTATION_ITEM ( )  RATIONAL_B_SPLINE_CURVE ( ( 0.9821626249036861100, 0.9896829947469995004, 1.000000000000000000, 0.9238795325112867385, 1.000000000000000000, 0.9238795325112867385, 1.000000000000000000, 0.9238795325112867385, 1.000000000000000000, 0.9341965377642872381, 0.9821626249036861100 ) ) 
 REPRESENTATION_ITEM ( '' )  );
#26039=CARTESIAN_POINT ( 'NONE',  ( -2.762550801365593500, -2.752080473201636845, 2.228590825266444586 ) ) ;
#26041=B_SPLINE_CURVE_WITH_KNOTS ( 'NONE', 3,
 ( #1471, #32055, #6458, #3991, #24355, #24503, #11329, #11647, #31747, #14305 ),
 .UNSPECIFIED., .F., .F.,
 ( 4, 2, 2, 2, 4 ),
 ( 2.740849916258459394E-07, 0.0005478761651001745094, 0.001095478245208723325, 0.001643080325317272140, 0.002190682405425820739 ),
 .UNSPECIFIED. ) ;
#26042=CARTESIAN_POINT ( 'NONE',  ( -3.604531657079157903, 2.325406398514293205, -1.883076972206379374 ) ) ;
#26046=ORIENTED_EDGE ( 'NONE', *, *, #25551, .T. ) ;
#26053=EDGE_CURVE ( 'NONE', #10466, #112, #24553, .T. ) ;
#26055=DIRECTION ( 'NONE',  ( -0.000000000000000000, 0.9961946980917454342, 0.08715574274765873486 ) ) ;
#26056=CARTESIAN_POINT ( 'NONE',  ( 6.883866557622099869, 8.415306967752711031, -2.328663417917355982 ) ) ;
#26059=CARTESIAN_POINT ( 'NONE',  ( 3.499999999999999556, 5.471841788314750765, -3.018103451449674068 ) ) ;
#26062=ORIENTED_EDGE ( 'NONE', *, *, #11202, .F. ) ;
#26063=CARTESIAN_POINT ( 'NONE',  ( -4.512550801365592612, 1.088641768524161613, 3.675193018007247403 ) ) ;
#26065=CARTESIAN_POINT ( 'NONE',  ( 7.249760686538667009, 2.741043480755029016, -7.530955069117485579 ) ) ;
#26066=ORIENTED_EDGE ( 'NONE', *, *, #11231, .F. ) ;
#26067=ORIENTED_EDGE ( 'NONE', *, *, #12990, .T. ) ;
#26068=CARTESIAN_POINT ( 'NONE',  ( 7.249760686538667009, -7.530955069117533540, 2.741043480754901118 ) ) ;
#26069=DIRECTION ( 'NONE',  ( 1.000000000000000000, -0.000000000000000000, -0.000000000000000000 ) ) ;
#26076=ORIENTED_EDGE ( 'NONE', *, *, #5808, .F. ) ;
#26082=VERTEX_POINT ( 'NONE', #9181 ) ;
#26084=ORIENTED_EDGE ( 'NONE', *, *, #6947, .T. ) ;
#26087=ORIENTED_EDGE ( 'NONE', *, *, #8186, .F. ) ;
#26091=CARTESIAN_POINT ( 'NONE',  ( -3.462550801365593678, -3.521866450007987037, -0.3701630799359323931 ) ) ;
#26095=ORIENTED_EDGE ( 'NONE', *, *, #14674, .T. ) ;
#26103=ORIENTED_EDGE ( 'NONE', *, *, #9855, .T. ) ;
#26104=CARTESIAN_POINT ( 'NONE',  ( 5.377543748152548986, -1.391664247347174754, -7.892520144992448472 ) ) ;
#26118=EDGE_CURVE ( 'NONE', #13402, #4337, #983, .T. ) ;
#26120=CARTESIAN_POINT ( 'NONE',  ( 7.249760686538667009, 6.940565734314597002, 4.007137495034836405 ) ) ;
#26122=EDGE_CURVE ( 'NONE', #19255, #1082, #16193, .T. ) ;
#26124=B_SPLINE_CURVE_WITH_KNOTS ( 'NONE', 3,
 ( #9781, #30350, #7421, #27825, #2767, #32872, #12762, #15287, #17808, #22968 ),
 .UNSPECIFIED., .F., .F.,
 ( 4, 2, 2, 2, 4 ),
 ( 3.032460776715785715E-07, 0.0005479053915603962011, 0.001095507537043120816, 0.001643109682525845322, 0.002190711828008569829 ),
 .UNSPECIFIED. ) ;
#26126=ORIENTED_EDGE ( 'NONE', *, *, #28624, .T. ) ;
#26127=DIRECTION ( 'NONE',  ( -1.000000000000000000, -0.000000000000000000, -0.000000000000000000 ) ) ;
#26136=DIRECTION ( 'NONE',  ( -1.000000000000000000, 0.000000000000000000, 0.000000000000000000 ) ) ;
#26148=AXIS2_PLACEMENT_3D ( 'NONE', #6915, #17303, #1765 ) ;
#26162=ADVANCED_FACE ( 'NONE', ( #5823 ), #11163, .F. ) ;
#26163=CIRCLE ( 'NONE', #23477, 2.999999999999999556 ) ;
#26169=ORIENTED_EDGE ( 'NONE', *, *, #14859, .F. ) ;
#26170=ORIENTED_EDGE ( 'NONE', *, *, #7251, .F. ) ;
#26174=CARTESIAN_POINT ( 'NONE',  ( 5.377543748152548098, 8.385837730238846314E-14, -8.014274990069656823 ) ) ;
#26176=ORIENTED_EDGE ( 'NONE', *, *, #3209, .T. ) ;
#26179=CARTESIAN_POINT ( 'NONE',  ( 3.499999999999999556, -5.233522515400055752, -4.720195129223329289 ) ) ;
#26180=DIRECTION ( 'NONE',  ( -1.000000000000000000, 0.000000000000000000, -0.000000000000000000 ) ) ;
#26184=CARTESIAN_POINT ( 'NONE',  ( 0.000000000000000000, 0.000000000000000000, 0.000000000000000000 ) ) ;
#26187=DIRECTION ( 'NONE',  ( 0.000000000000000000, 0.000000000000000000, 1.000000000000000000 ) ) ;
#26193=CIRCLE ( 'NONE', #11754, 2.999999999999999556 ) ;
#26195=CARTESIAN_POINT ( 'NONE',  ( -3.612550801365593589, -1.828967928396026510, 3.368539882008728004 ) ) ;
#26198=CARTESIAN_POINT ( 'NONE',  ( -4.354531657079157903, 3.105402419394639235, -0.9198621039125850496 ) ) ;
#26201=CYLINDRICAL_SURFACE ( 'NONE', #25279, 2.999999999999999112 ) ;
#26206=CARTESIAN_POINT ( 'NONE',  ( 7.249760686538667009, -6.139290821770219786, -5.151476664237539360 ) ) ;
#26211=CIRCLE ( 'NONE', #9625, 6.248999999999999666 ) ;
#26213=AXIS2_PLACEMENT_3D ( 'NONE', #9667, #6996, #22069 ) ;
#26214=CARTESIAN_POINT ( 'NONE',  ( 6.037141879243262288, 6.770886333893425757, 5.096219216992873058 ) ) ;
#26216=LINE ( 'NONE', #28876, #21040 ) ;
#26218=CARTESIAN_POINT ( 'NONE',  ( 1.750000000000000222, 8.357095590591338663, 1.552080310331533486 ) ) ;
#26222=VERTEX_POINT ( 'NONE', #21068 ) ;
#26223=CARTESIAN_POINT ( 'NONE',  ( -4.312550801365593323, -3.675193018007246071, 1.088641768524163167 ) ) ;
#26227=EDGE_LOOP ( 'NONE', ( #1619, #21892, #26103, #22056 ) ) ;
#26228=CARTESIAN_POINT ( 'NONE',  ( 3.499999999999999556, -5.233522515400120589, 4.720195129223259123 ) ) ;
#26234=AXIS2_PLACEMENT_3D ( 'NONE', #27817, #28801, #13112 ) ;
#26236=CARTESIAN_POINT ( 'NONE',  ( 7.249760686538667009, -4.007137495034764463, -6.940565734314639634 ) ) ;
#26238=CARTESIAN_POINT ( 'NONE',  ( -1.841338014675546475, 0.2391638310232261089, 3.112837935894453345 ) ) ;
#26241=CARTESIAN_POINT ( 'NONE',  ( -3.887550801365593500, 2.228590825266444142, 2.752080473201636845 ) ) ;
#26244=ORIENTED_EDGE ( 'NONE', *, *, #15136, .F. ) ;
#26245=CIRCLE ( 'NONE', #30529, 6.248999999999999666 ) ;
#26246=VERTEX_POINT ( 'NONE', #13673 ) ;
#26250=ORIENTED_EDGE ( 'NONE', *, *, #13637, .F. ) ;
#26254=VERTEX_POINT ( 'NONE', #4000 ) ;
#26256=CARTESIAN_POINT ( 'NONE',  ( -5.562550801365593323, 2.752080473201636845, -2.228590825266444142 ) ) ;
#26259=VECTOR ( 'NONE', #18958, 1000.000000000000000 ) ;
#26260=CARTESIAN_POINT ( 'NONE',  ( 1.750000000000000222, 7.003298780661427969, 4.817032923780590892 ) ) ;
#26261=CARTESIAN_POINT ( 'NONE',  ( 5.489343958331427409, 7.593062460271035263, -2.874233210898287538 ) ) ;
#26263=CARTESIAN_POINT ( 'NONE',  ( -6.887550801365593500, -2.752080473201636845, 2.228590825266444586 ) ) ;
#26268=AXIS2_PLACEMENT_3D ( 'NONE', #28111, #2702, #2899 ) ;
#26275=CARTESIAN_POINT ( 'NONE',  ( 7.249760686538667009, 2.210816291636212405, 8.466096581343489191 ) ) ;
#26281=CARTESIAN_POINT ( 'NONE',  ( 7.249760686538667009, 0.000000000000000000, 0.000000000000000000 ) ) ;
#26284=VECTOR ( 'NONE', #32420, 1000.000000000000000 ) ;
#26288=( BOUNDED_CURVE ( )  B_SPLINE_CURVE ( 2, ( #31469, #31323, #29130, #19091, #8548, #6216, #21606 ),
 .UNSPECIFIED., .F., .F. ) 
 B_SPLINE_CURVE_WITH_KNOTS ( ( 3, 2, 2, 3 ),
 ( 0.07856246879372839886, 0.09375000000000000000, 0.1093750000000000000, 0.1228822619934377414 ),
 .UNSPECIFIED. ) 
 CURVE ( )  GEOMETRIC_REPRESENTATION_ITEM ( )  RATIONAL_B_SPLINE_CURVE ( ( 0.9958568977429422819, 0.9260107535730678352, 1.000000000000000000, 0.9238795325112867385, 1.000000000000000000, 0.9341965377642873491, 0.9821626249036861100 ) ) 
 REPRESENTATION_ITEM ( '' )  );
#26292=CARTESIAN_POINT ( 'NONE',  ( 7.249760686538667009, -0.8180878109961253752, -8.711672189281435053 ) ) ;
#26296=ORIENTED_EDGE ( 'NONE', *, *, #19625, .F. ) ;
#26298=B_SPLINE_CURVE_WITH_KNOTS ( 'NONE', 3,
 ( #21049, #15990, #26056, #15845, #18032, #23528, #31254, #12824, #30594, #28071 ),
 .UNSPECIFIED., .F., .F.,
 ( 4, 2, 2, 2, 4 ),
 ( 1.968338519001761812E-07, 0.0005467927057105466870, 0.001093388577569193252, 0.001639984449427839925, 0.002186580321286487900 ),
 .UNSPECIFIED. ) ;
#26304=ORIENTED_EDGE ( 'NONE', *, *, #11508, .F. ) ;
#26307=CARTESIAN_POINT ( 'NONE',  ( 5.377543748152549874, -4.007137495034861274, 6.940565734314584567 ) ) ;
#26310=FACE_OUTER_BOUND ( 'NONE', #27210, .T. ) ;
#26313=CIRCLE ( 'NONE', #15069, 8.500000000000000000 ) ;
#26318=CARTESIAN_POINT ( 'NONE',  ( 6.037141848526922594, 3.315649934461718740, 7.798898458906289299 ) ) ;
#26321=VECTOR ( 'NONE', #23099, 1000.000000000000114 ) ;
#26325=ADVANCED_FACE ( 'NONE', ( #31910 ), #29381, .F. ) ;
#26328=CARTESIAN_POINT ( 'NONE',  ( 5.489344087273876127, 5.138668362895363551, -6.285690376021046077 ) ) ;
#26330=CARTESIAN_POINT ( 'NONE',  ( 5.612718622971681448, -2.996580135471476503, -7.650113768151205029 ) ) ;
#26333=ADVANCED_FACE ( 'NONE', ( #9475 ), #24210, .T. ) ;
#26335=ORIENTED_EDGE ( 'NONE', *, *, #10979, .T. ) ;
#26338=AXIS2_PLACEMENT_3D ( 'NONE', #24525, #14324, #32078 ) ;
#26347=ORIENTED_EDGE ( 'NONE', *, *, #6078, .F. ) ;
#26348=CARTESIAN_POINT ( 'NONE',  ( 6.530491627857222703, 3.540416224243776888, -7.903708701126651803 ) ) ;
#26356=DIRECTION ( 'NONE',  ( 1.000000000000000000, -0.000000000000000000, -0.000000000000000000 ) ) ;
#26361=CARTESIAN_POINT ( 'NONE',  ( 5.887530252753763627, 5.105578361685915390, 6.663910820542600533 ) ) ;
#26363=CIRCLE ( 'NONE', #30123, 8.500000000000000000 ) ;
#26365=CARTESIAN_POINT ( 'NONE',  ( -3.950050800000000528, -3.113457007523259268, 0.9222479816126455399 ) ) ;
#26371=AXIS2_PLACEMENT_3D ( 'NONE', #29304, #26802, #1412 ) ;
#26373=AXIS2_PLACEMENT_3D ( 'NONE', #21785, #31993, #16785 ) ;
#26381=EDGE_CURVE ( 'NONE', #26504, #572, #3827, .T. ) ;
#26382=CARTESIAN_POINT ( 'NONE',  ( -3.012550801365593500, 3.368539882008727115, 1.828967928396026954 ) ) ;
#26384=CARTESIAN_POINT ( 'NONE',  ( -4.850050800000001772, -1.549418761218565477, 2.853674364686380471 ) ) ;
#26389=CARTESIAN_POINT ( 'NONE',  ( 4.749760686538667009, -2.741043480754977946, 7.530955069117504230 ) ) ;
#26398=DIRECTION ( 'NONE',  ( -1.000000000000000000, 0.000000000000000000, -0.000000000000000000 ) ) ;
#26403=CARTESIAN_POINT ( 'NONE',  ( 7.249760686538667009, -8.466096581343496297, 2.210816291636187536 ) ) ;
#26408=CARTESIAN_POINT ( 'NONE',  ( -2.412550801365592967, 1.828967928396027176, -3.368539882008727115 ) ) ;
#26414=CARTESIAN_POINT ( 'NONE',  ( 0.000000000000000000, 2.429606751577119805, -5.757344182232886354 ) ) ;
#26416=DIRECTION ( 'NONE',  ( -1.000000000000000000, 0.000000000000000000, 0.000000000000000000 ) ) ;
#26417=CARTESIAN_POINT ( 'NONE',  ( 1.750000000000000222, -7.673322273190749776, 3.656518192455051608 ) ) ;
#26419=DIRECTION ( 'NONE',  ( 0.000000000000000000, 0.8660254037844362651, 0.5000000000000039968 ) ) ;
#26421=CARTESIAN_POINT ( 'NONE',  ( -3.337550801365593678, 1.828967928396027398, -3.368539882008727115 ) ) ;
#26431=CIRCLE ( 'NONE', #7212, 8.500000000000000000 ) ;
#26433=VERTEX_POINT ( 'NONE', #32260 ) ;
#26438=CARTESIAN_POINT ( 'NONE',  ( -3.312550801365593767, -1.088641768524163611, -3.675193018007245627 ) ) ;
#26444=CARTESIAN_POINT ( 'NONE',  ( -6.687550801365594211, -2.228590825266444586, -2.752080473201636401 ) ) ;
#26449=DIRECTION ( 'NONE',  ( 0.000000000000000000, 0.000000000000000000, 1.000000000000000000 ) ) ;
#26456=DIRECTION ( 'NONE',  ( 0.000000000000000000, 0.4067366430758009299, -0.9135454576426005335 ) ) ;
#26458=CARTESIAN_POINT ( 'NONE',  ( -6.837550801365593678, -3.675193018007246071, 1.088641768524163167 ) ) ;
#26461=LINE ( 'NONE', #23922, #18659 ) ;
#26464=ORIENTED_EDGE ( 'NONE', *, *, #13332, .F. ) ;
#26469=ORIENTED_EDGE ( 'NONE', *, *, #1821, .T. ) ;
#26470=ORIENTED_EDGE ( 'NONE', *, *, #20856, .T. ) ;
#26488=CARTESIAN_POINT ( 'NONE',  ( 7.249760686538667009, 0.000000000000000000, 0.000000000000000000 ) ) ;
#26495=ORIENTED_EDGE ( 'NONE', *, *, #25876, .T. ) ;
#26504=VERTEX_POINT ( 'NONE', #3300 ) ;
#26515=LINE ( 'NONE', #1586, #27428 ) ;
#26518=EDGE_CURVE ( 'NONE', #533, #33011, #3874, .T. ) ;
#26524=CARTESIAN_POINT ( 'NONE',  ( 5.489344087273876127, -6.285690376021061176, -5.138668362895343122 ) ) ;
#26527=CARTESIAN_POINT ( 'NONE',  ( -3.312550801365593767, -1.088641768524163389, -3.675193018007246071 ) ) ;
#26528=VERTEX_POINT ( 'NONE', #8311 ) ;
#26529=CARTESIAN_POINT ( 'NONE',  ( -7.550050800000000173, 3.113457007523260156, -0.9222479816126439855 ) ) ;
#26534=DIRECTION ( 'NONE',  ( -1.000000000000000000, -0.000000000000000000, -0.000000000000000000 ) ) ;
#26541=DIRECTION ( 'NONE',  ( 1.000000000000000000, 0.000000000000000000, 0.000000000000000000 ) ) ;
#26549=PLANE ( 'NONE',  #11752 ) ;
#26551=CARTESIAN_POINT ( 'NONE',  ( -3.512550801365593944, -3.675193018007246071, 1.088641768524163167 ) ) ;
#26555=EDGE_CURVE ( 'NONE', #17821, #13648, #16150, .T. ) ;
#26563=CARTESIAN_POINT ( 'NONE',  ( 5.885541736258997680, 2.519172009312041105, -8.006759975090627535 ) ) ;
#26564=CARTESIAN_POINT ( 'NONE',  ( -2.124956573341760357, 1.323625320507108460, 3.284597389080124774 ) ) ;
#26565=CARTESIAN_POINT ( 'NONE',  ( -2.837550801365593678, -3.675193018007245627, 1.088641768524163389 ) ) ;
#26577=CARTESIAN_POINT ( 'NONE',  ( -8.000050800000000351, 0.000000000000000000, 0.000000000000000000 ) ) ;
#26581=CARTESIAN_POINT ( 'NONE',  ( -5.912550801365594744, -3.675193018007245627, 1.088641768524163389 ) ) ;
#26583=CARTESIAN_POINT ( 'NONE',  ( -3.712942406915326288, 4.884725290497410777E-15, -2.999999999999999556 ) ) ;
#26586=CARTESIAN_POINT ( 'NONE',  ( -6.587550801365593678, 0.3701630799359330593, -3.521866450007987037 ) ) ;
#26589=DIRECTION ( 'NONE',  ( 0.000000000000000000, 0.7431448254773954654, -0.6691306063588569053 ) ) ;
#26592=EDGE_CURVE ( 'NONE', #32541, #5615, #1291, .T. ) ;
#26605=EDGE_CURVE ( 'NONE', #9995, #5270, #22559, .T. ) ;
#26613=VERTEX_POINT ( 'NONE', #11469 ) ;
#26618=ORIENTED_EDGE ( 'NONE', *, *, #25703, .T. ) ;
#26627=CARTESIAN_POINT ( 'NONE',  ( -3.050050800000000617, -2.853674364686378695, -1.549418761218566809 ) ) ;
#26637=CARTESIAN_POINT ( 'NONE',  ( -8.000050800000000351, 0.6450660259192652068, -3.401635239564149593 ) ) ;
#26641=ORIENTED_EDGE ( 'NONE', *, *, #26122, .T. ) ;
#26650=LINE ( 'NONE', #21491, #22434 ) ;
#26657=AXIS2_PLACEMENT_3D ( 'NONE', #9543, #11727, #17420 ) ;
#26663=CARTESIAN_POINT ( 'NONE',  ( 5.377543748152548098, 7.530955069117513112, 2.741043480754951744 ) ) ;
#26668=CARTESIAN_POINT ( 'NONE',  ( -5.750050802731187183, -0.3135853898029607456, 2.983565686104819648 ) ) ;
#26669=ORIENTED_EDGE ( 'NONE', *, *, #5130, .F. ) ;
#26670=CARTESIAN_POINT ( 'NONE',  ( -5.200050800000000528, 2.331437884370912705, -1.887961173149511618 ) ) ;
#26672=VECTOR ( 'NONE', #22257, 1000.000000000000000 ) ;
#26675=DIRECTION ( 'NONE',  ( 0.000000000000000000, -0.5735764363510469366, -0.8191520442889912434 ) ) ;
#26676=ORIENTED_EDGE ( 'NONE', *, *, #18751, .T. ) ;
#26677=CARTESIAN_POINT ( 'NONE',  ( -7.100050799999999995, -2.983565686104819648, -0.3135853898029605791 ) ) ;
#26678=CIRCLE ( 'NONE', #16527, 8.500000000000000000 ) ;
#26682=VERTEX_POINT ( 'NONE', #24166 ) ;
#26684=FACE_OUTER_BOUND ( 'NONE', #4946, .T. ) ;
#26689=DIRECTION ( 'NONE',  ( -1.000000000000000000, -0.000000000000000000, -0.000000000000000000 ) ) ;
#26691=CARTESIAN_POINT ( 'NONE',  ( 0.000000000000000000, 4.137773741518454784, -5.705158055754753654 ) ) ;
#26694=ORIENTED_EDGE ( 'NONE', *, *, #32465, .T. ) ;
#26702=DIRECTION ( 'NONE',  ( -1.000000000000000000, 0.000000000000000000, 0.000000000000000000 ) ) ;
#26706=ORIENTED_EDGE ( 'NONE', *, *, #6947, .F. ) ;
#26714=CARTESIAN_POINT ( 'NONE',  ( -3.937550801365593323, 3.368539882008727115, 1.828967928396027176 ) ) ;
#26722=VECTOR ( 'NONE', #71, 999.9999999999998863 ) ;
#26726=ADVANCED_FACE ( 'NONE', ( #20450 ), #25452, .F. ) ;
#26727=CIRCLE ( 'NONE', #30503, 8.750000000000000000 ) ;
#26732=ORIENTED_EDGE ( 'NONE', *, *, #21351, .F. ) ;
#26733=CARTESIAN_POINT ( 'NONE',  ( 6.883866621640343908, 6.224335161395018190, 6.123537914202261234 ) ) ;
#26734=CARTESIAN_POINT ( 'NONE',  ( -5.262550801365593500, -0.3701630799359326152, 3.521866450007987037 ) ) ;
#26739=CARTESIAN_POINT ( 'NONE',  ( -5.487550801365593145, 2.228590825266444142, 2.752080473201636845 ) ) ;
#26741=CARTESIAN_POINT ( 'NONE',  ( 6.038144853276842916, 1.911563584435307162, -8.256557579931646629 ) ) ;
#26744=CARTESIAN_POINT ( 'NONE',  ( 5.489321676144492734, -6.978593840069416743, -4.149060317827578892 ) ) ;
#26745=ORIENTED_EDGE ( 'NONE', *, *, #30625, .T. ) ;
#26747=AXIS2_PLACEMENT_3D ( 'NONE', #29073, #28726, #15999 ) ;
#26751=EDGE_CURVE ( 'NONE', #5304, #24201, #11336, .T. ) ;
#26757=CARTESIAN_POINT ( 'NONE',  ( 5.377543748152548098, 8.385837730238846314E-14, -8.014274990069656823 ) ) ;
#26758=CARTESIAN_POINT ( 'NONE',  ( -3.237550801365593589, 3.675193018007247403, -1.088641768524161391 ) ) ;
#26771=AXIS2_PLACEMENT_3D ( 'NONE', #32245, #9308, #3806 ) ;
#26786=FACE_OUTER_BOUND ( 'NONE', #24223, .T. ) ;
#26788=CARTESIAN_POINT ( 'NONE',  ( -2.962942409646513564, 4.884725290497410777E-15, -2.999999999999999556 ) ) ;
#26790=CARTESIAN_POINT ( 'NONE',  ( 7.249760686538667009, 3.647351267791570262, 7.953573330858228374 ) ) ;
#26802=DIRECTION ( 'NONE',  ( 0.000000000000000000, -0.8191520442889927978, -0.5735764363510448272 ) ) ;
#26806=CARTESIAN_POINT ( 'NONE',  ( -8.000050800000000351, 0.3588475416126519768, -3.414206294404568798 ) ) ;
#26809=CARTESIAN_POINT ( 'NONE',  ( 6.357668022120091855, 6.947679035623525401, -5.080751859797282499 ) ) ;
#26812=ORIENTED_EDGE ( 'NONE', *, *, #16861, .F. ) ;
#26814=CIRCLE ( 'NONE', #18285, 2.999999999999999556 ) ;
#26815=CARTESIAN_POINT ( 'NONE',  ( 3.499999999999999556, -4.724769925181146135, -4.089810527897805414 ) ) ;
#26816=ORIENTED_EDGE ( 'NONE', *, *, #21617, .T. ) ;
#26819=AXIS2_PLACEMENT_3D ( 'NONE', #26281, #22933, #21111 ) ;
#26824=VERTEX_POINT ( 'NONE', #3067 ) ;
#26830=CARTESIAN_POINT ( 'NONE',  ( 6.883866482134012976, 0.8319830743950653584, 8.691827696555161964 ) ) ;
#26831=DIRECTION ( 'NONE',  ( 1.000000000000000000, -0.000000000000000000, -0.000000000000000000 ) ) ;
#26833=CIRCLE ( 'NONE', #15086, 2.999999999999998668 ) ;
#26838=CARTESIAN_POINT ( 'NONE',  ( 3.500000000000000000, 0.000000000000000000, 6.000000000000000000 ) ) ;
#26840=VECTOR ( 'NONE', #30951, 999.9999999999998863 ) ;
#26845=LINE ( 'NONE', #19325, #3873 ) ;
#26846=CARTESIAN_POINT ( 'NONE',  ( -5.800050802731187005, 0.9222479816126443186, 3.113457007523260156 ) ) ;
#26850=CARTESIAN_POINT ( 'NONE',  ( -7.700050800000000528, 0.3135853898029611342, -2.983565686104819648 ) ) ;
#26856=LINE ( 'NONE', #29703, #719 ) ;
#26857=ORIENTED_EDGE ( 'NONE', *, *, #24656, .T. ) ;
#26860=CARTESIAN_POINT ( 'NONE',  ( 5.885541838704151374, 5.674471607902439985, 6.185046950422337986 ) ) ;
#26863=CARTESIAN_POINT ( 'NONE',  ( -5.800050800000000173, 1.887961173149511618, 2.331437884370912705 ) ) ;
#26866=DIRECTION ( 'NONE',  ( -1.000000000000000000, 0.000000000000000000, 0.000000000000000000 ) ) ;
#26867=CARTESIAN_POINT ( 'NONE',  ( 0.000000000000000000, 5.241389472434663688, 4.711457988287072851 ) ) ;
#26868=AXIS2_PLACEMENT_3D ( 'NONE', #29195, #6283, #14139 ) ;
#26869=EDGE_LOOP ( 'NONE', ( #10198, #8409, #6867, #11518 ) ) ;
#26871=ADVANCED_FACE ( 'NONE', ( #23422 ), #9731, .T. ) ;
#26876=AXIS2_PLACEMENT_3D ( 'NONE', #6035, #16231, #26589 ) ;
#26881=DIRECTION ( 'NONE',  ( -1.000000000000000000, 0.000000000000000000, -0.000000000000000000 ) ) ;
#26897=AXIS2_PLACEMENT_3D ( 'NONE', #27033, #26689, #19678 ) ;
#26898=( BOUNDED_CURVE ( )  B_SPLINE_CURVE ( 2, ( #21139, #15788, #14202, #16089, #11695, #8271, #21893, #8086, #5608, #3251, #564 ),
 .UNSPECIFIED., .F., .F. ) 
 B_SPLINE_CURVE_WITH_KNOTS ( ( 3, 2, 2, 2, 2, 3 ),
 ( 0.2478822619934377414, 0.2500000000000000000, 0.2656250000000000000, 0.2812500000000000000, 0.2968750000000000000, 0.3103822619934377136 ),
 .UNSPECIFIED. ) 
 CURVE ( )  GEOMETRIC_REPRESENTATION_ITEM ( )  RATIONAL_B_SPLINE_CURVE ( ( 0.9821626249036861100, 0.9896829947469993893, 1.000000000000000000, 0.9238795325112867385, 1.000000000000000000, 0.9238795325112867385, 1.000000000000000000, 0.9238795325112867385, 1.000000000000000000, 0.9341965377642874602, 0.9821626249036857770 ) ) 
 REPRESENTATION_ITEM ( '' )  );
#26903=EDGE_LOOP ( 'NONE', ( #21998, #30140, #8551 ) ) ;
#26913=CARTESIAN_POINT ( 'NONE',  ( 5.377543748152548986, 4.007137495034812424, 6.940565734314612101 ) ) ;
#26915=ORIENTED_EDGE ( 'NONE', *, *, #28979, .T. ) ;
#26916=DIRECTION ( 'NONE',  ( 0.000000000000000000, 0.4226182617406930020, 0.9063077870366529343 ) ) ;
#26917=LINE ( 'NONE', #27067, #608 ) ;
#26923=CARTESIAN_POINT ( 'NONE',  ( -7.937550801365594211, 3.368539882008727115, 1.828967928396026954 ) ) ;
#26924=DIRECTION ( 'NONE',  ( 0.000000000000000000, 0.000000000000000000, -1.000000000000000000 ) ) ;
#26925=EDGE_CURVE ( 'NONE', #9445, #16287, #13453, .T. ) ;
#26927=DIRECTION ( 'NONE',  ( 1.000000000000000000, -0.000000000000000000, -0.000000000000000000 ) ) ;
#26928=ORIENTED_EDGE ( 'NONE', *, *, #13019, .F. ) ;
#26931=DIRECTION ( 'NONE',  ( 0.000000000000000000, 0.2588190451025139671, 0.9659258262890701996 ) ) ;
#26945=EDGE_CURVE ( 'NONE', #19623, #12441, #19073, .T. ) ;
#26947=CARTESIAN_POINT ( 'NONE',  ( -3.500050800000000351, 2.983565686104819648, 0.3135853898029609677 ) ) ;
#26948=CARTESIAN_POINT ( 'NONE',  ( 5.489321676144491846, -7.082488557107319949, 3.969109389279940725 ) ) ;
#26950=DIRECTION ( 'NONE',  ( 1.000000000000000000, 0.000000000000000000, 0.000000000000000000 ) ) ;
#26959=CARTESIAN_POINT ( 'NONE',  ( 4.749760686538667009, -2.741043480754877582, -7.530955069117540646 ) ) ;
#26968=VERTEX_POINT ( 'NONE', #18925 ) ;
#26976=CARTESIAN_POINT ( 'NONE',  ( -6.512942406915326110, 3.284080845023683730E-15, 3.000000000000000000 ) ) ;
#26977=DIRECTION ( 'NONE',  ( -1.000000000000000000, -0.000000000000000000, 0.000000000000000000 ) ) ;
#26978=CARTESIAN_POINT ( 'NONE',  ( 3.499999999999999556, 3.771202944355708020, 4.982773259188384429 ) ) ;
#26985=EDGE_LOOP ( 'NONE', ( #22112, #6369, #21947, #19029 ) ) ;
#26986=VERTEX_POINT ( 'NONE', #18580 ) ;
#26989=CARTESIAN_POINT ( 'NONE',  ( 0.000000000000000000, -5.233522515400120589, 4.720195129223259123 ) ) ;
#27006=DIRECTION ( 'NONE',  ( -0.000000000000000000, -0.9659258262890700886, 0.2588190451025139116 ) ) ;
#27013=CARTESIAN_POINT ( 'NONE',  ( -5.600050802731187716, -3.113457007523259268, 0.9222479816126455399 ) ) ;
#27015=CARTESIAN_POINT ( 'NONE',  ( -5.800050800000000173, 1.887961173149511618, 2.331437884370912705 ) ) ;
#27017=CARTESIAN_POINT ( 'NONE',  ( -5.750050802731187183, -0.3135853898029607456, 2.983565686104819648 ) ) ;
#27033=CARTESIAN_POINT ( 'NONE',  ( 0.000000000000000000, 0.000000000000000000, 0.000000000000000000 ) ) ;
#27038=DIRECTION ( 'NONE',  ( 0.000000000000000000, -0.4067366430757887730, -0.9135454576426058626 ) ) ;
#27046=DIRECTION ( 'NONE',  ( 0.000000000000000000, 0.000000000000000000, 1.000000000000000000 ) ) ;
#27047=ORIENTED_EDGE ( 'NONE', *, *, #9962, .F. ) ;
#27048=CARTESIAN_POINT ( 'NONE',  ( -2.850050802731187716, 2.331437884370912705, -1.887961173149511618 ) ) ;
#27049=ORIENTED_EDGE ( 'NONE', *, *, #6291, .T. ) ;
#27050=CARTESIAN_POINT ( 'NONE',  ( 5.377543748152549874, 2.741043480755029016, -7.530955069117485579 ) ) ;
#27051=CARTESIAN_POINT ( 'NONE',  ( 7.249760686538667009, -8.437262856154180923, 2.318425219014200511 ) ) ;
#27052=DIRECTION ( 'NONE',  ( -1.000000000000000000, -0.000000000000000000, 0.000000000000000000 ) ) ;
#27062=CARTESIAN_POINT ( 'NONE',  ( -3.450050802731187805, 1.887961173149511618, 2.331437884370912705 ) ) ;
#27063=CARTESIAN_POINT ( 'NONE',  ( 6.037141879243264064, 6.194548269014965136, -5.783072176360581018 ) ) ;
#27064=VERTEX_POINT ( 'NONE', #5680 ) ;
#27067=CARTESIAN_POINT ( 'NONE',  ( 4.749760686538667009, 1.391664247347228045, 7.892520144992438702 ) ) ;
#27070=CARTESIAN_POINT ( 'NONE',  ( 0.000000000000000000, -2.417132211460119251, 8.149077976821791580 ) ) ;
#27072=CARTESIAN_POINT ( 'NONE',  ( -4.487550801365593145, -2.752080473201636845, 2.228590825266444586 ) ) ;
#27073=DIRECTION ( 'NONE',  ( 1.000000000000000000, -0.000000000000000000, -0.000000000000000000 ) ) ;
#27077=CARTESIAN_POINT ( 'NONE',  ( 6.883866601413089370, -7.193114723270776167, -4.949663153219604261 ) ) ;
#27104=DIRECTION ( 'NONE',  ( -1.000000000000000000, 0.000000000000000000, 0.000000000000000000 ) ) ;
#27109=DIRECTION ( 'NONE',  ( -1.000000000000000000, 0.000000000000000000, 0.000000000000000000 ) ) ;
#27122=ORIENTED_EDGE ( 'NONE', *, *, #7638, .F. ) ;
#27123=FACE_OUTER_BOUND ( 'NONE', #15567, .T. ) ;
#27124=EDGE_CURVE ( 'NONE', #508, #12143, #31662, .T. ) ;
#27128=ORIENTED_EDGE ( 'NONE', *, *, #30763, .T. ) ;
#27140=ORIENTED_EDGE ( 'NONE', *, *, #20954, .F. ) ;
#27148=CARTESIAN_POINT ( 'NONE',  ( 5.489321606599603776, -7.664118171219017839, 2.678948506461303225 ) ) ;
#27152=FACE_OUTER_BOUND ( 'NONE', #24518, .T. ) ;
#27157=CARTESIAN_POINT ( 'NONE',  ( -2.124956573341760357, 1.323625320507108460, 3.284597389080124774 ) ) ;
#27159=DIRECTION ( 'NONE',  ( -1.000000000000000000, -0.000000000000000000, 0.000000000000000000 ) ) ;
#27160=EDGE_CURVE ( 'NONE', #18803, #21638, #13333, .T. ) ;
#27162=EDGE_CURVE ( 'NONE', #31497, #28488, #6313, .T. ) ;
#27163=CARTESIAN_POINT ( 'NONE',  ( -5.950050802731187360, 2.983565686104819648, 0.3135853898029609677 ) ) ;
#27164=ORIENTED_EDGE ( 'NONE', *, *, #18765, .T. ) ;
#27165=CARTESIAN_POINT ( 'NONE',  ( -4.550050800000000173, -0.9222479816126459840, -3.113457007523259268 ) ) ;
#27167=CARTESIAN_POINT ( 'NONE',  ( -5.550050802731187893, -2.983565686104819648, -0.3135853898029605791 ) ) ;
#27168=CARTESIAN_POINT ( 'NONE',  ( -4.250050800000000351, 2.853674364686379583, 1.549418761218565921 ) ) ;
#27170=CARTESIAN_POINT ( 'NONE',  ( -2.100050802731187272, 1.549418761218566143, -2.853674364686379583 ) ) ;
#27182=CARTESIAN_POINT ( 'NONE',  ( 7.064632879756603145, -2.210816291636270137, 8.466096581343476757 ) ) ;
#27184=ORIENTED_EDGE ( 'NONE', *, *, #3599, .F. ) ;
#27194=ADVANCED_FACE ( 'NONE', ( #21219 ), #31417, .T. ) ;
#27197=LINE ( 'NONE', #29731, #20397 ) ;
#27198=CARTESIAN_POINT ( 'NONE',  ( 4.749760686538667009, -6.139290821770289064, 5.151476664237455871 ) ) ;
#27199=CARTESIAN_POINT ( 'NONE',  ( 3.499999999999999556, -3.573533178329615367, 5.126388750707211450 ) ) ;
#27200=AXIS2_PLACEMENT_3D ( 'NONE', #22299, #24454, #19480 ) ;
#27201=ORIENTED_EDGE ( 'NONE', *, *, #8383, .F. ) ;
#27204=CARTESIAN_POINT ( 'NONE',  ( -6.604531657079157903, 1.883076972206379374, 2.325406398514293205 ) ) ;
#27207=DIRECTION ( 'NONE',  ( 0.000000000000000000, -0.1045284632676536235, 0.9945218953682734009 ) ) ;
#27210=EDGE_LOOP ( 'NONE', ( #8329, #6692, #16815 ) ) ;
#27215=B_SPLINE_CURVE_WITH_KNOTS ( 'NONE', 3,
 ( #4660, #30403, #2147, #32766, #9844, #20057, #30252, #27709, #7476, #17681 ),
 .UNSPECIFIED., .F., .F.,
 ( 4, 2, 2, 2, 4 ),
 ( 2.493548413898819905E-07, 0.0005478513795029408152, 0.001095453404164491726, 0.001643055428826042637, 0.002190657453487593331 ),
 .UNSPECIFIED. ) ;
#27218=AXIS2_PLACEMENT_3D ( 'NONE', #8855, #3688, #31937 ) ;
#27228=CARTESIAN_POINT ( 'NONE',  ( 6.880159396099833735, 3.754731129947894708, -7.882559112973126503 ) ) ;
#27229=ORIENTED_EDGE ( 'NONE', *, *, #28979, .F. ) ;
#27230=CARTESIAN_POINT ( 'NONE',  ( -2.687550801365593323, -2.228590825266444586, -2.752080473201636401 ) ) ;
#27259=ORIENTED_EDGE ( 'NONE', *, *, #16861, .T. ) ;
#27274=ORIENTED_EDGE ( 'NONE', *, *, #12981, .T. ) ;
#27279=DIRECTION ( 'NONE',  ( 0.000000000000000000, -0.8660254037844432595, 0.4999999999999918399 ) ) ;
#27280=ADVANCED_FACE ( 'NONE', ( #4315 ), #6479, .T. ) ;
#27286=DIRECTION ( 'NONE',  ( 0.000000000000000000, -0.8191520442889893561, 0.5735764363510496011 ) ) ;
#27288=DIRECTION ( 'NONE',  ( 0.000000000000000000, 0.000000000000000000, -1.000000000000000000 ) ) ;
#27289=CYLINDRICAL_SURFACE ( 'NONE', #27841, 6.248999999999999666 ) ;
#27291=ORIENTED_EDGE ( 'NONE', *, *, #30669, .T. ) ;
#27292=LINE ( 'NONE', #24950, #30039 ) ;
#27296=ORIENTED_EDGE ( 'NONE', *, *, #24923, .T. ) ;
#27297=AXIS2_PLACEMENT_3D ( 'NONE', #15318, #10317, #6963 ) ;
#27302=AXIS2_PLACEMENT_3D ( 'NONE', #4596, #12256, #2432 ) ;
#27305=CIRCLE ( 'NONE', #17160, 6.248999999999999666 ) ;
#27309=EDGE_CURVE ( 'NONE', #18705, #3656, #14644, .T. ) ;
#27311=ORIENTED_EDGE ( 'NONE', *, *, #13721, .F. ) ;
#27314=ORIENTED_EDGE ( 'NONE', *, *, #15244, .F. ) ;
#27319=CARTESIAN_POINT ( 'NONE',  ( -1.756376981307136376, -0.1572233378491262878, 2.999999999999999556 ) ) ;
#27321=EDGE_CURVE ( 'NONE', #18225, #10070, #14931, .T. ) ;
#27329=ADVANCED_FACE ( 'NONE', ( #5305 ), #18388, .F. ) ;
#27330=DIRECTION ( 'NONE',  ( 0.000000000000000000, 0.9510565162951544194, -0.3090169943749448977 ) ) ;
#27332=VECTOR ( 'NONE', #1528, 1000.000000000000000 ) ;
#27339=CARTESIAN_POINT ( 'NONE',  ( -4.350050802731187716, 2.983565686104819648, 0.3135853898029609677 ) ) ;
#27342=CARTESIAN_POINT ( 'NONE',  ( -4.400050799999999818, 2.331437884370912705, -1.887961173149511618 ) ) ;
#27344=CARTESIAN_POINT ( 'NONE',  ( -3.850050802731187272, -1.887961173149512062, -2.331437884370912261 ) ) ;
#27347=DIRECTION ( 'NONE',  ( 0.000000000000000000, -0.2079116908177664480, 0.9781476007338041345 ) ) ;
#27352=AXIS2_PLACEMENT_3D ( 'NONE', #977, #28580, #13987 ) ;
#27357=CARTESIAN_POINT ( 'NONE',  ( 5.612718825656738630, 5.432357446996408434, 6.163864706063968413 ) ) ;
#27365=ORIENTED_EDGE ( 'NONE', *, *, #7767, .T. ) ;
#27369=CARTESIAN_POINT ( 'NONE',  ( 7.249760686538667009, 1.391664247347333294, -7.892520144992419162 ) ) ;
#27380=ADVANCED_FACE ( 'NONE', ( #279 ), #23642, .T. ) ;
#27381=CIRCLE ( 'NONE', #30073, 6.248999999999999666 ) ;
#27384=CARTESIAN_POINT ( 'NONE',  ( 5.377543748152548986, -6.139290821770219786, -5.151476664237539360 ) ) ;
#27385=DIRECTION ( 'NONE',  ( 0.000000000000000000, 0.08715574274765874874, -0.9961946980917455452 ) ) ;
#27387=ORIENTED_EDGE ( 'NONE', *, *, #13752, .T. ) ;
#27392=CARTESIAN_POINT ( 'NONE',  ( -5.454531657079156659, -2.846291840500172921, -1.545410377633947618 ) ) ;
#27396=DIRECTION ( 'NONE',  ( 0.000000000000000000, 0.000000000000000000, 1.000000000000000000 ) ) ;
#27403=AXIS2_PLACEMENT_3D ( 'NONE', #1992, #14681, #9484 ) ;
#27410=CARTESIAN_POINT ( 'NONE',  ( 7.249760686538667009, -0.7071067811864522046, -8.721381771256211834 ) ) ;
#27419=ORIENTED_EDGE ( 'NONE', *, *, #427, .F. ) ;
#27420=CARTESIAN_POINT ( 'NONE',  ( -3.237550801365593589, 3.675193018007247403, -1.088641768524161391 ) ) ;
#27421=FACE_OUTER_BOUND ( 'NONE', #19521, .T. ) ;
#27423=CARTESIAN_POINT ( 'NONE',  ( -8.000050800000000351, 3.673940397442060361E-16, 3.000000000000000444 ) ) ;
#27428=VECTOR ( 'NONE', #26831, 1000.000000000000000 ) ;
#27437=CARTESIAN_POINT ( 'NONE',  ( 6.530491712438077023, 7.168846788212690058, 4.859093986587880387 ) ) ;
#27448=EDGE_CURVE ( 'NONE', #20419, #15831, #3110, .T. ) ;
#27457=DIRECTION ( 'NONE',  ( 0.000000000000000000, -0.5877852522924797984, 0.8090169943749426773 ) ) ;
#27473=DIRECTION ( 'NONE',  ( -1.000000000000000000, 0.000000000000000000, 0.000000000000000000 ) ) ;
#27478=CARTESIAN_POINT ( 'NONE',  ( -7.637550801365593500, -3.675193018007245627, 1.088641768524163389 ) ) ;
#27485=ADVANCED_FACE ( 'NONE', ( #8579 ), #13599, .F. ) ;
#27493=CARTESIAN_POINT ( 'NONE',  ( 7.249760686538667009, -8.721381771256204729, 0.7071067811865423547 ) ) ;
#27502=CARTESIAN_POINT ( 'NONE',  ( 3.499999999999999556, 0.6700234925292691823, 8.473551116235677583 ) ) ;
#27503=CARTESIAN_POINT ( 'NONE',  ( 5.489321289187128805, 8.118169347437836691, 0.1038943573681802152 ) ) ;
#27509=CYLINDRICAL_SURFACE ( 'NONE', #9706, 3.000000000000000000 ) ;
#27512=CARTESIAN_POINT ( 'NONE',  ( -8.000050800000000351, 0.000000000000000000, 0.000000000000000000 ) ) ;
#27513=CARTESIAN_POINT ( 'NONE',  ( -2.650050802731187094, 1.887961173149511618, 2.331437884370912705 ) ) ;
#27514=ORIENTED_EDGE ( 'NONE', *, *, #25752, .F. ) ;
#27515=CARTESIAN_POINT ( 'NONE',  ( -8.087550801365594566, 2.752080473201636845, -2.228590825266444142 ) ) ;
#27516=EDGE_CURVE ( 'NONE', #18705, #17188, #21149, .T. ) ;
#27518=CARTESIAN_POINT ( 'NONE',  ( -4.300050800000000173, 2.983565686104819648, 0.3135853898029609677 ) ) ;
#27521=CARTESIAN_POINT ( 'NONE',  ( 6.037141879243262288, -5.783072176360604111, -6.194548269014942932 ) ) ;
#27525=CARTESIAN_POINT ( 'NONE',  ( -2.906376978575949455, 0.1572233378491263989, -2.999999999999999556 ) ) ;
#27530=CARTESIAN_POINT ( 'NONE',  ( 1.750000000000000000, 8.265874651078044977, -1.981241088980699061 ) ) ;
#27538=CYLINDRICAL_SURFACE ( 'NONE', #16017, 2.999999999999999112 ) ;
#27551=VERTEX_POINT ( 'NONE', #32173 ) ;
#27554=CARTESIAN_POINT ( 'NONE',  ( -6.354531657079158791, -3.105402419394638791, 0.9198621039125867149 ) ) ;
#27562=EDGE_CURVE ( 'NONE', #3016, #3811, #21632, .T. ) ;
#27564=DIRECTION ( 'NONE',  ( 0.000000000000000000, -0.9961946980917449901, -0.08715574274766567375 ) ) ;
#27567=CARTESIAN_POINT ( 'NONE',  ( 5.612974384376776982, 4.279837954023570923, -7.013635602076161213 ) ) ;
#27568=CARTESIAN_POINT ( 'NONE',  ( 6.524595623740806261, 6.215987993068528894, -6.028129343649548666 ) ) ;
#27569=CYLINDRICAL_SURFACE ( 'NONE', #24646, 3.000000000000000444 ) ;
#27571=CARTESIAN_POINT ( 'NONE',  ( -7.362942409646514363, 1.214281993118000652E-15, 3.000000000000000000 ) ) ;
#27578=CARTESIAN_POINT ( 'NONE',  ( -2.937550801365593323, -1.828967928396026510, 3.368539882008728004 ) ) ;
#27586=CARTESIAN_POINT ( 'NONE',  ( -10.00000000000000000, 0.000000000000000000, 0.000000000000000000 ) ) ;
#27588=ADVANCED_FACE ( 'NONE', ( #29153 ), #21465, .T. ) ;
#27598=ORIENTED_EDGE ( 'NONE', *, *, #2472, .F. ) ;
#27599=ADVANCED_FACE ( 'NONE', ( #4226 ), #24298, .F. ) ;
#27603=ORIENTED_EDGE ( 'NONE', *, *, #4835, .F. ) ;
#27609=ORIENTED_EDGE ( 'NONE', *, *, #24542, .F. ) ;
#27619=DIRECTION ( 'NONE',  ( -1.000000000000000000, -0.000000000000000000, -0.000000000000000000 ) ) ;
#27621=ORIENTED_EDGE ( 'NONE', *, *, #4387, .T. ) ;
#27622=DIRECTION ( 'NONE',  ( -1.000000000000000000, -0.000000000000000000, -0.000000000000000000 ) ) ;
#27633=DIRECTION ( 'NONE',  ( 0.000000000000000000, -0.5735764363510502672, 0.8191520442889888010 ) ) ;
#27634=CARTESIAN_POINT ( 'NONE',  ( -6.537550801365592967, 1.828967928396027398, -3.368539882008727115 ) ) ;
#27636=CARTESIAN_POINT ( 'NONE',  ( 5.887530180601100227, 7.449245365665851715, -3.870837198608021001 ) ) ;
#27650=ORIENTED_EDGE ( 'NONE', *, *, #21919, .F. ) ;
#27651=CARTESIAN_POINT ( 'NONE',  ( 7.249760686538667009, 0.8180878109962995692, -8.711672189281419065 ) ) ;
#27665=CARTESIAN_POINT ( 'NONE',  ( -1.850050802731187716, 1.887961173149511618, 2.331437884370912705 ) ) ;
#27667=CARTESIAN_POINT ( 'NONE',  ( -7.937550801365594211, 3.368539882008727115, 1.828967928396026954 ) ) ;
#27669=CARTESIAN_POINT ( 'NONE',  ( -3.762942409646513386, 4.884725290497410777E-15, -2.999999999999999556 ) ) ;
#27678=EDGE_LOOP ( 'NONE', ( #18103, #23141, #9928, #21169 ) ) ;
#27688=EDGE_CURVE ( 'NONE', #11907, #16750, #25593, .T. ) ;
#27694=CARTESIAN_POINT ( 'NONE',  ( -8.000050800000055418, 1.847639235587218209, 2.786559910703183984 ) ) ;
#27695=DIRECTION ( 'NONE',  ( 0.000000000000000000, -0.8191520442889844711, -0.5735764363510564845 ) ) ;
#27699=CARTESIAN_POINT ( 'NONE',  ( -5.212550801365593678, -1.828967928396026510, 3.368539882008728004 ) ) ;
#27701=CARTESIAN_POINT ( 'NONE',  ( -8.154531657079159501, 0.9198621039125853827, 3.105402419394639235 ) ) ;
#27708=ORIENTED_EDGE ( 'NONE', *, *, #31411, .F. ) ;
#27709=CARTESIAN_POINT ( 'NONE',  ( 6.880159329304570193, -5.066480354148979792, 7.110803091624043226 ) ) ;
#27715=LINE ( 'NONE', #15194, #19320 ) ;
#27716=EDGE_CURVE ( 'NONE', #16327, #9445, #11837, .T. ) ;
#27718=CARTESIAN_POINT ( 'NONE',  ( -8.000050800000000351, -2.963268750767338755, -0.5301859913251431022 ) ) ;
#27719=DIRECTION ( 'NONE',  ( 0.000000000000000000, -0.7431448254773863615, -0.6691306063588671194 ) ) ;
#27723=ORIENTED_EDGE ( 'NONE', *, *, #6697, .T. ) ;
#27724=CARTESIAN_POINT ( 'NONE',  ( -3.587550801365593678, -3.521866450007987037, -0.3701630799359323931 ) ) ;
#27727=CARTESIAN_POINT ( 'NONE',  ( 5.887530252753765403, -6.663910820542616520, 5.105578361685893185 ) ) ;
#27728=FACE_OUTER_BOUND ( 'NONE', #3267, .T. ) ;
#27732=VERTEX_POINT ( 'NONE', #29739 ) ;
#27733=EDGE_CURVE ( 'NONE', #10967, #26019, #22212, .T. ) ;
#27734=CIRCLE ( 'NONE', #10648, 8.750000000000000000 ) ;
#27735=( BOUNDED_CURVE ( )  B_SPLINE_CURVE ( 2, ( #6783, #4468, #14795, #27170, #4620, #7431, #21999, #17630, #12284, #24662, #30036 ),
 .UNSPECIFIED., .F., .F. ) 
 B_SPLINE_CURVE_WITH_KNOTS ( ( 3, 2, 2, 2, 2, 3 ),
 ( 0.8728822619934377691, 0.8750000000000000000, 0.8906250000000000000, 0.9062500000000000000, 0.9218750000000000000, 0.9353822619934377691 ),
 .UNSPECIFIED. ) 
 CURVE ( )  GEOMETRIC_REPRESENTATION_ITEM ( )  RATIONAL_B_SPLINE_CURVE ( ( 0.9821626249036861100, 0.9896829947469995004, 1.000000000000000000, 0.9238795325112867385, 1.000000000000000000, 0.9238795325112867385, 1.000000000000000000, 0.9238795325112867385, 1.000000000000000000, 0.9341965377642872381, 0.9821626249036861100 ) ) 
 REPRESENTATION_ITEM ( '' )  );
#27744=CARTESIAN_POINT ( 'NONE',  ( 7.249760686538667009, -1.391664247347174754, -7.892520144992448472 ) ) ;
#27747=ADVANCED_FACE ( 'NONE', ( #12018 ), #9483, .T. ) ;
#27748=AXIS2_PLACEMENT_3D ( 'NONE', #9292, #4275, #27347 ) ;
#27749=AXIS2_PLACEMENT_3D ( 'NONE', #8782, #10966, #1087 ) ;
#27758=ORIENTED_EDGE ( 'NONE', *, *, #6126, .F. ) ;
#27761=CARTESIAN_POINT ( 'NONE',  ( 3.499999999999999556, 1.418488851014406693, 6.085876303339381899 ) ) ;
#27772=ADVANCED_FACE ( 'NONE', ( #21862 ), #19382, .T. ) ;
#27773=LINE ( 'NONE', #22125, #16198 ) ;
#27774=AXIS2_PLACEMENT_3D ( 'NONE', #16488, #8823, #6648 ) ;
#27776=CARTESIAN_POINT ( 'NONE',  ( 6.038145077921538650, -2.472816103755196782, -8.106170535363476759 ) ) ;
#27780=DIRECTION ( 'NONE',  ( 1.000000000000000000, -0.000000000000000000, -0.000000000000000000 ) ) ;
#27782=AXIS2_PLACEMENT_3D ( 'NONE', #8452, #18497, #31373 ) ;
#27784=CARTESIAN_POINT ( 'NONE',  ( 6.357667975083868939, -4.790963222208053374, 7.150591204917380317 ) ) ;
#27786=CARTESIAN_POINT ( 'NONE',  ( -7.437550801365595099, -1.088641768524163611, -3.675193018007245627 ) ) ;
#27787=ORIENTED_EDGE ( 'NONE', *, *, #2633, .T. ) ;
#27791=AXIS2_PLACEMENT_3D ( 'NONE', #29417, #27073, #26924 ) ;
#27797=ORIENTED_EDGE ( 'NONE', *, *, #19997, .T. ) ;
#27801=VERTEX_POINT ( 'NONE', #13003 ) ;
#27802=CARTESIAN_POINT ( 'NONE',  ( 7.249760686538667009, 2.741043480755029016, -7.530955069117485579 ) ) ;
#27804=ORIENTED_EDGE ( 'NONE', *, *, #31043, .T. ) ;
#27817=CARTESIAN_POINT ( 'NONE',  ( 4.749760686538667009, 2.741043480754926875, 7.530955069117522882 ) ) ;
#27821=AXIS2_PLACEMENT_3D ( 'NONE', #25054, #29766, #2172 ) ;
#27825=CARTESIAN_POINT ( 'NONE',  ( 5.885541615502094537, 8.322568858718552676, 1.090540896198838761 ) ) ;
#27828=CARTESIAN_POINT ( 'NONE',  ( -1.800050802731187227, 0.9222479816126443186, 3.113457007523260156 ) ) ;
#27830=CARTESIAN_POINT ( 'NONE',  ( -5.337550801365593678, -1.828967928396026510, 3.368539882008728004 ) ) ;
#27831=ADVANCED_FACE ( 'NONE', ( #33065 ), #5309, .F. ) ;
#27834=CARTESIAN_POINT ( 'NONE',  ( -4.150050802731187538, -0.3135853898029607456, 2.983565686104819648 ) ) ;
#27836=DIRECTION ( 'NONE',  ( -1.000000000000000000, 0.000000000000000000, 0.000000000000000000 ) ) ;
#27841=AXIS2_PLACEMENT_3D ( 'NONE', #22282, #19768, #29974 ) ;
#27844=VERTEX_POINT ( 'NONE', #4810 ) ;
#27846=EDGE_CURVE ( 'NONE', #30729, #15643, #11389, .T. ) ;
#27851=CARTESIAN_POINT ( 'NONE',  ( -2.361419555135669590, 0.8502021591709224557, 3.209614657730603060 ) ) ;
#27852=ORIENTED_EDGE ( 'NONE', *, *, #10400, .F. ) ;
#27862=ORIENTED_EDGE ( 'NONE', *, *, #1379, .F. ) ;
#27869=DIRECTION ( 'NONE',  ( 0.000000000000000000, 0.8660254037844361541, 0.5000000000000041078 ) ) ;
#27874=AXIS2_PLACEMENT_3D ( 'NONE', #23879, #21373, #8671 ) ;
#27875=CARTESIAN_POINT ( 'NONE',  ( -6.962550801365593678, 2.228590825266444142, 2.752080473201636845 ) ) ;
#27879=CARTESIAN_POINT ( 'NONE',  ( -8.304531657079156304, 2.975847129947406522, 0.3127741368606808403 ) ) ;
#27889=LINE ( 'NONE', #22102, #20816 ) ;
#27894=EDGE_CURVE ( 'NONE', #29891, #24488, #16202, .T. ) ;
#27899=DIRECTION ( 'NONE',  ( 0.000000000000000000, 0.000000000000000000, -1.000000000000000000 ) ) ;
#27902=AXIS2_PLACEMENT_3D ( 'NONE', #27198, #27385, #8831 ) ;
#27911=CARTESIAN_POINT ( 'NONE',  ( -7.312550801365594211, -1.088641768524163389, -3.675193018007246071 ) ) ;
#27925=VECTOR ( 'NONE', #11815, 1000.000000000000000 ) ;
#27932=ORIENTED_EDGE ( 'NONE', *, *, #2657, .T. ) ;
#27933=CARTESIAN_POINT ( 'NONE',  ( 0.000000000000000000, -7.851777359434021442, 3.255701506262407285 ) ) ;
#27935=EDGE_CURVE ( 'NONE', #22300, #16325, #16322, .T. ) ;
#27939=ORIENTED_EDGE ( 'NONE', *, *, #29112, .F. ) ;
#27948=CARTESIAN_POINT ( 'NONE',  ( -6.562550801365594211, -2.228590825266444586, -2.752080473201636401 ) ) ;
#27949=LINE ( 'NONE', #27761, #18834 ) ;
#27951=DIRECTION ( 'NONE',  ( -1.000000000000000000, -0.000000000000000000, 0.000000000000000000 ) ) ;
#27953=VECTOR ( 'NONE', #19310, 1000.000000000000000 ) ;
#27954=AXIS2_PLACEMENT_3D ( 'NONE', #20066, #13022, #10506 ) ;
#27962=DIRECTION ( 'NONE',  ( -1.000000000000000000, 0.000000000000000000, 0.000000000000000000 ) ) ;
#27964=AXIS2_PLACEMENT_3D ( 'NONE', #30959, #23578, #6197 ) ;
#27968=CARTESIAN_POINT ( 'NONE',  ( 4.749760686538667009, -2.789499415801756586E-14, 8.014274990069656823 ) ) ;
#27969=CARTESIAN_POINT ( 'NONE',  ( -6.112942406915326643, -3.366872799099910998E-15, -3.000000000000000000 ) ) ;
#27971=VERTEX_POINT ( 'NONE', #18513 ) ;
#27972=DIRECTION ( 'NONE',  ( 0.000000000000000000, 0.000000000000000000, 1.000000000000000000 ) ) ;
#27975=CARTESIAN_POINT ( 'NONE',  ( -7.937550801365593323, 3.368539882008727115, 1.828967928396027176 ) ) ;
#27979=CARTESIAN_POINT ( 'NONE',  ( 0.000000000000000000, -6.200809695932780308, 0.7745709230444962623 ) ) ;
#27981=EDGE_CURVE ( 'NONE', #13793, #15643, #21516, .T. ) ;
#27982=CARTESIAN_POINT ( 'NONE',  ( 6.356381451270080696, -8.587653982362812854, 0.5733789922931548100 ) ) ;
#27983=CIRCLE ( 'NONE', #3956, 2.999999999999999112 ) ;
#27988=CARTESIAN_POINT ( 'NONE',  ( 4.749760686538667009, -4.007137495034764463, -6.940565734314639634 ) ) ;
#27991=DIRECTION ( 'NONE',  ( 1.000000000000000000, -0.000000000000000000, -0.000000000000000000 ) ) ;
#27992=EDGE_LOOP ( 'NONE', ( #11510, #29308, #7873, #22531 ) ) ;
#28000=EDGE_LOOP ( 'NONE', ( #3824, #22499, #8179, #13997 ) ) ;
#28004=DIRECTION ( 'NONE',  ( 0.000000000000000000, 0.000000000000000000, 1.000000000000000000 ) ) ;
#28008=CARTESIAN_POINT ( 'NONE',  ( 3.500000000000000000, 0.000000000000000000, 0.000000000000000000 ) ) ;
#28016=DIRECTION ( 'NONE',  ( 1.000000000000000000, -0.000000000000000000, 0.000000000000000000 ) ) ;
#28020=CARTESIAN_POINT ( 'NONE',  ( -4.187550801365593323, 0.3701630799359330593, -3.521866450007987037 ) ) ;
#28021=ADVANCED_FACE ( 'NONE', ( #21034 ), #28706, .F. ) ;
#28022=CARTESIAN_POINT ( 'NONE',  ( 3.499999999999999556, 4.058600654062948898, -7.468451026206158083 ) ) ;
#28025=CARTESIAN_POINT ( 'NONE',  ( -6.912942406915326465, 7.727249047114547632E-16, -2.999999999999999556 ) ) ;
#28027=ORIENTED_EDGE ( 'NONE', *, *, #30553, .T. ) ;
#28028=DIRECTION ( 'NONE',  ( -1.000000000000000000, -0.000000000000000000, -0.000000000000000000 ) ) ;
#28035=CARTESIAN_POINT ( 'NONE',  ( 3.499999999999999556, -7.851777359433977921, -3.255701506262513423 ) ) ;
#28039=DIRECTION ( 'NONE',  ( 0.000000000000000000, 0.000000000000000000, 1.000000000000000000 ) ) ;
#28045=CARTESIAN_POINT ( 'NONE',  ( 6.524595623740805372, -6.215987993068485373, 6.028129343649593963 ) ) ;
#28046=DIRECTION ( 'NONE',  ( -1.000000000000000000, -0.000000000000000000, 0.000000000000000000 ) ) ;
#28047=DIRECTION ( 'NONE',  ( 0.000000000000000000, 0.2588190451025219607, -0.9659258262890679791 ) ) ;
#28049=CARTESIAN_POINT ( 'NONE',  ( -8.000050800000003903, -1.933527166425570432, 2.356997308372758226 ) ) ;
#28050=CARTESIAN_POINT ( 'NONE',  ( -7.200050802731187360, -3.113457007523259268, 0.9222479816126455399 ) ) ;
#28054=CARTESIAN_POINT ( 'NONE',  ( -7.912550801365592967, 3.675193018007247403, -1.088641768524161391 ) ) ;
#28055=ORIENTED_EDGE ( 'NONE', *, *, #31689, .F. ) ;
#28057=CARTESIAN_POINT ( 'NONE',  ( -3.304531657079157192, -0.3127741368606806738, 2.975847129947406522 ) ) ;
#28071=CARTESIAN_POINT ( 'NONE',  ( 5.377543748152550762, 7.530955069117551304, -2.741043480754851380 ) ) ;
#28073=CARTESIAN_POINT ( 'NONE',  ( -8.000050800000002127, -1.705663490921306646, -2.472570538722632882 ) ) ;
#28074=CARTESIAN_POINT ( 'NONE',  ( 3.499999999999999556, -6.106419733535023653, 3.518755179752782958 ) ) ;
#28078=ORIENTED_EDGE ( 'NONE', *, *, #12990, .F. ) ;
#28079=CARTESIAN_POINT ( 'NONE',  ( -5.762550801365593500, -2.228590825266444586, -2.752080473201636401 ) ) ;
#28081=CARTESIAN_POINT ( 'NONE',  ( 6.357668022120090079, -6.947679035623489874, 5.080751859797330461 ) ) ;
#28085=ORIENTED_EDGE ( 'NONE', *, *, #9768, .F. ) ;
#28086=CARTESIAN_POINT ( 'NONE',  ( 5.377543748152548986, -4.007137495034764463, -6.940565734314639634 ) ) ;
#28093=DIRECTION ( 'NONE',  ( -0.000000000000000000, 0.9659258262890678681, 0.2588190451025219052 ) ) ;
#28097=ORIENTED_EDGE ( 'NONE', *, *, #24276, .F. ) ;
#28101=CARTESIAN_POINT ( 'NONE',  ( -6.962942409646511344, 7.727249047114547632E-16, -2.999999999999999556 ) ) ;
#28106=ORIENTED_EDGE ( 'NONE', *, *, #10529, .T. ) ;
#28108=CARTESIAN_POINT ( 'NONE',  ( -7.612550801365594033, -1.828967928396026732, 3.368539882008728004 ) ) ;
#28109=CARTESIAN_POINT ( 'NONE',  ( 6.038145077921539539, -8.106170535363467877, 2.472816103755222095 ) ) ;
#28110=B_SPLINE_CURVE_WITH_KNOTS ( 'NONE', 3,
 ( #7458, #24867, #4986, #1825, #17498, #7307, #22203, #9473, #19688, #14669 ),
 .UNSPECIFIED., .F., .F.,
 ( 4, 2, 2, 2, 4 ),
 ( 3.512955446118278440E-07, 0.0005479535487287108021, 0.001095555801912809820, 0.001643158055096908838, 0.002190760308281007856 ),
 .UNSPECIFIED. ) ;
#28111=CARTESIAN_POINT ( 'NONE',  ( 4.749760686538667009, -5.151476664237518044, 6.139290821770238438 ) ) ;
#28113=EDGE_LOOP ( 'NONE', ( #23927, #27708, #6408 ) ) ;
#28114=FACE_OUTER_BOUND ( 'NONE', #7234, .T. ) ;
#28118=DIRECTION ( 'NONE',  ( -1.000000000000000000, 0.000000000000000000, 0.000000000000000000 ) ) ;
#28122=ADVANCED_FACE ( 'NONE', ( #22174 ), #22324, .F. ) ;
#28125=DIRECTION ( 'NONE',  ( -1.000000000000000000, -0.000000000000000000, -0.000000000000000000 ) ) ;
#28131=CARTESIAN_POINT ( 'NONE',  ( -4.937550801365593323, 1.828967928396027398, -3.368539882008727115 ) ) ;
#28132=ORIENTED_EDGE ( 'NONE', *, *, #17651, .F. ) ;
#28133=CARTESIAN_POINT ( 'NONE',  ( -10.00000000000000000, 0.000000000000000000, 0.000000000000000000 ) ) ;
#28134=CARTESIAN_POINT ( 'NONE',  ( 7.249760686538667009, 7.906491560603716273, -3.748318449932209973 ) ) ;
#28154=CARTESIAN_POINT ( 'NONE',  ( 7.249760686538667009, 0.8180878109961843281, 8.711672189281429723 ) ) ;
#28167=CARTESIAN_POINT ( 'NONE',  ( -2.100050802731186828, 1.549418761218566143, -2.853674364686379583 ) ) ;
#28169=CARTESIAN_POINT ( 'NONE',  ( -6.737550801365594033, -3.368539882008727115, -1.828967928396028064 ) ) ;
#28176=VERTEX_POINT ( 'NONE', #12956 ) ;
#28181=ORIENTED_EDGE ( 'NONE', *, *, #3149, .T. ) ;
#28188=CYLINDRICAL_SURFACE ( 'NONE', #2674, 2.999999999999999112 ) ;
#28194=CARTESIAN_POINT ( 'NONE',  ( -4.207304909706596874, 1.062355717592091686, 3.000000000000001332 ) ) ;
#28196=PLANE ( 'NONE',  #15177 ) ;
#28197=ADVANCED_FACE ( 'NONE', ( #98 ), #2278, .T. ) ;
#28204=CARTESIAN_POINT ( 'NONE',  ( -7.562550801365593323, -2.752080473201636845, 2.228590825266444586 ) ) ;
#28206=CARTESIAN_POINT ( 'NONE',  ( -4.154531657079156837, 0.9198621039125853827, 3.105402419394639235 ) ) ;
#28211=DIRECTION ( 'NONE',  ( 1.000000000000000000, 0.000000000000000000, 0.000000000000000000 ) ) ;
#28229=CARTESIAN_POINT ( 'NONE',  ( -4.962550801365593678, -2.228590825266444586, -2.752080473201636401 ) ) ;
#28233=EDGE_LOOP ( 'NONE', ( #18585, #15606, #29824 ) ) ;
#28235=B_SPLINE_CURVE_WITH_KNOTS ( 'NONE', 3,
 ( #306, #14814, #10123, #20690, #12645, #25012, #28045, #12792, #25685, #32905 ),
 .UNSPECIFIED., .F., .F.,
 ( 4, 2, 2, 2, 4 ),
 ( 2.493548413911061648E-07, 0.0005478513795029421162, 0.001095453404164493244, 0.001643055428826044372, 0.002190657453487595066 ),
 .UNSPECIFIED. ) ;
#28248=ORIENTED_EDGE ( 'NONE', *, *, #20079, .T. ) ;
#28250=ORIENTED_EDGE ( 'NONE', *, *, #27321, .T. ) ;
#28257=CARTESIAN_POINT ( 'NONE',  ( -7.662550801365593856, -0.3701630799359326152, 3.521866450007987037 ) ) ;
#28261=VECTOR ( 'NONE', #30551, 1000.000000000000000 ) ;
#28276=CARTESIAN_POINT ( 'NONE',  ( 6.524595551582241804, 7.168326838405008061, -4.857153507487872446 ) ) ;
#28281=CARTESIAN_POINT ( 'NONE',  ( 3.499999999999999556, 6.226349476952025341, -0.5315761383463578627 ) ) ;
#28282=ORIENTED_EDGE ( 'NONE', *, *, #15669, .T. ) ;
#28285=CARTESIAN_POINT ( 'NONE',  ( 7.249760686538667009, -8.437262856154147173, -2.318425219014316419 ) ) ;
#28289=ORIENTED_EDGE ( 'NONE', *, *, #27935, .F. ) ;
#28292=ORIENTED_EDGE ( 'NONE', *, *, #29748, .F. ) ;
#28302=FACE_OUTER_BOUND ( 'NONE', #6332, .T. ) ;
#28319=CARTESIAN_POINT ( 'NONE',  ( 6.524595126109738352, -8.613374939462820734, -0.8869162863045405576 ) ) ;
#28320=CARTESIAN_POINT ( 'NONE',  ( 3.499999999999999556, 4.137773741518454784, -5.705158055754753654 ) ) ;
#28321=ORIENTED_EDGE ( 'NONE', *, *, #30206, .T. ) ;
#28322=CARTESIAN_POINT ( 'NONE',  ( -7.187550801365593323, 3.521866450007987037, 0.3701630799359328372 ) ) ;
#28323=AXIS2_PLACEMENT_3D ( 'NONE', #17029, #8863, #22389 ) ;
#28331=AXIS2_PLACEMENT_3D ( 'NONE', #8300, #12788, #28039 ) ;
#28332=CIRCLE ( 'NONE', #12310, 2.999999999999999112 ) ;
#28334=ORIENTED_EDGE ( 'NONE', *, *, #969, .T. ) ;
#28348=CIRCLE ( 'NONE', #9648, 3.000000000000000444 ) ;
#28349=ADVANCED_FACE ( 'NONE', ( #11099 ), #21296, .T. ) ;
#28352=AXIS2_PLACEMENT_3D ( 'NONE', #1820, #7155, #4491 ) ;
#28358=DIRECTION ( 'NONE',  ( 0.000000000000000000, 0.000000000000000000, 1.000000000000000000 ) ) ;
#28359=EDGE_CURVE ( 'NONE', #10070, #18803, #1487, .T. ) ;
#28367=CARTESIAN_POINT ( 'NONE',  ( 7.249760686538667009, -7.135485519861965109, -5.064320921489893657 ) ) ;
#28368=ORIENTED_EDGE ( 'NONE', *, *, #3036, .T. ) ;
#28369=CARTESIAN_POINT ( 'NONE',  ( -7.462550801365593678, -3.521866450007987037, -0.3701630799359323931 ) ) ;
#28372=CARTESIAN_POINT ( 'NONE',  ( -2.704531657079157103, 2.975847129947406522, 0.3127741368606808403 ) ) ;
#28375=CARTESIAN_POINT ( 'NONE',  ( 3.499999999999999556, -5.349675154362342866, 3.229702268444914370 ) ) ;
#28393=CARTESIAN_POINT ( 'NONE',  ( 5.612718825656740407, 6.420171604529186560, 5.126902779943806721 ) ) ;
#28402=CARTESIAN_POINT ( 'NONE',  ( -6.512550801365594388, -1.088641768524163389, -3.675193018007246071 ) ) ;
#28407=ORIENTED_EDGE ( 'NONE', *, *, #10983, .T. ) ;
#28412=CIRCLE ( 'NONE', #25205, 8.750000000000000000 ) ;
#28422=VERTEX_POINT ( 'NONE', #32178 ) ;
#28424=EDGE_CURVE ( 'NONE', #442, #24619, #27983, .T. ) ;
#28425=AXIS2_PLACEMENT_3D ( 'NONE', #28549, #2812, #23502 ) ;
#28427=AXIS2_PLACEMENT_3D ( 'NONE', #4767, #22170, #12458 ) ;
#28428=EDGE_CURVE ( 'NONE', #16327, #19712, #6267, .T. ) ;
#28433=DIRECTION ( 'NONE',  ( 1.000000000000000000, -0.000000000000000000, -0.000000000000000000 ) ) ;
#28434=CIRCLE ( 'NONE', #4326, 2.999999999999999112 ) ;
#28441=CIRCLE ( 'NONE', #2833, 8.500000000000000000 ) ;
#28443=CARTESIAN_POINT ( 'NONE',  ( -7.762550801365593500, 2.228590825266444142, 2.752080473201636845 ) ) ;
#28459=VECTOR ( 'NONE', #21354, 1000.000000000000000 ) ;
#28464=CIRCLE ( 'NONE', #20449, 3.000000000000000000 ) ;
#28467=CARTESIAN_POINT ( 'NONE',  ( 6.037141869538510619, 7.104659103919411578, -4.619542287584830653 ) ) ;
#28472=ORIENTED_EDGE ( 'NONE', *, *, #3865, .F. ) ;
#28475=ADVANCED_FACE ( 'NONE', ( #32502, #9561 ), #29986, .F. ) ;
#28481=AXIS2_PLACEMENT_3D ( 'NONE', #1093, #1280, #11461 ) ;
#28486=CARTESIAN_POINT ( 'NONE',  ( 3.499999999999999556, 4.438567988583082879, 7.249076783337693008 ) ) ;
#28487=ORIENTED_EDGE ( 'NONE', *, *, #29112, .T. ) ;
#28488=VERTEX_POINT ( 'NONE', #31839 ) ;
#28493=DIRECTION ( 'NONE',  ( 1.000000000000000000, -0.000000000000000000, -0.000000000000000000 ) ) ;
#28511=CARTESIAN_POINT ( 'NONE',  ( 7.249760686538667009, 3.647351267791570262, 7.953573330858228374 ) ) ;
#28517=ORIENTED_EDGE ( 'NONE', *, *, #25497, .F. ) ;
#28518=AXIS2_PLACEMENT_3D ( 'NONE', #1789, #20162, #7429 ) ;
#28524=FACE_OUTER_BOUND ( 'NONE', #8335, .T. ) ;
#28525=( NAMED_UNIT ( * ) SI_UNIT ( $, .STERADIAN. ) SOLID_ANGLE_UNIT ( ) );
#28526=ORIENTED_EDGE ( 'NONE', *, *, #17101, .F. ) ;
#28530=ORIENTED_EDGE ( 'NONE', *, *, #14567, .F. ) ;
#28542=ORIENTED_EDGE ( 'NONE', *, *, #21231, .T. ) ;
#28544=DIRECTION ( 'NONE',  ( -1.000000000000000000, 0.000000000000000000, -0.000000000000000000 ) ) ;
#28549=CARTESIAN_POINT ( 'NONE',  ( 4.749760686538667009, 2.741043480755029016, -7.530955069117485579 ) ) ;
#28553=CARTESIAN_POINT ( 'NONE',  ( -7.700050802731188249, 1.549418761218566143, -2.853674364686379583 ) ) ;
#28554=ORIENTED_EDGE ( 'NONE', *, *, #11475, .T. ) ;
#28555=CARTESIAN_POINT ( 'NONE',  ( -4.054531657079157192, -1.545410377633946286, 2.846291840500174697 ) ) ;
#28557=EDGE_CURVE ( 'NONE', #28881, #11175, #20627, .T. ) ;
#28559=DIRECTION ( 'NONE',  ( -1.000000000000000000, 0.000000000000000000, 0.000000000000000000 ) ) ;
#28562=DIRECTION ( 'NONE',  ( -1.000000000000000000, 0.000000000000000000, 0.000000000000000000 ) ) ;
#28570=DIRECTION ( 'NONE',  ( -1.000000000000000000, 0.000000000000000000, -0.000000000000000000 ) ) ;
#28572=EDGE_CURVE ( 'NONE', #24916, #21064, #763, .T. ) ;
#28578=CARTESIAN_POINT ( 'NONE',  ( -5.512550801365595277, 3.675193018007247403, -1.088641768524161391 ) ) ;
#28580=DIRECTION ( 'NONE',  ( -1.000000000000000000, -0.000000000000000000, -0.000000000000000000 ) ) ;
#28587=EDGE_CURVE ( 'NONE', #24201, #1536, #19014, .T. ) ;
#28588=EDGE_CURVE ( 'NONE', #22005, #6622, #12241, .T. ) ;
#28598=CARTESIAN_POINT ( 'NONE',  ( 4.749760686538667009, -4.007137495034861274, 6.940565734314584567 ) ) ;
#28605=ORIENTED_EDGE ( 'NONE', *, *, #4060, .F. ) ;
#28608=CARTESIAN_POINT ( 'NONE',  ( -4.512550801365592612, 1.088641768524161613, 3.675193018007246959 ) ) ;
#28617=LINE ( 'NONE', #25781, #10138 ) ;
#28621=DIRECTION ( 'NONE',  ( 0.000000000000000000, 0.5735764363510594821, -0.8191520442889824727 ) ) ;
#28624=EDGE_CURVE ( 'NONE', #9705, #5581, #10894, .T. ) ;
#28625=ADVANCED_FACE ( 'NONE', ( #10241, #14908 ), #32666, .F. ) ;
#28634=LINE ( 'NONE', #22791, #22088 ) ;
#28638=ADVANCED_FACE ( 'NONE', ( #7570 ), #12420, .T. ) ;
#28647=CARTESIAN_POINT ( 'NONE',  ( 7.249760686538667009, 0.000000000000000000, 0.000000000000000000 ) ) ;
#28649=ORIENTED_EDGE ( 'NONE', *, *, #20856, .F. ) ;
#28654=CARTESIAN_POINT ( 'NONE',  ( -2.492109178653469037, -0.3150232093026757996, 2.997245624844496081 ) ) ;
#28660=CARTESIAN_POINT ( 'NONE',  ( -3.200050800000000528, -2.331437884370912705, 1.887961173149512062 ) ) ;
#28663=CARTESIAN_POINT ( 'NONE',  ( 6.883866621640341243, -6.123537914202284327, 6.224335161394995986 ) ) ;
#28665=DIRECTION ( 'NONE',  ( 0.000000000000000000, 0.2588190451025100813, 0.9659258262890711988 ) ) ;
#28666=EDGE_LOOP ( 'NONE', ( #1791, #26694, #2858, #3669 ) ) ;
#28673=EDGE_CURVE ( 'NONE', #30996, #6099, #24545, .T. ) ;
#28674=EDGE_LOOP ( 'NONE', ( #22452, #28743, #8774, #22801 ) ) ;
#28682=CARTESIAN_POINT ( 'NONE',  ( -7.550050800000000173, 3.113457007523260156, -0.9222479816126439855 ) ) ;
#28690=EDGE_CURVE ( 'NONE', #19221, #7973, #26163, .T. ) ;
#28703=CARTESIAN_POINT ( 'NONE',  ( -3.562550801365592879, -2.752080473201636845, 2.228590825266444586 ) ) ;
#28705=CARTESIAN_POINT ( 'NONE',  ( -2.754531657079157814, 3.105402419394639235, -0.9198621039125850496 ) ) ;
#28706=PLANE ( 'NONE',  #14580 ) ;
#28719=CARTESIAN_POINT ( 'NONE',  ( 6.037141812302424526, -8.256172215043587670, 1.911013226338381221 ) ) ;
#28724=CARTESIAN_POINT ( 'NONE',  ( -2.512550801365593056, -1.088641768524163389, -3.675193018007246071 ) ) ;
#28726=DIRECTION ( 'NONE',  ( -1.000000000000000000, -0.000000000000000000, 0.000000000000000000 ) ) ;
#28729=CARTESIAN_POINT ( 'NONE',  ( -2.249956573341760357, 1.323625320507108460, 3.284597389080124774 ) ) ;
#28736=CARTESIAN_POINT ( 'NONE',  ( -2.937550801365593323, -1.828967928396026732, 3.368539882008728004 ) ) ;
#28740=DIRECTION ( 'NONE',  ( -1.000000000000000000, -0.000000000000000000, 0.000000000000000000 ) ) ;
#28742=B_SPLINE_CURVE_WITH_KNOTS ( 'NONE', 3,
 ( #7971, #26524, #28852, #18507, #313, #10485, #10638, #5952, #20697, #28367 ),
 .UNSPECIFIED., .F., .F.,
 ( 4, 2, 2, 2, 4 ),
 ( 2.493548413898819905E-07, 0.0005478513795029404899, 0.001095453404164491076, 0.001643055428826041770, 0.002190657453487592030 ),
 .UNSPECIFIED. ) ;
#28743=ORIENTED_EDGE ( 'NONE', *, *, #18207, .T. ) ;
#28754=CARTESIAN_POINT ( 'NONE',  ( -3.912550801365593411, 3.675193018007246959, -1.088641768524161391 ) ) ;
#28759=CARTESIAN_POINT ( 'NONE',  ( -5.987550801365593145, -3.521866450007987037, -0.3701630799359323931 ) ) ;
#28761=CARTESIAN_POINT ( 'NONE',  ( 7.249760686538667009, 2.210816291636326092, -8.466096581343458993 ) ) ;
#28777=CARTESIAN_POINT ( 'NONE',  ( 5.489343958331425632, -7.664144799260931507, -2.678936089601521520 ) ) ;
#28782=CARTESIAN_POINT ( 'NONE',  ( -4.600050799999999995, -1.887961173149512062, -2.331437884370912261 ) ) ;
#28783=ORIENTED_EDGE ( 'NONE', *, *, #31232, .T. ) ;
#28792=ORIENTED_EDGE ( 'NONE', *, *, #11006, .T. ) ;
#28801=DIRECTION ( 'NONE',  ( 0.000000000000000000, -0.9063077870366508249, -0.4226182617406976094 ) ) ;
#28804=EDGE_CURVE ( 'NONE', #1551, #16558, #25246, .T. ) ;
#28813=DIRECTION ( 'NONE',  ( -0.000000000000000000, 0.7071067811865507924, 0.7071067811865441310 ) ) ;
#28816=B_SPLINE_CURVE_WITH_KNOTS ( 'NONE', 3,
 ( #5327, #7841, #7682, #17880, #2349, #28073, #7333, #2507, #22560, #5018, #7489, #4670, #5170, #20718, #27718, #15196, #333, #2852, #2158, #20215, #12676, #18034, #33082 ),
 .UNSPECIFIED., .F., .F.,
 ( 4, 2, 2, 2, 2, 2, 2, 1, 2, 2, 2, 4 ),
 ( 0.5000000000000000000, 0.5443742905368078588, 0.5887485810736157177, 0.6109357263420195361, 0.6331228716104234655, 0.6774971621472312133, 0.6996843074156350317, 0.7218714526840389611, 0.7440585979524427795, 0.7662457432208467090, 0.8106200337576545678, 0.8549943242944623156 ),
 .UNSPECIFIED. ) ;
#28822=AXIS2_PLACEMENT_3D ( 'NONE', #20991, #22981, #10609 ) ;
#28834=CARTESIAN_POINT ( 'NONE',  ( 5.489321289187128805, 0.1038943573682652305, -8.118169347437836691 ) ) ;
#28839=CARTESIAN_POINT ( 'NONE',  ( 3.499999999999999556, 5.471841788314708133, 3.018103451449746899 ) ) ;
#28842=FACE_OUTER_BOUND ( 'NONE', #14524, .T. ) ;
#28845=CARTESIAN_POINT ( 'NONE',  ( -6.800050802731188782, 3.113457007523260156, -0.9222479816126439855 ) ) ;
#28847=AXIS2_PLACEMENT_3D ( 'NONE', #830, #1138, #6156 ) ;
#28851=CARTESIAN_POINT ( 'NONE',  ( 0.000000000000000000, 0.000000000000000000, 0.000000000000000000 ) ) ;
#28852=CARTESIAN_POINT ( 'NONE',  ( 5.612718825656735966, -6.420171604529151921, -5.126902779943848465 ) ) ;
#28855=CARTESIAN_POINT ( 'NONE',  ( -4.512550801365592612, 1.088641768524161613, 3.675193018007247403 ) ) ;
#28856=ORIENTED_EDGE ( 'NONE', *, *, #7767, .F. ) ;
#28857=CARTESIAN_POINT ( 'NONE',  ( -5.000050800000001239, 1.887961173149511618, 2.331437884370912705 ) ) ;
#28866=CARTESIAN_POINT ( 'NONE',  ( 7.249760686538667009, -2.318425219014288885, 8.437262856154156054 ) ) ;
#28873=AXIS2_PLACEMENT_3D ( 'NONE', #8030, #30296, #7725 ) ;
#28876=CARTESIAN_POINT ( 'NONE',  ( 4.749760686538667009, 8.014274990069656823, -8.669741416787380218E-17 ) ) ;
#28881=VERTEX_POINT ( 'NONE', #2523 ) ;
#28882=CARTESIAN_POINT ( 'NONE',  ( -2.462550801365593678, 0.3701630799359330593, -3.521866450007987037 ) ) ;
#28891=CIRCLE ( 'NONE', #14455, 8.750000000000000000 ) ;
#28893=DIRECTION ( 'NONE',  ( 1.000000000000000000, -0.000000000000000000, -0.000000000000000000 ) ) ;
#28894=AXIS2_PLACEMENT_3D ( 'NONE', #10020, #20229, #5343 ) ;
#28896=CARTESIAN_POINT ( 'NONE',  ( 6.524595395369781947, 2.369138865965942031, -8.328507089302155109 ) ) ;
#28899=CARTESIAN_POINT ( 'NONE',  ( -2.987550801365593145, -0.3701630799359326152, 3.521866450007987037 ) ) ;
#28900=CARTESIAN_POINT ( 'NONE',  ( 7.249760686538667009, -5.151476664237518044, 6.139290821770238438 ) ) ;
#28903=ORIENTED_EDGE ( 'NONE', *, *, #31075, .F. ) ;
#28907=VECTOR ( 'NONE', #15909, 1000.000000000000000 ) ;
#28915=EDGE_LOOP ( 'NONE', ( #8843, #13001, #2053 ) ) ;
#28917=EDGE_LOOP ( 'NONE', ( #25507, #17017, #20333 ) ) ;
#28919=CARTESIAN_POINT ( 'NONE',  ( -3.362550801365593589, -2.228590825266444586, -2.752080473201636401 ) ) ;
#28920=AXIS2_PLACEMENT_3D ( 'NONE', #4112, #14278, #1948 ) ;
#28926=CARTESIAN_POINT ( 'NONE',  ( -7.087550801365593678, 2.228590825266444142, 2.752080473201636845 ) ) ;
#28949=CARTESIAN_POINT ( 'NONE',  ( -6.937550801365595099, -1.828967928396026510, 3.368539882008728004 ) ) ;
#28951=ADVANCED_FACE ( 'NONE', ( #5344 ), #20731, .T. ) ;
#28961=VERTEX_POINT ( 'NONE', #17472 ) ;
#28966=ORIENTED_EDGE ( 'NONE', *, *, #22824, .F. ) ;
#28971=B_SPLINE_CURVE_WITH_KNOTS ( 'NONE', 3,
 ( #14849, #25049, #12837, #33093, #28081, #30925, #27727, #4836, #22888, #177 ),
 .UNSPECIFIED., .F., .F.,
 ( 4, 2, 2, 2, 4 ),
 ( 1.968338519012285402E-07, 0.0005467926089500457082, 0.001093388384048190210, 0.001639984159146334712, 0.002186579934244479214 ),
 .UNSPECIFIED. ) ;
#28973=CARTESIAN_POINT ( 'NONE',  ( 7.249760686538667009, -4.007137495034764463, -6.940565734314639634 ) ) ;
#28974=EDGE_LOOP ( 'NONE', ( #15950, #18017, #19064, #7665 ) ) ;
#28978=VECTOR ( 'NONE', #8055, 999.9999999999998863 ) ;
#28979=EDGE_CURVE ( 'NONE', #3016, #25317, #29342, .T. ) ;
#28984=CARTESIAN_POINT ( 'NONE',  ( -4.750050802731187183, -2.983565686104819648, -0.3135853898029605791 ) ) ;
#28991=DIRECTION ( 'NONE',  ( 0.000000000000000000, 0.000000000000000000, 1.000000000000000000 ) ) ;
#29000=CIRCLE ( 'NONE', #26338, 6.249000000000000554 ) ;
#29004=ORIENTED_EDGE ( 'NONE', *, *, #1446, .F. ) ;
#29008=AXIS2_PLACEMENT_3D ( 'NONE', #11517, #1491, #18892 ) ;
#29012=CARTESIAN_POINT ( 'NONE',  ( 4.749760686538667009, -5.151476664237435443, -6.139290821770307716 ) ) ;
#29013=VERTEX_POINT ( 'NONE', #20164 ) ;
#29022=CARTESIAN_POINT ( 'NONE',  ( -4.912942406915327354, -5.022711880624455567E-15, 2.999999999999999556 ) ) ;
#29023=CARTESIAN_POINT ( 'NONE',  ( 1.750000000000000222, 6.745408891279541130, 5.171987904998129437 ) ) ;
#29027=( BOUNDED_CURVE ( )  B_SPLINE_CURVE ( 2, ( #22520, #15613, #30060, #2123, #12303, #9817, #6379, #31483, #8566, #16416, #26788 ),
 .UNSPECIFIED., .F., .F. ) 
 B_SPLINE_CURVE_WITH_KNOTS ( ( 3, 2, 2, 2, 2, 3 ),
 ( 0.6853822619934377691, 0.6875000000000000000, 0.7031250000000000000, 0.7187500000000000000, 0.7343750000000000000, 0.7478822619934377691 ),
 .UNSPECIFIED. ) 
 CURVE ( )  GEOMETRIC_REPRESENTATION_ITEM ( )  RATIONAL_B_SPLINE_CURVE ( ( 0.9821626249036861100, 0.9896829947469995004, 1.000000000000000000, 0.9238795325112867385, 1.000000000000000000, 0.9238795325112867385, 1.000000000000000000, 0.9238795325112867385, 1.000000000000000000, 0.9341965377642872381, 0.9821626249036861100 ) ) 
 REPRESENTATION_ITEM ( '' )  );
#29029=DIRECTION ( 'NONE',  ( -0.000000000000000000, 0.8191520442889933529, -0.5735764363510439390 ) ) ;
#29032=DIRECTION ( 'NONE',  ( 1.000000000000000000, 0.000000000000000000, 0.000000000000000000 ) ) ;
#29041=EDGE_CURVE ( 'NONE', #18803, #9165, #27735, .T. ) ;
#29044=EDGE_CURVE ( 'NONE', #5581, #30729, #4797, .T. ) ;
#29045=CARTESIAN_POINT ( 'NONE',  ( -4.712550801365592790, 3.675193018007247403, -1.088641768524161391 ) ) ;
#29047=CARTESIAN_POINT ( 'NONE',  ( -7.300050800000001061, -0.3135853898029607456, 2.983565686104819648 ) ) ;
#29053=VECTOR ( 'NONE', #27962, 1000.000000000000000 ) ;
#29061=CARTESIAN_POINT ( 'NONE',  ( 3.499999999999999556, -7.673322273190748888, 3.656518192455052052 ) ) ;
#29064=ORIENTED_EDGE ( 'NONE', *, *, #32934, .F. ) ;
#29066=DIRECTION ( 'NONE',  ( -1.000000000000000000, 0.000000000000000000, 0.000000000000000000 ) ) ;
#29071=CARTESIAN_POINT ( 'NONE',  ( -3.062550801365593323, 3.521866450007987037, 0.3701630799359328372 ) ) ;
#29073=CARTESIAN_POINT ( 'NONE',  ( 3.499999999999999556, -1.471047635026823786, -6.892461014225975013 ) ) ;
#29075=EDGE_CURVE ( 'NONE', #19878, #19600, #9049, .T. ) ;
#29078=DIRECTION ( 'NONE',  ( 0.000000000000000000, -0.9961946980917465444, 0.08715574274764703588 ) ) ;
#29082=VERTEX_POINT ( 'NONE', #22177 ) ;
#29083=CARTESIAN_POINT ( 'NONE',  ( 5.489343958331427409, 2.678936089601548165, -7.664144799260921737 ) ) ;
#29085=CARTESIAN_POINT ( 'NONE',  ( -3.537550801365593411, -3.368539882008727115, -1.828967928396027842 ) ) ;
#29089=DIRECTION ( 'NONE',  ( -1.000000000000000000, -0.000000000000000000, -0.000000000000000000 ) ) ;
#29093=CIRCLE ( 'NONE', #9319, 8.750000000000000000 ) ;
#29100=CARTESIAN_POINT ( 'NONE',  ( -2.912550801365593411, 1.088641768524161613, 3.675193018007246959 ) ) ;
#29103=CARTESIAN_POINT ( 'NONE',  ( 6.524595395369783724, 7.902859683906662269, -3.538595500939507144 ) ) ;
#29104=VERTEX_POINT ( 'NONE', #32387 ) ;
#29105=CARTESIAN_POINT ( 'NONE',  ( -7.037550801365593856, 1.088641768524161613, 3.675193018007247403 ) ) ;
#29110=DIRECTION ( 'NONE',  ( 0.000000000000000000, -0.9510565162951502005, -0.3090169943749573878 ) ) ;
#29112=EDGE_CURVE ( 'NONE', #22455, #28961, #15801, .T. ) ;
#29113=ADVANCED_FACE ( 'NONE', ( #28524 ), #7618, .T. ) ;
#29121=CARTESIAN_POINT ( 'NONE',  ( -2.287550801365593856, 2.228590825266444142, 2.752080473201636845 ) ) ;
#29126=CARTESIAN_POINT ( 'NONE',  ( 5.887530180601100227, -7.449245365665823293, 3.870837198608072072 ) ) ;
#29128=DIRECTION ( 'NONE',  ( -1.000000000000000000, 0.000000000000000000, -0.000000000000000000 ) ) ;
#29130=CARTESIAN_POINT ( 'NONE',  ( -7.900050800000000706, -2.983565686104819648, -0.3135853898029605791 ) ) ;
#29134=CARTESIAN_POINT ( 'NONE',  ( -8.000050800000002127, 3.541248556864417196, 0.01107501445590582979 ) ) ;
#29135=APPLICATION_CONTEXT ( 'configuration controlled 3d designs of mechanical parts and assemblies' ) ;
#29145=CARTESIAN_POINT ( 'NONE',  ( -4.562942409646513653, -3.366872799099910998E-15, -3.000000000000000000 ) ) ;
#29147=CARTESIAN_POINT ( 'NONE',  ( 7.249760686538667009, 0.000000000000000000, 0.000000000000000000 ) ) ;
#29148=CARTESIAN_POINT ( 'NONE',  ( 7.064423637758999952, 8.437262856155495427, 2.318425219013635630 ) ) ;
#29149=CARTESIAN_POINT ( 'NONE',  ( 0.000000000000000000, -0.1221666339524086348, 6.247805719894683918 ) ) ;
#29151=CARTESIAN_POINT ( 'NONE',  ( -6.157304906975411107, -1.062355717592097015, -2.999999999999998668 ) ) ;
#29152=CARTESIAN_POINT ( 'NONE',  ( -8.000050800000000351, 0.000000000000000000, 0.000000000000000000 ) ) ;
#29153=FACE_OUTER_BOUND ( 'NONE', #4544, .T. ) ;
#29175=CARTESIAN_POINT ( 'NONE',  ( 5.489321289187125252, -0.1038943573682082760, 8.118169347437836691 ) ) ;
#29190=CARTESIAN_POINT ( 'NONE',  ( -7.500050802731188071, 2.853674364686379583, 1.549418761218565921 ) ) ;
#29193=CARTESIAN_POINT ( 'NONE',  ( -7.800050800000000173, -1.887961173149512062, -2.331437884370912261 ) ) ;
#29195=CARTESIAN_POINT ( 'NONE',  ( -8.125050801365594211, 0.3701630799359330593, -3.521866450007987037 ) ) ;
#29196=FACE_OUTER_BOUND ( 'NONE', #5833, .T. ) ;
#29202=EDGE_LOOP ( 'NONE', ( #6489, #996 ) ) ;
#29211=EDGE_CURVE ( 'NONE', #14221, #27844, #6208, .T. ) ;
#29215=ORIENTED_EDGE ( 'NONE', *, *, #19047, .T. ) ;
#29217=B_SPLINE_CURVE_WITH_KNOTS ( 'NONE', 3,
 ( #1850, #9495, #31930, #12028, #8996, #19888, #2155, #19210, #6500, #26913 ),
 .UNSPECIFIED., .F., .F.,
 ( 4, 2, 2, 2, 4 ),
 ( 1.968338519004493228E-07, 0.0005467926395225673275, 0.001093388445193233666, 0.001639984250863899895, 0.002186580056534566125 ),
 .UNSPECIFIED. ) ;
#29222=CARTESIAN_POINT ( 'NONE',  ( 7.249760686538667009, 7.530955069117551304, -2.741043480754851380 ) ) ;
#29230=PLANE ( 'NONE',  #29503 ) ;
#29232=CARTESIAN_POINT ( 'NONE',  ( -2.019764013714869577, 0.9872008099554112626, 3.231313631359007399 ) ) ;
#29234=CARTESIAN_POINT ( 'NONE',  ( -2.687550801365593323, -2.228590825266444586, -2.752080473201636401 ) ) ;
#29250=CARTESIAN_POINT ( 'NONE',  ( -4.962550801365593678, -2.228590825266444586, -2.752080473201636401 ) ) ;
#29255=CARTESIAN_POINT ( 'NONE',  ( -5.937550801365592434, -3.368539882008727115, -1.828967928396028064 ) ) ;
#29257=CARTESIAN_POINT ( 'NONE',  ( 6.357667697713668353, 2.056386458247386528, -8.357963647880058744 ) ) ;
#29259=ORIENTED_EDGE ( 'NONE', *, *, #14033, .T. ) ;
#29260=DIRECTION ( 'NONE',  ( 0.000000000000000000, 0.08715574274765541807, -0.9961946980917457672 ) ) ;
#29267=CARTESIAN_POINT ( 'NONE',  ( 7.249760686538667009, -6.139290821770219786, -5.151476664237539360 ) ) ;
#29268=CARTESIAN_POINT ( 'NONE',  ( -2.787550801365593411, -3.521866450007987037, -0.3701630799359323931 ) ) ;
#29271=CARTESIAN_POINT ( 'NONE',  ( 0.000000000000000000, 1.418488851014487073, -6.085876303339362359 ) ) ;
#29273=CARTESIAN_POINT ( 'NONE',  ( 7.064632940817598517, -7.906491560603691404, 3.748318449932268148 ) ) ;
#29279=ORIENTED_EDGE ( 'NONE', *, *, #20687, .F. ) ;
#29281=EDGE_CURVE ( 'NONE', #24417, #901, #5457, .T. ) ;
#29301=ORIENTED_EDGE ( 'NONE', *, *, #12943, .T. ) ;
#29304=CARTESIAN_POINT ( 'NONE',  ( 4.749760686538667009, 1.391664247347228045, 7.892520144992438702 ) ) ;
#29308=ORIENTED_EDGE ( 'NONE', *, *, #25703, .F. ) ;
#29311=EDGE_LOOP ( 'NONE', ( #852, #27797, #29805, #3290 ) ) ;
#29316=CARTESIAN_POINT ( 'NONE',  ( 5.887529755120530339, -8.323904922804405970, 1.089605374054344544 ) ) ;
#29318=ORIENTED_EDGE ( 'NONE', *, *, #12541, .T. ) ;
#29320=ORIENTED_EDGE ( 'NONE', *, *, #2480, .F. ) ;
#29326=LINE ( 'NONE', #29023, #22939 ) ;
#29328=CARTESIAN_POINT ( 'NONE',  ( 6.038145268433179780, 5.096160642893651449, 6.771555838910872538 ) ) ;
#29333=LINE ( 'NONE', #6769, #17859 ) ;
#29336=DIRECTION ( 'NONE',  ( 0.000000000000000000, -0.9659258262890720870, 0.2588190451025066952 ) ) ;
#29339=CARTESIAN_POINT ( 'NONE',  ( -4.550050802731187005, 0.3135853898029611342, -2.983565686104819648 ) ) ;
#29341=CARTESIAN_POINT ( 'NONE',  ( -7.850050800000000883, -2.853674364686378695, -1.549418761218566809 ) ) ;
#29342=CIRCLE ( 'NONE', #21872, 6.248999999999999666 ) ;
#29343=EDGE_CURVE ( 'NONE', #31349, #11409, #29492, .T. ) ;
#29355=DIRECTION ( 'NONE',  ( -1.000000000000000000, 0.000000000000000000, 0.000000000000000000 ) ) ;
#29357=VERTEX_POINT ( 'NONE', #29667 ) ;
#29361=CARTESIAN_POINT ( 'NONE',  ( 3.499999999999999556, 6.226349476952025341, -0.5315761383463578627 ) ) ;
#29373=CARTESIAN_POINT ( 'NONE',  ( 3.499999999999999556, -2.834406817834963732, 8.013497238472769624 ) ) ;
#29381=PLANE ( 'NONE',  #27902 ) ;
#29387=CARTESIAN_POINT ( 'NONE',  ( 6.880159540721329847, 2.328896285337303418, -8.414807581959433236 ) ) ;
#29388=CARTESIAN_POINT ( 'NONE',  ( -1.867022907593409276, 0.3751246966288243057, 3.134367353446092963 ) ) ;
#29390=CARTESIAN_POINT ( 'NONE',  ( -4.437550801365594211, -3.675193018007245627, 1.088641768524163389 ) ) ;
#29394=FACE_OUTER_BOUND ( 'NONE', #1377, .T. ) ;
#29397=EDGE_CURVE ( 'NONE', #15831, #4708, #9750, .T. ) ;
#29406=CARTESIAN_POINT ( 'NONE',  ( 6.880159329304570193, 6.224287131858889488, -6.122988934091214475 ) ) ;
#29415=ORIENTED_EDGE ( 'NONE', *, *, #17322, .F. ) ;
#29416=CARTESIAN_POINT ( 'NONE',  ( -8.037550801365592079, 3.675193018007247403, -1.088641768524161391 ) ) ;
#29417=CARTESIAN_POINT ( 'NONE',  ( -8.000050800000000351, 0.000000000000000000, 0.000000000000000000 ) ) ;
#29419=CARTESIAN_POINT ( 'NONE',  ( 5.887529755120530339, 1.823049025159297232, -8.194579018285272909 ) ) ;
#29421=AXIS2_PLACEMENT_3D ( 'NONE', #297, #20680, #30883 ) ;
#29423=FACE_OUTER_BOUND ( 'NONE', #21213, .T. ) ;
#29424=VERTEX_POINT ( 'NONE', #12910 ) ;
#29429=( BOUNDED_CURVE ( )  B_SPLINE_CURVE ( 2, ( #21847, #29727, #6805, #32062, #4302, #6652, #19364, #1979, #9975, #28194, #20185 ),
 .UNSPECIFIED., .F., .F. ) 
 B_SPLINE_CURVE_WITH_KNOTS ( ( 3, 2, 2, 2, 2, 3 ),
 ( 0.4978822619934377136, 0.5000000000000000000, 0.5156250000000000000, 0.5312500000000000000, 0.5468750000000000000, 0.5603822619934377691 ),
 .UNSPECIFIED. ) 
 CURVE ( )  GEOMETRIC_REPRESENTATION_ITEM ( )  RATIONAL_B_SPLINE_CURVE ( ( 0.9821626249036857770, 0.9896829947469991673, 1.000000000000000000, 0.9238795325112867385, 1.000000000000000000, 0.9238795325112867385, 1.000000000000000000, 0.9238795325112867385, 1.000000000000000000, 0.9341965377642872381, 0.9821626249036861100 ) ) 
 REPRESENTATION_ITEM ( '' )  );
#29442=CARTESIAN_POINT ( 'NONE',  ( 7.249760686538667009, 6.147671362329302447, -6.226446564517854831 ) ) ;
#29445=CARTESIAN_POINT ( 'NONE',  ( -3.357304906975409953, 1.062355717592091686, 3.000000000000001332 ) ) ;
#29457=AXIS2_PLACEMENT_3D ( 'NONE', #23934, #1044, #31654 ) ;
#29471=CARTESIAN_POINT ( 'NONE',  ( -4.900050802731187538, -1.549418761218565255, 2.853674364686380471 ) ) ;
#29472=AXIS2_PLACEMENT_3D ( 'NONE', #28133, #8057, #30834 ) ;
#29492=LINE ( 'NONE', #24614, #31076 ) ;
#29494=VECTOR ( 'NONE', #23750, 1000.000000000000114 ) ;
#29496=CARTESIAN_POINT ( 'NONE',  ( 6.883866557622099869, 3.625395379390193629, -7.943335131954968986 ) ) ;
#29498=CARTESIAN_POINT ( 'NONE',  ( 6.883866482134012976, -8.691827696555163740, 0.8319830743950369367 ) ) ;
#29502=AXIS2_PLACEMENT_3D ( 'NONE', #12894, #23116, #7554 ) ;
#29503=AXIS2_PLACEMENT_3D ( 'NONE', #24519, #1645, #24026 ) ;
#29508=CARTESIAN_POINT ( 'NONE',  ( 5.377543748152548986, 6.940565734314653845, -4.007137495034738706 ) ) ;
#29518=B_SPLINE_CURVE_WITH_KNOTS ( 'NONE', 3,
 ( #102, #15141, #17823, #24993, #27521, #12625, #2457, #22328, #17473, #33033 ),
 .UNSPECIFIED., .F., .F.,
 ( 4, 2, 2, 2, 4 ),
 ( 2.493548413898819905E-07, 0.0005478513795029405983, 0.001095453404164491292, 0.001643055428826041987, 0.002190657453487592464 ),
 .UNSPECIFIED. ) ;
#29519=CARTESIAN_POINT ( 'NONE',  ( 3.499999999999999556, 6.100541242131516384, 3.528937025535512362 ) ) ;
#29531=DIRECTION ( 'NONE',  ( -1.000000000000000000, 0.000000000000000000, 0.000000000000000000 ) ) ;
#29532=CARTESIAN_POINT ( 'NONE',  ( -6.700050802731187360, 2.853674364686379583, 1.549418761218565921 ) ) ;
#29536=CARTESIAN_POINT ( 'NONE',  ( -5.750050799999999462, 0.9222479816126443186, 3.113457007523260156 ) ) ;
#29538=FACE_OUTER_BOUND ( 'NONE', #29799, .T. ) ;
#29540=CIRCLE ( 'NONE', #21002, 8.500000000000000000 ) ;
#29547=ORIENTED_EDGE ( 'NONE', *, *, #8813, .T. ) ;
#29549=CARTESIAN_POINT ( 'NONE',  ( 3.499999999999999556, -7.009698679648292519, 0.7308381473896670144 ) ) ;
#29550=CIRCLE ( 'NONE', #729, 2.999999999999999112 ) ;
#29564=ORIENTED_EDGE ( 'NONE', *, *, #32909, .T. ) ;
#29567=CARTESIAN_POINT ( 'NONE',  ( 5.612974384376776982, -3.934067627273155399, -7.213266193303299545 ) ) ;
#29575=CARTESIAN_POINT ( 'NONE',  ( -2.562942409646512321, -5.022711880624455567E-15, 2.999999999999999556 ) ) ;
#29581=EDGE_CURVE ( 'NONE', #11409, #22634, #13567, .T. ) ;
#29583=AXIS2_PLACEMENT_3D ( 'NONE', #22449, #25618, #32845 ) ;
#29586=ORIENTED_EDGE ( 'NONE', *, *, #969, .F. ) ;
#29588=VERTEX_POINT ( 'NONE', #16250 ) ;
#29593=DIRECTION ( 'NONE',  ( -1.000000000000000000, -0.000000000000000000, -0.000000000000000000 ) ) ;
#29598=CARTESIAN_POINT ( 'NONE',  ( 5.489321708267617339, 6.152096559282836274, 5.297846913781713241 ) ) ;
#29599=CARTESIAN_POINT ( 'NONE',  ( 5.885541806331896275, -7.447669719165306290, -3.871259391815531359 ) ) ;
#29605=CARTESIAN_POINT ( 'NONE',  ( -2.637550801365593500, -1.088641768524163389, -3.675193018007246071 ) ) ;
#29606=CYLINDRICAL_SURFACE ( 'NONE', #27791, 3.000000000000000444 ) ;
#29609=ORIENTED_EDGE ( 'NONE', *, *, #7944, .F. ) ;
#29614=CARTESIAN_POINT ( 'NONE',  ( 5.489321486716459475, 7.976795196726687465, 1.512021494499613761 ) ) ;
#29624=EDGE_LOOP ( 'NONE', ( #20634, #17775, #23363 ) ) ;
#29628=CARTESIAN_POINT ( 'NONE',  ( -8.000050800000018114, 1.979734913925816908, -2.936190332390367086 ) ) ;
#29629=LINE ( 'NONE', #15340, #10770 ) ;
#29633=ORIENTED_EDGE ( 'NONE', *, *, #7732, .T. ) ;
#29636=ORIENTED_EDGE ( 'NONE', *, *, #31925, .T. ) ;
#29640=CARTESIAN_POINT ( 'NONE',  ( 5.887530252753766291, 5.676096663009888132, -6.185189124321764709 ) ) ;
#29652=DIRECTION ( 'NONE',  ( 0.000000000000000000, 0.000000000000000000, 1.000000000000000000 ) ) ;
#29656=DIRECTION ( 'NONE',  ( -1.000000000000000000, 0.000000000000000000, 0.000000000000000000 ) ) ;
#29661=EDGE_LOOP ( 'NONE', ( #7183, #5210, #12220, #4722 ) ) ;
#29662=EDGE_CURVE ( 'NONE', #3311, #15684, #14060, .T. ) ;
#29666=ORIENTED_EDGE ( 'NONE', *, *, #9363, .T. ) ;
#29667=CARTESIAN_POINT ( 'NONE',  ( 0.000000000000000000, 4.561279057474472154, -4.271385531633124621 ) ) ;
#29669=EDGE_LOOP ( 'NONE', ( #16498, #24047, #18392, #6994 ) ) ;
#29673=ORIENTED_EDGE ( 'NONE', *, *, #33085, .T. ) ;
#29682=CARTESIAN_POINT ( 'NONE',  ( 1.750000000000000222, -5.848742439617879540, -6.167836887841045446 ) ) ;
#29684=CARTESIAN_POINT ( 'NONE',  ( 5.489321486716458587, 1.307389195612976618, 8.012877392144801547 ) ) ;
#29693=FACE_OUTER_BOUND ( 'NONE', #19411, .T. ) ;
#29695=CARTESIAN_POINT ( 'NONE',  ( -5.000050802731188959, 0.9222479816126443186, 3.113457007523260156 ) ) ;
#29697=CARTESIAN_POINT ( 'NONE',  ( -7.487550801365594033, -2.228590825266444586, -2.752080473201636401 ) ) ;
#29703=CARTESIAN_POINT ( 'NONE',  ( 1.750000000000000222, 7.003298780661491918, -4.817032923780496745 ) ) ;
#29708=DIRECTION ( 'NONE',  ( 0.000000000000000000, 0.5877852522924689183, 0.8090169943749503378 ) ) ;
#29712=ADVANCED_FACE ( 'NONE', ( #3885 ), #24266, .T. ) ;
#29716=FACE_OUTER_BOUND ( 'NONE', #30907, .T. ) ;
#29718=EDGE_CURVE ( 'NONE', #29588, #27801, #15188, .T. ) ;
#29727=CARTESIAN_POINT ( 'NONE',  ( -4.556376981307135310, 0.1572233378491222633, -3.000000000000000000 ) ) ;
#29730=CARTESIAN_POINT ( 'NONE',  ( 6.356381935169121533, -0.9265622495396348413, 8.556754636093206301 ) ) ;
#29731=CARTESIAN_POINT ( 'NONE',  ( 7.249760686538667009, -1.391664247347174754, -7.892520144992448472 ) ) ;
#29737=CARTESIAN_POINT ( 'NONE',  ( -7.104531657079157014, -2.975847129947406522, -0.3127741368606805072 ) ) ;
#29739=CARTESIAN_POINT ( 'NONE',  ( -6.162942409646512409, 7.727249047114547632E-16, -2.999999999999999556 ) ) ;
#29741=DIRECTION ( 'NONE',  ( 0.000000000000000000, -0.9659258262890643154, -0.2588190451025359495 ) ) ;
#29742=ORIENTED_EDGE ( 'NONE', *, *, #4956, .F. ) ;
#29745=ORIENTED_EDGE ( 'NONE', *, *, #235, .F. ) ;
#29746=MECHANICAL_CONTEXT ( 'NONE', #31920, 'mechanical' ) ;
#29748=EDGE_CURVE ( 'NONE', #18185, #8026, #29629, .T. ) ;
#29754=CARTESIAN_POINT ( 'NONE',  ( -2.144454921107342038, 1.816023192640135786, 3.086171154715485088 ) ) ;
#29759=CARTESIAN_POINT ( 'NONE',  ( -2.787550801365593411, -3.521866450007987037, -0.3701630799359323931 ) ) ;
#29760=DIRECTION ( 'NONE',  ( 0.000000000000000000, -0.7071067811865483499, -0.7071067811865466846 ) ) ;
#29766=DIRECTION ( 'NONE',  ( -1.000000000000000000, 0.000000000000000000, -0.000000000000000000 ) ) ;
#29767=DIRECTION ( 'NONE',  ( -1.000000000000000000, -0.000000000000000000, 0.000000000000000000 ) ) ;
#29773=ADVANCED_FACE ( 'NONE', ( #11709 ), #19435, .F. ) ;
#29776=CARTESIAN_POINT ( 'NONE',  ( -2.537550801365592967, 1.828967928396027176, -3.368539882008727115 ) ) ;
#29777=VERTEX_POINT ( 'NONE', #22870 ) ;
#29779=EDGE_LOOP ( 'NONE', ( #23487, #12593, #9497 ) ) ;
#29780=EDGE_CURVE ( 'NONE', #31964, #20990, #4310, .T. ) ;
#29783=EDGE_CURVE ( 'NONE', #11951, #23972, #12892, .T. ) ;
#29795=EDGE_CURVE ( 'NONE', #12441, #6329, #24865, .T. ) ;
#29799=EDGE_LOOP ( 'NONE', ( #20078, #20238, #16647 ) ) ;
#29805=ORIENTED_EDGE ( 'NONE', *, *, #10190, .T. ) ;
#29806=CARTESIAN_POINT ( 'NONE',  ( 4.749760686538667009, -7.892520144992426268, -1.391664247347309535 ) ) ;
#29807=EDGE_CURVE ( 'NONE', #26246, #13763, #27215, .T. ) ;
#29811=FACE_OUTER_BOUND ( 'NONE', #6182, .T. ) ;
#29813=ORIENTED_EDGE ( 'NONE', *, *, #29854, .T. ) ;
#29817=ORIENTED_EDGE ( 'NONE', *, *, #16834, .T. ) ;
#29824=ORIENTED_EDGE ( 'NONE', *, *, #17433, .F. ) ;
#29835=DIRECTION ( 'NONE',  ( 1.000000000000000000, -0.000000000000000000, -0.000000000000000000 ) ) ;
#29838=DIRECTION ( 'NONE',  ( -1.000000000000000000, -0.000000000000000000, -0.000000000000000000 ) ) ;
#29848=DIRECTION ( 'NONE',  ( 0.000000000000000000, -0.2588190451025066396, -0.9659258262890719759 ) ) ;
#29849=LINE ( 'NONE', #2449, #31628 ) ;
#29850=CARTESIAN_POINT ( 'NONE',  ( -5.900050802731187538, 2.853674364686379583, 1.549418761218565921 ) ) ;
#29851=VERTEX_POINT ( 'NONE', #18667 ) ;
#29852=CARTESIAN_POINT ( 'NONE',  ( -3.050050800000000617, -2.853674364686378695, -1.549418761218566809 ) ) ;
#29854=EDGE_CURVE ( 'NONE', #21409, #533, #31394, .T. ) ;
#29855=CARTESIAN_POINT ( 'NONE',  ( -3.807304909706596519, -1.062355717592093463, -3.000000000000000888 ) ) ;
#29862=CARTESIAN_POINT ( 'NONE',  ( -2.650050800000000262, 2.853674364686379583, 1.549418761218565921 ) ) ;
#29871=ORIENTED_EDGE ( 'NONE', *, *, #8279, .F. ) ;
#29878=CARTESIAN_POINT ( 'NONE',  ( 6.530491241813344061, -8.637950316517745364, -0.6236753264480845438 ) ) ;
#29880=CARTESIAN_POINT ( 'NONE',  ( 5.377543748152548986, -4.007137495034764463, -6.940565734314639634 ) ) ;
#29886=DIRECTION ( 'NONE',  ( 0.000000000000000000, 0.000000000000000000, 1.000000000000000000 ) ) ;
#29891=VERTEX_POINT ( 'NONE', #28866 ) ;
#29893=CARTESIAN_POINT ( 'NONE',  ( -5.804531657079157192, 1.883076972206379374, 2.325406398514293205 ) ) ;
#29894=VECTOR ( 'NONE', #12979, 1000.000000000000000 ) ;
#29895=( BOUNDED_CURVE ( )  B_SPLINE_CURVE ( 2, ( #26976, #11932, #4079, #19466, #18964, #14395, #6579, #9241, #16423, #29151, #18785 ),
 .UNSPECIFIED., .F., .F. ) 
 B_SPLINE_CURVE_WITH_KNOTS ( ( 3, 2, 2, 2, 2, 3 ),
 ( 0.3103822619934377136, 0.3125000000000000000, 0.3281250000000000000, 0.3437500000000000000, 0.3593750000000000000, 0.3728822619934377136 ),
 .UNSPECIFIED. ) 
 CURVE ( )  GEOMETRIC_REPRESENTATION_ITEM ( )  RATIONAL_B_SPLINE_CURVE ( ( 0.9821626249036857770, 0.9896829947469991673, 1.000000000000000000, 0.9238795325112867385, 1.000000000000000000, 0.9238795325112867385, 1.000000000000000000, 0.9238795325112867385, 1.000000000000000000, 0.9341965377642874602, 0.9821626249036857770 ) ) 
 REPRESENTATION_ITEM ( '' )  );
#29899=DIRECTION ( 'NONE',  ( 1.000000000000000000, -0.000000000000000000, -0.000000000000000000 ) ) ;
#29901=EDGE_LOOP ( 'NONE', ( #26495, #26469, #5175 ) ) ;
#29902=DIRECTION ( 'NONE',  ( -1.000000000000000000, -0.000000000000000000, -0.000000000000000000 ) ) ;
#29903=B_SPLINE_CURVE_WITH_KNOTS ( 'NONE', 3,
 ( #13494, #23226, #28393, #18523, #26214, #15696, #25902, #20560, #10657, #31080 ),
 .UNSPECIFIED., .F., .F.,
 ( 4, 2, 2, 2, 4 ),
 ( 2.493548413898819905E-07, 0.0005478513795029395141, 0.001095453404164489124, 0.001643055428826038734, 0.002190657453487588127 ),
 .UNSPECIFIED. ) ;
#29904=ORIENTED_EDGE ( 'NONE', *, *, #19564, .T. ) ;
#29909=CARTESIAN_POINT ( 'NONE',  ( 5.489344087273877015, 6.152099123112526158, -5.297876218488255518 ) ) ;
#29910=LINE ( 'NONE', #6993, #20407 ) ;
#29916=AXIS2_PLACEMENT_3D ( 'NONE', #13407, #13252, #905 ) ;
#29917=CARTESIAN_POINT ( 'NONE',  ( 3.499999999999999556, -5.233522515400120589, 4.720195129223259123 ) ) ;
#29919=CARTESIAN_POINT ( 'NONE',  ( -4.537550801365592967, -1.828967928396026510, 3.368539882008728004 ) ) ;
#29930=EDGE_CURVE ( 'NONE', #10433, #19561, #27305, .T. ) ;
#29931=CIRCLE ( 'NONE', #19786, 2.999999999999999556 ) ;
#29936=CARTESIAN_POINT ( 'NONE',  ( 0.000000000000000000, 0.000000000000000000, 0.000000000000000000 ) ) ;
#29942=CIRCLE ( 'NONE', #5898, 8.750000000000000000 ) ;
#29946=CARTESIAN_POINT ( 'NONE',  ( 7.249760686538667009, 0.000000000000000000, 0.000000000000000000 ) ) ;
#29964=CARTESIAN_POINT ( 'NONE',  ( -10.00000000000000000, 0.000000000000000000, 0.000000000000000000 ) ) ;
#29970=CARTESIAN_POINT ( 'NONE',  ( 7.064632918400240769, -2.318425219014176974, -8.437262856154180923 ) ) ;
#29974=DIRECTION ( 'NONE',  ( 0.000000000000000000, 0.000000000000000000, 1.000000000000000000 ) ) ;
#29976=ORIENTED_EDGE ( 'NONE', *, *, #4387, .F. ) ;
#29981=CARTESIAN_POINT ( 'NONE',  ( -6.187550801365593323, -0.3701630799359326152, 3.521866450007987037 ) ) ;
#29986=PLANE ( 'NONE',  #22641 ) ;
#29992=ORIENTED_EDGE ( 'NONE', *, *, #8279, .T. ) ;
#29998=ORIENTED_EDGE ( 'NONE', *, *, #7097, .T. ) ;
#30005=ORIENTED_EDGE ( 'NONE', *, *, #24976, .F. ) ;
#30020=AXIS2_PLACEMENT_3D ( 'NONE', #25437, #2547, #7727 ) ;
#30028=CARTESIAN_POINT ( 'NONE',  ( -2.050050802731187449, 2.331437884370912705, -1.887961173149511618 ) ) ;
#30029=ORIENTED_EDGE ( 'NONE', *, *, #16828, .F. ) ;
#30030=CARTESIAN_POINT ( 'NONE',  ( -4.700050800000001416, -2.983565686104819648, -0.3135853898029605791 ) ) ;
#30032=DIRECTION ( 'NONE',  ( 0.000000000000000000, 0.2588190451025135785, 0.9659258262890703106 ) ) ;
#30033=CARTESIAN_POINT ( 'NONE',  ( -4.162942409646514186, -5.022711880624455567E-15, 2.999999999999999556 ) ) ;
#30035=VERTEX_POINT ( 'NONE', #590 ) ;
#30036=CARTESIAN_POINT ( 'NONE',  ( -1.762942409646513164, -5.022711880624455567E-15, 2.999999999999999556 ) ) ;
#30039=VECTOR ( 'NONE', #4412, 1000.000000000000000 ) ;
#30042=EDGE_LOOP ( 'NONE', ( #16360, #14099, #22419, #12015 ) ) ;
#30046=CARTESIAN_POINT ( 'NONE',  ( 3.499999999999999556, -7.009698679648292519, 0.7308381473896670144 ) ) ;
#30048=DIRECTION ( 'NONE',  ( 1.000000000000000000, -0.000000000000000000, -0.000000000000000000 ) ) ;
#30049=AXIS2_PLACEMENT_3D ( 'NONE', #33070, #2145, #9840 ) ;
#30051=LINE ( 'NONE', #27530, #18177 ) ;
#30052=CARTESIAN_POINT ( 'NONE',  ( -6.512942406915326110, 3.284080845023683730E-15, 3.000000000000000000 ) ) ;
#30060=CARTESIAN_POINT ( 'NONE',  ( -3.350050802731187272, -0.3135853898029607456, 2.983565686104819648 ) ) ;
#30061=EDGE_LOOP ( 'NONE', ( #20679, #13764, #9256, #6537 ) ) ;
#30063=CARTESIAN_POINT ( 'NONE',  ( 5.887529311434773760, -8.386653846779019261, -0.3723788567093603841 ) ) ;
#30070=EDGE_CURVE ( 'NONE', #22634, #20949, #22013, .T. ) ;
#30073=AXIS2_PLACEMENT_3D ( 'NONE', #25609, #27473, #7745 ) ;
#30082=CARTESIAN_POINT ( 'NONE',  ( 6.038145077921538650, 2.472816103755249184, 8.106170535363455443 ) ) ;
#30085=CARTESIAN_POINT ( 'NONE',  ( -5.204531657079157547, 2.325406398514293205, -1.883076972206379374 ) ) ;
#30097=CIRCLE ( 'NONE', #15661, 5.500000000000000000 ) ;
#30104=CARTESIAN_POINT ( 'NONE',  ( 6.037141869538508843, 7.552970526864689838, 3.843044125430091107 ) ) ;
#30106=EDGE_LOOP ( 'NONE', ( #31290, #3535, #24303 ) ) ;
#30115=CARTESIAN_POINT ( 'NONE',  ( -3.437550801365593767, -1.088641768524163389, -3.675193018007246071 ) ) ;
#30122=( BOUNDED_CURVE ( )  B_SPLINE_CURVE ( 2, ( #30033, #22325, #27834, #9605, #9444, #17324, #17135, #12282, #27344, #29855, #27669 ),
 .UNSPECIFIED., .F., .F. ) 
 B_SPLINE_CURVE_WITH_KNOTS ( ( 3, 2, 2, 2, 2, 3 ),
 ( 0.5603822619934377691, 0.5625000000000000000, 0.5781250000000000000, 0.5937500000000000000, 0.6093750000000000000, 0.6228822619934377691 ),
 .UNSPECIFIED. ) 
 CURVE ( )  GEOMETRIC_REPRESENTATION_ITEM ( )  RATIONAL_B_SPLINE_CURVE ( ( 0.9821626249036861100, 0.9896829947469995004, 1.000000000000000000, 0.9238795325112867385, 1.000000000000000000, 0.9238795325112867385, 1.000000000000000000, 0.9238795325112867385, 1.000000000000000000, 0.9341965377642872381, 0.9821626249036861100 ) ) 
 REPRESENTATION_ITEM ( '' )  );
#30123=AXIS2_PLACEMENT_3D ( 'NONE', #5896, #6083, #11426 ) ;
#30124=CARTESIAN_POINT ( 'NONE',  ( 0.000000000000000000, -1.471047635026914380, 6.892461014225956362 ) ) ;
#30134=ORIENTED_EDGE ( 'NONE', *, *, #32934, .T. ) ;
#30139=CARTESIAN_POINT ( 'NONE',  ( 3.499999999999999556, 2.429606751577119805, -5.757344182232886354 ) ) ;
#30140=ORIENTED_EDGE ( 'NONE', *, *, #32311, .T. ) ;
#30146=VERTEX_POINT ( 'NONE', #7797 ) ;
#30154=CARTESIAN_POINT ( 'NONE',  ( 6.880159396099833735, 4.949130873693378341, 7.192972099401642616 ) ) ;
#30157=CARTESIAN_POINT ( 'NONE',  ( 7.249760686538667009, -3.647351267791625773, 7.953573330858203505 ) ) ;
#30168=CIRCLE ( 'NONE', #15728, 2.999999999999999112 ) ;
#30170=CARTESIAN_POINT ( 'NONE',  ( 5.489321676144490958, -4.149060317827554023, 6.978593840069431842 ) ) ;
#30171=CARTESIAN_POINT ( 'NONE',  ( 3.499999999999999556, -7.009698679648281860, -0.7308381473897611613 ) ) ;
#30172=CARTESIAN_POINT ( 'NONE',  ( -7.487550801365594033, -2.228590825266444586, -2.752080473201636401 ) ) ;
#30173=ORIENTED_EDGE ( 'NONE', *, *, #11171, .T. ) ;
#30176=EDGE_LOOP ( 'NONE', ( #18105, #8093, #27201 ) ) ;
#30182=CARTESIAN_POINT ( 'NONE',  ( 3.499999999999999556, 5.904264776415128146, -2.046865518294647579 ) ) ;
#30186=EDGE_LOOP ( 'NONE', ( #3040, #1795, #31202, #28085 ) ) ;
#30193=FACE_OUTER_BOUND ( 'NONE', #11326, .T. ) ;
#30199=CARTESIAN_POINT ( 'NONE',  ( 3.499999999999999556, 1.459547570502368385, 6.894905428400277536 ) ) ;
#30203=CARTESIAN_POINT ( 'NONE',  ( -2.150050802731187538, 0.3135853898029611342, -2.983565686104819648 ) ) ;
#30205=CARTESIAN_POINT ( 'NONE',  ( -2.500050800000000351, -0.3135853898029607456, 2.983565686104819648 ) ) ;
#30206=EDGE_CURVE ( 'NONE', #24760, #25632, #12496, .T. ) ;
#30208=CARTESIAN_POINT ( 'NONE',  ( -4.200050800000000528, 1.887961173149511618, 2.331437884370912705 ) ) ;
#30209=ORIENTED_EDGE ( 'NONE', *, *, #6930, .T. ) ;
#30220=DIRECTION ( 'NONE',  ( -0.000000000000000000, -0.9961946980917449901, -0.08715574274766567375 ) ) ;
#30223=FACE_OUTER_BOUND ( 'NONE', #18948, .T. ) ;
#30224=VERTEX_POINT ( 'NONE', #17293 ) ;
#30228=CARTESIAN_POINT ( 'NONE',  ( 0.000000000000000000, 4.438567988583181467, -7.249076783337631724 ) ) ;
#30229=CARTESIAN_POINT ( 'NONE',  ( 7.249760686538667009, 0.000000000000000000, 0.000000000000000000 ) ) ;
#30230=ORIENTED_EDGE ( 'NONE', *, *, #16946, .T. ) ;
#30231=DIRECTION ( 'NONE',  ( -1.000000000000000000, 0.000000000000000000, -0.000000000000000000 ) ) ;
#30242=CARTESIAN_POINT ( 'NONE',  ( -7.212550801365592790, 1.828967928396027176, -3.368539882008727115 ) ) ;
#30244=CARTESIAN_POINT ( 'NONE',  ( -7.754531657079159146, -0.9198621039125872700, -3.105402419394638791 ) ) ;
#30245=CARTESIAN_POINT ( 'NONE',  ( 4.749760686538667009, 5.151476664237558900, -6.139290821770204687 ) ) ;
#30248=DIRECTION ( 'NONE',  ( 0.000000000000000000, 0.000000000000000000, 1.000000000000000000 ) ) ;
#30252=CARTESIAN_POINT ( 'NONE',  ( 6.524595623740805372, -5.074779492939337722, 7.015943501182377418 ) ) ;
#30261=EDGE_CURVE ( 'NONE', #4026, #292, #22297, .T. ) ;
#30266=CARTESIAN_POINT ( 'NONE',  ( 5.612974044843318744, 8.123783100924566014, -1.229732182294818621 ) ) ;
#30268=CARTESIAN_POINT ( 'NONE',  ( -3.837550801365593234, 1.088641768524161613, 3.675193018007247403 ) ) ;
#30274=ORIENTED_EDGE ( 'NONE', *, *, #30465, .F. ) ;
#30281=CARTESIAN_POINT ( 'NONE',  ( 5.489321676144490958, 6.978593840069445164, 4.149060317827530042 ) ) ;
#30282=CARTESIAN_POINT ( 'NONE',  ( -1.750050802731187405, -0.3135853898029607456, 2.983565686104819648 ) ) ;
#30285=DIRECTION ( 'NONE',  ( 0.000000000000000000, 0.000000000000000000, 1.000000000000000000 ) ) ;
#30286=EDGE_CURVE ( 'NONE', #32504, #28422, #24620, .T. ) ;
#30296=DIRECTION ( 'NONE',  ( 0.000000000000000000, -0.4226182617406961661, -0.9063077870366516020 ) ) ;
#30300=ORIENTED_EDGE ( 'NONE', *, *, #1635, .T. ) ;
#30305=CARTESIAN_POINT ( 'NONE',  ( 6.883866557622099869, -3.625395379390139894, 7.943335131954991191 ) ) ;
#30313=DIRECTION ( 'NONE',  ( 0.000000000000000000, 0.000000000000000000, -1.000000000000000000 ) ) ;
#30319=CARTESIAN_POINT ( 'NONE',  ( -7.687550801365593323, -2.752080473201636845, 2.228590825266444586 ) ) ;
#30323=CARTESIAN_POINT ( 'NONE',  ( -5.756376981307136376, -0.1572233378491221800, 3.000000000000000000 ) ) ;
#30324=EDGE_CURVE ( 'NONE', #901, #4009, #4590, .T. ) ;
#30327=ORIENTED_EDGE ( 'NONE', *, *, #15383, .T. ) ;
#30331=ORIENTED_EDGE ( 'NONE', *, *, #10190, .F. ) ;
#30335=ORIENTED_EDGE ( 'NONE', *, *, #14129, .F. ) ;
#30339=DIRECTION ( 'NONE',  ( 1.000000000000000000, 0.000000000000000000, -0.000000000000000000 ) ) ;
#30342=CARTESIAN_POINT ( 'NONE',  ( -5.450050799999999640, -2.853674364686378695, -1.549418761218566809 ) ) ;
#30350=CARTESIAN_POINT ( 'NONE',  ( 5.489343806296448136, 8.012901424861411215, 1.307372367723665940 ) ) ;
#30352=ADVANCED_FACE ( 'NONE', ( #4428 ), #9923, .T. ) ;
#30353=CYLINDRICAL_SURFACE ( 'NONE', #19890, 3.000000000000000444 ) ;
#30355=CARTESIAN_POINT ( 'NONE',  ( -2.500050802731187627, -1.549418761218565477, 2.853674364686380471 ) ) ;
#30358=CARTESIAN_POINT ( 'NONE',  ( -3.100050800000000439, -2.983565686104819648, -0.3135853898029605791 ) ) ;
#30360=CARTESIAN_POINT ( 'NONE',  ( 7.249760686538667009, -8.711672189281420842, -0.8180878109962766986 ) ) ;
#30369=VERTEX_POINT ( 'NONE', #20950 ) ;
#30386=CARTESIAN_POINT ( 'NONE',  ( 6.524595126109738352, -0.8869162863045095824, 8.613374939462822510 ) ) ;
#30391=CARTESIAN_POINT ( 'NONE',  ( -8.012550801365593500, 1.828967928396027176, -3.368539882008727115 ) ) ;
#30393=CARTESIAN_POINT ( 'NONE',  ( -5.554531657079158080, -3.105402419394638791, 0.9198621039125867149 ) ) ;
#30400=CYLINDRICAL_SURFACE ( 'NONE', #30049, 2.999999999999999112 ) ;
#30401=DIRECTION ( 'NONE',  ( 0.000000000000000000, 0.000000000000000000, 1.000000000000000000 ) ) ;
#30403=CARTESIAN_POINT ( 'NONE',  ( 5.489344087273876127, -5.138668362895322694, 6.285690376021081605 ) ) ;
#30409=CARTESIAN_POINT ( 'NONE',  ( 5.885541416630536204, -0.3712256868991837266, -8.385500676968934641 ) ) ;
#30417=CARTESIAN_POINT ( 'NONE',  ( -4.562550801365594211, 2.228590825266444142, 2.752080473201636845 ) ) ;
#30424=CARTESIAN_POINT ( 'NONE',  ( 3.499999999999999556, -5.848742439617962141, 6.167836887840967286 ) ) ;
#30455=DIRECTION ( 'NONE',  ( 0.000000000000000000, 0.000000000000000000, 1.000000000000000000 ) ) ;
#30459=CARTESIAN_POINT ( 'NONE',  ( 7.249760686538667009, -6.147671362329260702, 6.226446564517894799 ) ) ;
#30465=EDGE_CURVE ( 'NONE', #14398, #27971, #26288, .T. ) ;
#30466=CARTESIAN_POINT ( 'NONE',  ( 7.249760686538667009, -5.151476664237518044, 6.139290821770238438 ) ) ;
#30467=AXIS2_PLACEMENT_3D ( 'NONE', #24200, #1322, #21692 ) ;
#30477=CARTESIAN_POINT ( 'NONE',  ( 7.249760686538667009, -4.973063321323927255, 7.199384779417104419 ) ) ;
#30478=DIRECTION ( 'NONE',  ( -1.000000000000000000, 0.000000000000000000, 0.000000000000000000 ) ) ;
#30479=CARTESIAN_POINT ( 'NONE',  ( -6.937550801365595099, -1.828967928396026732, 3.368539882008728004 ) ) ;
#30485=DIRECTION ( 'NONE',  ( -1.000000000000000000, -0.000000000000000000, -0.000000000000000000 ) ) ;
#30486=CARTESIAN_POINT ( 'NONE',  ( 5.885541416630534428, -8.385500676968931089, 0.3712256868992730441 ) ) ;
#30500=CARTESIAN_POINT ( 'NONE',  ( 4.749760686538667009, 8.014274990069656823, -8.669741416787380218E-17 ) ) ;
#30503=AXIS2_PLACEMENT_3D ( 'NONE', #29946, #24770, #7036 ) ;
#30517=CIRCLE ( 'NONE', #27821, 2.999999999999999112 ) ;
#30525=LINE ( 'NONE', #17812, #137 ) ;
#30526=CARTESIAN_POINT ( 'NONE',  ( -2.250050802731187183, -1.887961173149512062, -2.331437884370912261 ) ) ;
#30528=CARTESIAN_POINT ( 'NONE',  ( -4.287550801365592967, -2.228590825266444586, -2.752080473201636401 ) ) ;
#30529=AXIS2_PLACEMENT_3D ( 'NONE', #25817, #5094, #15104 ) ;
#30533=CARTESIAN_POINT ( 'NONE',  ( 5.377543748152548986, -5.151476664237435443, -6.139290821770307716 ) ) ;
#30534=CARTESIAN_POINT ( 'NONE',  ( 5.377543748152548098, 7.530955069117513112, 2.741043480754951744 ) ) ;
#30539=DIRECTION ( 'NONE',  ( 1.000000000000000000, 0.000000000000000000, 0.000000000000000000 ) ) ;
#30541=ORIENTED_EDGE ( 'NONE', *, *, #647, .F. ) ;
#30551=DIRECTION ( 'NONE',  ( 1.000000000000000000, -0.000000000000000000, -0.000000000000000000 ) ) ;
#30553=EDGE_CURVE ( 'NONE', #22104, #17772, #6002, .T. ) ;
#30554=LINE ( 'NONE', #17841, #5031 ) ;
#30568=FACE_OUTER_BOUND ( 'NONE', #8145, .T. ) ;
#30571=CIRCLE ( 'NONE', #27964, 8.750000000000000000 ) ;
#30572=CARTESIAN_POINT ( 'NONE',  ( -7.712550801365593678, 1.088641768524161613, 3.675193018007247403 ) ) ;
#30576=CARTESIAN_POINT ( 'NONE',  ( -4.954531657079158435, 0.9198621039125853827, 3.105402419394639235 ) ) ;
#30579=DIRECTION ( 'NONE',  ( 0.000000000000000000, 0.000000000000000000, 1.000000000000000000 ) ) ;
#30583=ORIENTED_EDGE ( 'NONE', *, *, #12657, .F. ) ;
#30587=CARTESIAN_POINT ( 'NONE',  ( 7.249760686538667009, 2.210816291636212405, 8.466096581343489191 ) ) ;
#30594=CARTESIAN_POINT ( 'NONE',  ( 5.489321606599604664, 7.664118171219035602, -2.678948506461252599 ) ) ;
#30595=VECTOR ( 'NONE', #20409, 1000.000000000000000 ) ;
#30602=VECTOR ( 'NONE', #20123, 999.9999999999998863 ) ;
#30606=CARTESIAN_POINT ( 'NONE',  ( -6.462550801365593678, 0.3701630799359330593, -3.521866450007987037 ) ) ;
#30613=EDGE_LOOP ( 'NONE', ( #25170, #5080, #13441 ) ) ;
#30625=EDGE_CURVE ( 'NONE', #3908, #16153, #7045, .T. ) ;
#30626=AXIS2_PLACEMENT_3D ( 'NONE', #28320, #8098, #10604 ) ;
#30643=ORIENTED_EDGE ( 'NONE', *, *, #5299, .T. ) ;
#30648=CARTESIAN_POINT ( 'NONE',  ( 6.883866557622099869, -8.415306967752693268, 2.328663417917411049 ) ) ;
#30649=PLANE ( 'NONE',  #26268 ) ;
#30655=VECTOR ( 'NONE', #15587, 999.9999999999998863 ) ;
#30659=DIRECTION ( 'NONE',  ( 0.000000000000000000, 0.5735764363510510444, -0.8191520442889883569 ) ) ;
#30669=EDGE_CURVE ( 'NONE', #29851, #14011, #20100, .T. ) ;
#30674=PLANE ( 'NONE',  #24657 ) ;
#30675=CARTESIAN_POINT ( 'NONE',  ( -5.537550801365593856, 3.368539882008727115, 1.828967928396027176 ) ) ;
#30691=CARTESIAN_POINT ( 'NONE',  ( 5.377543748152548986, -4.007137495034764463, -6.940565734314639634 ) ) ;
#30697=CARTESIAN_POINT ( 'NONE',  ( 7.249760686538667009, 7.953573330858214163, 3.647351267791597795 ) ) ;
#30699=CARTESIAN_POINT ( 'NONE',  ( -5.712942406915326288, 3.284080845023683730E-15, 3.000000000000000000 ) ) ;
#30704=CARTESIAN_POINT ( 'NONE',  ( 6.038144483126824724, 8.463061282283012687, 0.4487862922133540877 ) ) ;
#30708=CARTESIAN_POINT ( 'NONE',  ( 4.749760686538667009, -4.007137495034764463, -6.940565734314639634 ) ) ;
#30709=CARTESIAN_POINT ( 'NONE',  ( 3.499999999999999556, 5.471841788314708133, 3.018103451449746899 ) ) ;
#30711=DIRECTION ( 'NONE',  ( -1.000000000000000000, -0.000000000000000000, 0.000000000000000000 ) ) ;
#30714=CARTESIAN_POINT ( 'NONE',  ( -3.400050802731187982, 0.9222479816126443186, 3.113457007523260156 ) ) ;
#30716=CARTESIAN_POINT ( 'NONE',  ( -6.687550801365594211, -2.228590825266444586, -2.752080473201636401 ) ) ;
#30724=VERTEX_POINT ( 'NONE', #2194 ) ;
#30729=VERTEX_POINT ( 'NONE', #12382 ) ;
#30732=CARTESIAN_POINT ( 'NONE',  ( 7.064632816082964339, 0.7071067811866330599, -8.721381771256195847 ) ) ;
#30738=CARTESIAN_POINT ( 'NONE',  ( 3.499999999999999556, 0.000000000000000000, 0.000000000000000000 ) ) ;
#30750=ORIENTED_EDGE ( 'NONE', *, *, #22054, .F. ) ;
#30751=CARTESIAN_POINT ( 'NONE',  ( -6.762550801365593500, -2.752080473201636845, 2.228590825266444586 ) ) ;
#30753=CARTESIAN_POINT ( 'NONE',  ( -5.004531657079158258, 1.883076972206379374, 2.325406398514293205 ) ) ;
#30763=EDGE_CURVE ( 'NONE', #5413, #10538, #17080, .T. ) ;
#30770=CARTESIAN_POINT ( 'NONE',  ( -7.700050802731188249, 1.549418761218566143, -2.853674364686379583 ) ) ;
#30772=DIRECTION ( 'NONE',  ( 0.000000000000000000, 0.000000000000000000, 1.000000000000000000 ) ) ;
#30773=CARTESIAN_POINT ( 'NONE',  ( 1.750000000000000222, 4.058600654062949786, -7.468451026206159860 ) ) ;
#30775=EDGE_LOOP ( 'NONE', ( #11445, #10349, #12030, #21309 ) ) ;
#30776=CARTESIAN_POINT ( 'NONE',  ( -5.162550801365593856, -2.752080473201636845, 2.228590825266444586 ) ) ;
#30792=EDGE_LOOP ( 'NONE', ( #29564, #2041, #19593 ) ) ;
#30804=ORIENTED_EDGE ( 'NONE', *, *, #24510, .T. ) ;
#30807=CARTESIAN_POINT ( 'NONE',  ( -6.262550801365593500, 3.521866450007987037, 0.3701630799359328372 ) ) ;
#30818=ORIENTED_EDGE ( 'NONE', *, *, #18380, .T. ) ;
#30824=CARTESIAN_POINT ( 'NONE',  ( 7.064423539573518873, 8.721381771257245674, -0.7071067811875828557 ) ) ;
#30828=DIRECTION ( 'NONE',  ( 0.000000000000000000, -0.1045284632676534292, 0.9945218953682734009 ) ) ;
#30831=ADVANCED_FACE ( 'NONE', ( #16368 ), #1002, .T. ) ;
#30834=DIRECTION ( 'NONE',  ( 0.000000000000000000, 0.000000000000000000, 1.000000000000000000 ) ) ;
#30835=CARTESIAN_POINT ( 'NONE',  ( 7.064423637758999952, -8.437262856155475887, -2.318425219013692473 ) ) ;
#30839=ORIENTED_EDGE ( 'NONE', *, *, #17254, .T. ) ;
#30847=VERTEX_POINT ( 'NONE', #31598 ) ;
#30851=ORIENTED_EDGE ( 'NONE', *, *, #19550, .T. ) ;
#30853=DIRECTION ( 'NONE',  ( -1.000000000000000000, -0.000000000000000000, -0.000000000000000000 ) ) ;
#30855=CARTESIAN_POINT ( 'NONE',  ( 0.000000000000000000, 0.000000000000000000, 0.000000000000000000 ) ) ;
#30862=CARTESIAN_POINT ( 'NONE',  ( 6.880159540721329847, -3.624895993596817245, -7.943102264535292001 ) ) ;
#30864=CARTESIAN_POINT ( 'NONE',  ( 6.037141812302426302, -8.411869123983608532, -1.028012177296172780 ) ) ;
#30868=CARTESIAN_POINT ( 'NONE',  ( -5.387550801365593500, -0.3701630799359326152, 3.521866450007987037 ) ) ;
#30871=ORIENTED_EDGE ( 'NONE', *, *, #13752, .F. ) ;
#30875=DIRECTION ( 'NONE',  ( 0.000000000000000000, 0.000000000000000000, 1.000000000000000000 ) ) ;
#30883=DIRECTION ( 'NONE',  ( 0.000000000000000000, 0.000000000000000000, 1.000000000000000000 ) ) ;
#30895=CARTESIAN_POINT ( 'NONE',  ( -8.000050799999998574, -1.094676798671502471, 2.924497836550261187 ) ) ;
#30899=ORIENTED_EDGE ( 'NONE', *, *, #24908, .F. ) ;
#30901=CARTESIAN_POINT ( 'NONE',  ( -5.462550801365593678, 3.521866450007987037, 0.3701630799359328372 ) ) ;
#30903=CARTESIAN_POINT ( 'NONE',  ( -3.354531657079158347, 0.9198621039125853827, 3.105402419394639235 ) ) ;
#30907=EDGE_LOOP ( 'NONE', ( #18127, #15139, #12862 ) ) ;
#30915=CARTESIAN_POINT ( 'NONE',  ( 3.499999999999999556, 0.005878491403554959860, -7.047692205288322853 ) ) ;
#30919=DIRECTION ( 'NONE',  ( 0.000000000000000000, 0.8660254037844362651, 0.5000000000000038858 ) ) ;
#30923=EDGE_LOOP ( 'NONE', ( #25403, #14069, #25582, #5692 ) ) ;
#30924=CARTESIAN_POINT ( 'NONE',  ( -5.912550801365592967, -3.675193018007246071, 1.088641768524163167 ) ) ;
#30925=CARTESIAN_POINT ( 'NONE',  ( 6.038145268433180668, -6.771555838910892966, 5.096160642893628356 ) ) ;
#30938=ORIENTED_EDGE ( 'NONE', *, *, #16834, .F. ) ;
#30947=ORIENTED_EDGE ( 'NONE', *, *, #8526, .F. ) ;
#30949=CARTESIAN_POINT ( 'NONE',  ( 7.249760686538667009, -7.892520144992426268, -1.391664247347309535 ) ) ;
#30951=DIRECTION ( 'NONE',  ( 0.000000000000000000, 0.2588190451025135785, 0.9659258262890703106 ) ) ;
#30953=VECTOR ( 'NONE', #27109, 1000.000000000000000 ) ;
#30959=CARTESIAN_POINT ( 'NONE',  ( 7.249760686538667009, 0.000000000000000000, 0.000000000000000000 ) ) ;
#30964=LINE ( 'NONE', #30466, #16747 ) ;
#30968=CARTESIAN_POINT ( 'NONE',  ( -8.000050800000000351, 0.1053597294728410155, -2.998641260211496462 ) ) ;
#30970=FACE_OUTER_BOUND ( 'NONE', #30775, .T. ) ;
#30979=CARTESIAN_POINT ( 'NONE',  ( 6.356382228872881512, -8.265862592379907170, -2.398350474622027662 ) ) ;
#30984=FACE_OUTER_BOUND ( 'NONE', #31217, .T. ) ;
#30985=ORIENTED_EDGE ( 'NONE', *, *, #12026, .F. ) ;
#30990=CARTESIAN_POINT ( 'NONE',  ( 6.037141869538512395, -4.619542287584855522, -7.104659103919393814 ) ) ;
#30991=VECTOR ( 'NONE', #5604, 1000.000000000000000 ) ;
#30994=CARTESIAN_POINT ( 'NONE',  ( -3.312942406915326377, -5.022711880624455567E-15, 2.999999999999999556 ) ) ;
#30996=VERTEX_POINT ( 'NONE', #1500 ) ;
#31001=CARTESIAN_POINT ( 'NONE',  ( -8.000050800000000351, 3.673940397442060361E-16, 3.000000000000000444 ) ) ;
#31005=EDGE_CURVE ( 'NONE', #901, #12812, #14871, .T. ) ;
#31015=CARTESIAN_POINT ( 'NONE',  ( 5.377543748152551650, -7.892520144992426268, -1.391664247347309535 ) ) ;
#31021=ADVANCED_FACE ( 'NONE', ( #25037 ), #9162, .F. ) ;
#31022=DIRECTION ( 'NONE',  ( 0.000000000000000000, 0.000000000000000000, 1.000000000000000000 ) ) ;
#31035=DIRECTION ( 'NONE',  ( 0.000000000000000000, 0.000000000000000000, 1.000000000000000000 ) ) ;
#31036=ORIENTED_EDGE ( 'NONE', *, *, #24442, .T. ) ;
#31038=DIRECTION ( 'NONE',  ( 0.000000000000000000, 0.000000000000000000, 1.000000000000000000 ) ) ;
#31043=EDGE_CURVE ( 'NONE', #32504, #26433, #29217, .T. ) ;
#31046=AXIS2_PLACEMENT_3D ( 'NONE', #4109, #14431, #21811 ) ;
#31049=CARTESIAN_POINT ( 'NONE',  ( -3.800050800000000617, -1.887961173149512062, -2.331437884370912261 ) ) ;
#31052=LINE ( 'NONE', #20838, #25889 ) ;
#31057=CARTESIAN_POINT ( 'NONE',  ( -4.462550801365592790, -0.3701630799359326152, 3.521866450007987037 ) ) ;
#31060=CARTESIAN_POINT ( 'NONE',  ( -4.804531657079157192, -2.325406398514293205, 1.883076972206379818 ) ) ;
#31061=CARTESIAN_POINT ( 'NONE',  ( 1.750000000000000222, -8.497168642645966941, 0.2193742428684632428 ) ) ;
#31064=ORIENTED_EDGE ( 'NONE', *, *, #20101, .T. ) ;
#31065=DIRECTION ( 'NONE',  ( 0.000000000000000000, 0.7431448254773954654, -0.6691306063588569053 ) ) ;
#31075=EDGE_CURVE ( 'NONE', #25757, #22634, #21286, .T. ) ;
#31076=VECTOR ( 'NONE', #16788, 1000.000000000000227 ) ;
#31077=VECTOR ( 'NONE', #18373, 1000.000000000000000 ) ;
#31078=CARTESIAN_POINT ( 'NONE',  ( 7.064632879756605810, -8.466096581343467875, -2.210816291636299002 ) ) ;
#31080=CARTESIAN_POINT ( 'NONE',  ( 7.249760686538667009, 7.135485519861997972, 5.064320921489847471 ) ) ;
#31083=CARTESIAN_POINT ( 'NONE',  ( 5.489343806296449024, -7.976812024616034336, 1.512045527216178575 ) ) ;
#31089=CARTESIAN_POINT ( 'NONE',  ( -6.562550801365594211, -2.228590825266444586, -2.752080473201636401 ) ) ;
#31096=CIRCLE ( 'NONE', #7033, 2.750000000000000444 ) ;
#31101=AXIS2_PLACEMENT_3D ( 'NONE', #25591, #31134, #20601 ) ;
#31111=CARTESIAN_POINT ( 'NONE',  ( 6.524595395369781947, -2.369138865965884744, 8.328507089302171096 ) ) ;
#31119=ADVANCED_FACE ( 'NONE', ( #25395 ), #18031, .T. ) ;
#31123=ORIENTED_EDGE ( 'NONE', *, *, #31204, .T. ) ;
#31128=EDGE_LOOP ( 'NONE', ( #25973, #30331, #1996, #13020 ) ) ;
#31129=VECTOR ( 'NONE', #7174, 999.9999999999998863 ) ;
#31130=DIRECTION ( 'NONE',  ( 0.000000000000000000, 0.000000000000000000, -1.000000000000000000 ) ) ;
#31131=CARTESIAN_POINT ( 'NONE',  ( -4.012550801365593500, 1.828967928396027398, -3.368539882008727115 ) ) ;
#31134=DIRECTION ( 'NONE',  ( 0.000000000000000000, -0.5735764363510434949, -0.8191520442889936859 ) ) ;
#31144=ORIENTED_EDGE ( 'NONE', *, *, #17710, .F. ) ;
#31164=EDGE_CURVE ( 'NONE', #11105, #9082, #26833, .T. ) ;
#31175=CARTESIAN_POINT ( 'NONE',  ( -8.000050800000009232, 2.460349816355251296, -2.612134329618188922 ) ) ;
#31176=AXIS2_PLACEMENT_3D ( 'NONE', #16856, #27052, #4157 ) ;
#31198=CARTESIAN_POINT ( 'NONE',  ( 6.357668022120090079, -5.959864878090717966, 6.210015626210365625 ) ) ;
#31200=DIRECTION ( 'NONE',  ( -1.000000000000000000, 0.000000000000000000, -0.000000000000000000 ) ) ;
#31202=ORIENTED_EDGE ( 'NONE', *, *, #19387, .T. ) ;
#31204=EDGE_CURVE ( 'NONE', #299, #9383, #15004, .T. ) ;
#31217=EDGE_LOOP ( 'NONE', ( #4781, #23479, #21789 ) ) ;
#31218=CARTESIAN_POINT ( 'NONE',  ( -1.765934045424250254, -0.3164610288023907980, 3.010925563584172515 ) ) ;
#31225=CARTESIAN_POINT ( 'NONE',  ( 3.499999999999999556, 0.000000000000000000, 0.000000000000000000 ) ) ;
#31228=CARTESIAN_POINT ( 'NONE',  ( 4.749760686538667009, -6.139290821770289064, 5.151476664237455871 ) ) ;
#31230=DIRECTION ( 'NONE',  ( 1.000000000000000000, -0.000000000000000000, -0.000000000000000000 ) ) ;
#31232=EDGE_CURVE ( 'NONE', #28176, #29851, #14535, .T. ) ;
#31238=CARTESIAN_POINT ( 'NONE',  ( -3.812550801365593323, 3.368539882008727115, 1.828967928396026954 ) ) ;
#31240=CARTESIAN_POINT ( 'NONE',  ( -2.854531657079157903, 1.545410377633947174, -2.846291840500173365 ) ) ;
#31242=DIRECTION ( 'NONE',  ( -0.000000000000000000, 0.9659258262890683122, -0.2588190451025207950 ) ) ;
#31243=EDGE_CURVE ( 'NONE', #23656, #26528, #20715, .T. ) ;
#31248=ORIENTED_EDGE ( 'NONE', *, *, #11276, .T. ) ;
#31253=CARTESIAN_POINT ( 'NONE',  ( 6.357667697713667465, -8.357963647880060520, -2.056386458247358551 ) ) ;
#31254=CARTESIAN_POINT ( 'NONE',  ( 5.887530024394194150, 8.008238305624880482, -2.518482652462476157 ) ) ;
#31257=CARTESIAN_POINT ( 'NONE',  ( 7.249760686538667009, 4.007137495034909236, -6.940565734314555257 ) ) ;
#31262=CARTESIAN_POINT ( 'NONE',  ( -2.562550801365592879, -2.228590825266444586, -2.752080473201636401 ) ) ;
#31263=CARTESIAN_POINT ( 'NONE',  ( 4.749760686538667009, 7.530955069117551304, -2.741043480754851380 ) ) ;
#31290=ORIENTED_EDGE ( 'NONE', *, *, #9103, .T. ) ;
#31292=CARTESIAN_POINT ( 'NONE',  ( -3.062550801365593323, 3.521866450007987037, 0.3701630799359328372 ) ) ;
#31294=EDGE_CURVE ( 'NONE', #12581, #13848, #32669, .T. ) ;
#31296=CARTESIAN_POINT ( 'NONE',  ( 7.064423637759001728, 7.953573330858883850, -3.647351267792822149 ) ) ;
#31298=CARTESIAN_POINT ( 'NONE',  ( -6.087550801365593678, -2.752080473201636845, 2.228590825266444586 ) ) ;
#31303=CARTESIAN_POINT ( 'NONE',  ( -7.750050802731187183, 0.3135853898029611342, -2.983565686104819648 ) ) ;
#31306=DIRECTION ( 'NONE',  ( 0.000000000000000000, -0.7071067811865570096, 0.7071067811865380248 ) ) ;
#31323=CARTESIAN_POINT ( 'NONE',  ( -7.948539046346460246, -3.109529733928910744, 0.8848824693245758155 ) ) ;
#31329=CARTESIAN_POINT ( 'NONE',  ( 7.249760686538667009, -7.199384779417155045, 4.973063321323851760 ) ) ;
#31330=CARTESIAN_POINT ( 'NONE',  ( 7.064423659272770273, -3.748318449931968832, 7.906491560605070745 ) ) ;
#31338=CARTESIAN_POINT ( 'NONE',  ( 3.499999999999999556, 8.357095590591338663, -1.552080310331533486 ) ) ;
#31344=ORIENTED_EDGE ( 'NONE', *, *, #7108, .T. ) ;
#31349=VERTEX_POINT ( 'NONE', #17604 ) ;
#31353=ORIENTED_EDGE ( 'NONE', *, *, #18502, .T. ) ;
#31365=CARTESIAN_POINT ( 'NONE',  ( -7.357304906975410397, 1.062355717592093463, 3.000000000000000000 ) ) ;
#31367=ORIENTED_EDGE ( 'NONE', *, *, #26118, .F. ) ;
#31368=DIRECTION ( 'NONE',  ( 0.000000000000000000, -0.9945218953682744001, 0.1045284632676436593 ) ) ;
#31373=DIRECTION ( 'NONE',  ( 0.000000000000000000, 0.000000000000000000, 1.000000000000000000 ) ) ;
#31377=DIRECTION ( 'NONE',  ( 0.000000000000000000, -0.5735764363510537089, 0.8191520442889864695 ) ) ;
#31379=ADVANCED_FACE ( 'NONE', ( #22305 ), #32516, .T. ) ;
#31380=LINE ( 'NONE', #1102, #11799 ) ;
#31381=CARTESIAN_POINT ( 'NONE',  ( 4.749760686538667009, 7.892520144992453801, -1.391664247347147443 ) ) ;
#31385=CARTESIAN_POINT ( 'NONE',  ( -4.212550801365593678, -3.368539882008727115, -1.828967928396028064 ) ) ;
#31387=CARTESIAN_POINT ( 'NONE',  ( -5.550050800000001061, -3.113457007523259268, 0.9222479816126455399 ) ) ;
#31391=VERTEX_POINT ( 'NONE', #22151 ) ;
#31393=ORIENTED_EDGE ( 'NONE', *, *, #2151, .F. ) ;
#31394=LINE ( 'NONE', #26206, #23586 ) ;
#31406=CARTESIAN_POINT ( 'NONE',  ( -2.962550801365593234, 2.228590825266444142, 2.752080473201636845 ) ) ;
#31411=EDGE_CURVE ( 'NONE', #16537, #18185, #32363, .T. ) ;
#31413=CYLINDRICAL_SURFACE ( 'NONE', #10733, 2.999999999999999112 ) ;
#31417=CYLINDRICAL_SURFACE ( 'NONE', #3391, 3.000000000000000444 ) ;
#31419=CARTESIAN_POINT ( 'NONE',  ( -1.799351409542603308, -0.03945526729468277344, 3.068704260183690913 ) ) ;
#31421=CARTESIAN_POINT ( 'NONE',  ( -3.087550801365593234, 2.228590825266444142, 2.752080473201636845 ) ) ;
#31423=CARTESIAN_POINT ( 'NONE',  ( 7.249760686538667009, 2.318425219014230265, 8.437262856154170265 ) ) ;
#31425=CARTESIAN_POINT ( 'NONE',  ( 6.356382228872880624, -2.398350474622000128, 8.265862592379914275 ) ) ;
#31433=ADVANCED_FACE ( 'NONE', ( #6910 ), #14923, .F. ) ;
#31437=CARTESIAN_POINT ( 'NONE',  ( -5.462550801365593678, 3.521866450007987037, 0.3701630799359328372 ) ) ;
#31442=CARTESIAN_POINT ( 'NONE',  ( -5.037550801365593856, -1.088641768524163389, -3.675193018007246071 ) ) ;
#31448=ORIENTED_EDGE ( 'NONE', *, *, #25073, .T. ) ;
#31455=CARTESIAN_POINT ( 'NONE',  ( 5.377543748152548986, -6.139290821770289064, 5.151476664237455871 ) ) ;
#31456=DIRECTION ( 'NONE',  ( -1.000000000000000000, 0.000000000000000000, -0.000000000000000000 ) ) ;
#31458=CARTESIAN_POINT ( 'NONE',  ( -6.037550801365592967, -3.675193018007246071, 1.088641768524163167 ) ) ;
#31459=ORIENTED_EDGE ( 'NONE', *, *, #3981, .F. ) ;
#31467=CARTESIAN_POINT ( 'NONE',  ( 7.249760686538667009, 0.8180878109962995692, -8.711672189281419065 ) ) ;
#31469=CARTESIAN_POINT ( 'NONE',  ( -7.998722633285748174, -2.371517779863575370, 1.837526800715260533 ) ) ;
#31483=CARTESIAN_POINT ( 'NONE',  ( -3.100050802731187272, -2.853674364686378695, -1.549418761218566809 ) ) ;
#31484=EDGE_CURVE ( 'NONE', #20064, #4337, #32802, .T. ) ;
#31485=DIRECTION ( 'NONE',  ( -1.000000000000000000, -0.000000000000000000, 0.000000000000000000 ) ) ;
#31488=CARTESIAN_POINT ( 'NONE',  ( 7.249760686538667009, -6.226446564517957860, 6.147671362329200306 ) ) ;
#31490=CARTESIAN_POINT ( 'NONE',  ( 6.037141848526923482, 8.105561522824309861, 2.473100090966190656 ) ) ;
#31497=VERTEX_POINT ( 'NONE', #25982 ) ;
#31498=ADVANCED_FACE ( 'NONE', ( #28302 ), #15921, .F. ) ;
#31504=AXIS2_PLACEMENT_3D ( 'NONE', #20681, #12975, #31035 ) ;
#31505=ORIENTED_EDGE ( 'NONE', *, *, #26118, .T. ) ;
#31508=DIRECTION ( 'NONE',  ( 0.000000000000000000, -0.08715574274766220431, 0.9961946980917452121 ) ) ;
#31510=VERTEX_POINT ( 'NONE', #15423 ) ;
#31514=VERTEX_POINT ( 'NONE', #13102 ) ;
#31516=DIRECTION ( 'NONE',  ( -0.000000000000000000, 0.8191520442889909104, 0.5735764363510474917 ) ) ;
#31520=CARTESIAN_POINT ( 'NONE',  ( 5.377543748152548098, -2.789499415801756586E-14, 8.014274990069656823 ) ) ;
#31521=EDGE_CURVE ( 'NONE', #16776, #10415, #31673, .T. ) ;
#31523=DIRECTION ( 'NONE',  ( -1.000000000000000000, 0.000000000000000000, 0.000000000000000000 ) ) ;
#31532=DIRECTION ( 'NONE',  ( 0.000000000000000000, 0.000000000000000000, -1.000000000000000000 ) ) ;
#31535=CIRCLE ( 'NONE', #25658, 6.249000000000000554 ) ;
#31536=B_SPLINE_CURVE_WITH_KNOTS ( 'NONE', 3,
 ( #30477, #14594, #9910, #7391, #27784, #19616, #22285, #15079, #30170, #17279 ),
 .UNSPECIFIED., .F., .F.,
 ( 4, 2, 2, 2, 4 ),
 ( 1.968338519003008803E-07, 0.0005467926395225666770, 0.001093388445193233015, 0.001639984250863899245, 0.002186580056534565691 ),
 .UNSPECIFIED. ) ;
#31538=CARTESIAN_POINT ( 'NONE',  ( -2.062550801365593323, -0.3701630799359326152, 3.521866450007987037 ) ) ;
#31540=CARTESIAN_POINT ( 'NONE',  ( -7.400050800000000706, 1.887961173149511618, 2.331437884370912705 ) ) ;
#31552=EDGE_CURVE ( 'NONE', #23417, #20990, #23446, .T. ) ;
#31565=CIRCLE ( 'NONE', #17133, 2.999999999999999112 ) ;
#31566=CARTESIAN_POINT ( 'NONE',  ( -10.00000000000000000, 0.000000000000000000, 0.000000000000000000 ) ) ;
#31568=CARTESIAN_POINT ( 'NONE',  ( -3.762550801365593500, 2.228590825266444142, 2.752080473201636845 ) ) ;
#31570=LINE ( 'NONE', #5521, #8608 ) ;
#31571=VERTEX_POINT ( 'NONE', #10927 ) ;
#31577=DIRECTION ( 'NONE',  ( 1.000000000000000000, -0.000000000000000000, -0.000000000000000000 ) ) ;
#31581=LINE ( 'NONE', #16197, #19393 ) ;
#31583=AXIS2_PLACEMENT_3D ( 'NONE', #3578, #3425, #9044 ) ;
#31585=CARTESIAN_POINT ( 'NONE',  ( -4.237550801365593145, -1.088641768524163611, -3.675193018007245627 ) ) ;
#31587=CARTESIAN_POINT ( 'NONE',  ( -2.162942409646512854, 4.884725290497410777E-15, -2.999999999999999556 ) ) ;
#31588=AXIS2_PLACEMENT_3D ( 'NONE', #26959, #1223, #31816 ) ;
#31597=ORIENTED_EDGE ( 'NONE', *, *, #27124, .T. ) ;
#31598=CARTESIAN_POINT ( 'NONE',  ( 7.249760686538667009, -7.906491560603691404, 3.748318449932265484 ) ) ;
#31600=VECTOR ( 'NONE', #9402, 1000.000000000000000 ) ;
#31601=ORIENTED_EDGE ( 'NONE', *, *, #17958, .T. ) ;
#31603=CARTESIAN_POINT ( 'NONE',  ( -3.812550801365593323, 3.368539882008727115, 1.828967928396027176 ) ) ;
#31607=DIRECTION ( 'NONE',  ( 1.000000000000000000, -0.000000000000000000, 0.000000000000000000 ) ) ;
#31610=CARTESIAN_POINT ( 'NONE',  ( -5.637550801365595277, 3.675193018007247403, -1.088641768524161391 ) ) ;
#31613=CARTESIAN_POINT ( 'NONE',  ( 7.064632879756604034, 2.210816291636326980, -8.466096581343460770 ) ) ;
#31625=VECTOR ( 'NONE', #11707, 1000.000000000000000 ) ;
#31627=ADVANCED_FACE ( 'NONE', ( #2585 ), #23147, .T. ) ;
#31628=VECTOR ( 'NONE', #17318, 1000.000000000000000 ) ;
#31631=CARTESIAN_POINT ( 'NONE',  ( -6.437550801365593323, 3.675193018007247403, -1.088641768524161391 ) ) ;
#31633=CIRCLE ( 'NONE', #1204, 2.999999999999999112 ) ;
#31639=CARTESIAN_POINT ( 'NONE',  ( 3.499999999999999556, 1.418488851014487073, -6.085876303339362359 ) ) ;
#31646=DIRECTION ( 'NONE',  ( 0.000000000000000000, 0.4067366430758009299, -0.9135454576426005335 ) ) ;
#31653=EDGE_CURVE ( 'NONE', #27732, #32541, #8802, .T. ) ;
#31654=DIRECTION ( 'NONE',  ( 0.000000000000000000, 0.000000000000000000, -1.000000000000000000 ) ) ;
#31660=AXIS2_PLACEMENT_3D ( 'NONE', #18438, #6353, #1200 ) ;
#31661=PLANE ( 'NONE',  #17153 ) ;
#31662=CIRCLE ( 'NONE', #9760, 6.249000000000000554 ) ;
#31667=CIRCLE ( 'NONE', #18292, 8.750000000000000000 ) ;
#31671=CARTESIAN_POINT ( 'NONE',  ( 4.749760686538667009, 2.741043480755029016, -7.530955069117485579 ) ) ;
#31673=CIRCLE ( 'NONE', #11297, 8.750000000000000000 ) ;
#31674=CARTESIAN_POINT ( 'NONE',  ( 6.524595395369781059, 8.328507089302179978, 2.369138865965855878 ) ) ;
#31675=CYLINDRICAL_SURFACE ( 'NONE', #4931, 3.000000000000000444 ) ;
#31683=DIRECTION ( 'NONE',  ( 0.000000000000000000, 0.000000000000000000, -1.000000000000000000 ) ) ;
#31686=AXIS2_PLACEMENT_3D ( 'NONE', #9603, #19825, #30032 ) ;
#31689=EDGE_CURVE ( 'NONE', #3605, #8263, #91, .T. ) ;
#31694=CARTESIAN_POINT ( 'NONE',  ( 5.612974259723589654, 2.996912441296280427, -7.650268724902028694 ) ) ;
#31696=ORIENTED_EDGE ( 'NONE', *, *, #1497, .F. ) ;
#31703=PLANE ( 'NONE',  #27749 ) ;
#31704=ORIENTED_EDGE ( 'NONE', *, *, #30286, .T. ) ;
#31708=FACE_OUTER_BOUND ( 'NONE', #23403, .T. ) ;
#31717=AXIS2_PLACEMENT_3D ( 'NONE', #20507, #18478, #23174 ) ;
#31724=CARTESIAN_POINT ( 'NONE',  ( -4.912550801365593856, -1.088641768524163389, -3.675193018007246071 ) ) ;
#31727=CARTESIAN_POINT ( 'NONE',  ( -5.400050800000000706, -1.887961173149512062, -2.331437884370912261 ) ) ;
#31729=CARTESIAN_POINT ( 'NONE',  ( -5.000050800000001239, 1.887961173149511618, 2.331437884370912705 ) ) ;
#31733=CIRCLE ( 'NONE', #13037, 8.500000000000000000 ) ;
#31747=CARTESIAN_POINT ( 'NONE',  ( 7.064423637759001728, -7.953573330858861645, 3.647351267792873220 ) ) ;
#31750=CARTESIAN_POINT ( 'NONE',  ( -3.162550801365593856, 2.752080473201636845, -2.228590825266444142 ) ) ;
#31751=CARTESIAN_POINT ( 'NONE',  ( 0.000000000000000000, -2.834406817834963732, 8.013497238472769624 ) ) ;
#31753=PLANE ( 'NONE',  #5984 ) ;
#31758=ORIENTED_EDGE ( 'NONE', *, *, #9879, .T. ) ;
#31762=ADVANCED_FACE ( 'NONE', ( #3721 ), #9039, .F. ) ;
#31766=CARTESIAN_POINT ( 'NONE',  ( -4.737550801365594033, 3.368539882008727115, 1.828967928396027176 ) ) ;
#31770=LINE ( 'NONE', #6321, #31129 ) ;
#31775=CARTESIAN_POINT ( 'NONE',  ( -3.600050802731187716, 3.113457007523260156, -0.9222479816126439855 ) ) ;
#31781=CARTESIAN_POINT ( 'NONE',  ( -4.412550801365592079, -1.828967928396026732, 3.368539882008728004 ) ) ;
#31786=CARTESIAN_POINT ( 'NONE',  ( -7.637550801365593500, -3.675193018007246071, 1.088641768524163167 ) ) ;
#31801=DIRECTION ( 'NONE',  ( -0.000000000000000000, 0.9063077870366493816, 0.4226182617407007736 ) ) ;
#31811=CARTESIAN_POINT ( 'NONE',  ( 0.000000000000000000, 0.000000000000000000, 0.000000000000000000 ) ) ;
#31814=ORIENTED_EDGE ( 'NONE', *, *, #21436, .F. ) ;
#31816=DIRECTION ( 'NONE',  ( 0.000000000000000000, -0.4226182617407034936, 0.9063077870366480493 ) ) ;
#31818=ORIENTED_EDGE ( 'NONE', *, *, #27894, .T. ) ;
#31826=CARTESIAN_POINT ( 'NONE',  ( 5.377543748152548986, 7.892520144992453801, -1.391664247347147443 ) ) ;
#31829=DIRECTION ( 'NONE',  ( 0.000000000000000000, 0.000000000000000000, 1.000000000000000000 ) ) ;
#31831=CARTESIAN_POINT ( 'NONE',  ( 5.885541736258995904, 8.006759975090648851, 2.519172009311959837 ) ) ;
#31834=CARTESIAN_POINT ( 'NONE',  ( 7.249760686538666121, 0.000000000000000000, 0.000000000000000000 ) ) ;
#31839=CARTESIAN_POINT ( 'NONE',  ( 7.249760686538667009, -8.466096581343496297, 2.210816291636187536 ) ) ;
#31845=ADVANCED_FACE ( 'NONE', ( #5704 ), #32975, .F. ) ;
#31850=ORIENTED_EDGE ( 'NONE', *, *, #10559, .T. ) ;
#31851=ORIENTED_EDGE ( 'NONE', *, *, #3154, .F. ) ;
#31854=ORIENTED_EDGE ( 'NONE', *, *, #27562, .F. ) ;
#31872=CARTESIAN_POINT ( 'NONE',  ( 0.000000000000000000, -6.700937042937042065, -2.183447440113257976 ) ) ;
#31876=CARTESIAN_POINT ( 'NONE',  ( -4.650050802731187538, -1.887961173149512062, -2.331437884370912261 ) ) ;
#31878=CARTESIAN_POINT ( 'NONE',  ( -7.650050800000001594, 1.549418761218566143, -2.853674364686379583 ) ) ;
#31882=ORIENTED_EDGE ( 'NONE', *, *, #3209, .F. ) ;
#31884=EDGE_CURVE ( 'NONE', #508, #16345, #24644, .T. ) ;
#31890=DIRECTION ( 'NONE',  ( 0.000000000000000000, 0.000000000000000000, 1.000000000000000000 ) ) ;
#31896=ADVANCED_FACE ( 'NONE', ( #24 ), #30649, .F. ) ;
#31901=CARTESIAN_POINT ( 'NONE',  ( -3.012550801365593500, 3.368539882008727115, 1.828967928396026954 ) ) ;
#31904=CARTESIAN_POINT ( 'NONE',  ( 6.883866601413088482, -3.754588506078551102, -7.883091392499357752 ) ) ;
#31906=DIRECTION ( 'NONE',  ( 0.000000000000000000, -0.9659258262890710878, 0.2588190451025100258 ) ) ;
#31910=FACE_OUTER_BOUND ( 'NONE', #22839, .T. ) ;
#31919=CARTESIAN_POINT ( 'NONE',  ( -2.337550801365593678, 3.368539882008727115, 1.828967928396027176 ) ) ;
#31920=APPLICATION_CONTEXT ( 'configuration controlled 3d designs of mechanical parts and assemblies' ) ;
#31922=CARTESIAN_POINT ( 'NONE',  ( 4.749760686538667009, 6.940565734314653845, -4.007137495034738706 ) ) ;
#31925=EDGE_CURVE ( 'NONE', #32003, #24925, #1177, .T. ) ;
#31928=CARTESIAN_POINT ( 'NONE',  ( -3.756376981307136376, 0.1572233378491263989, -2.999999999999999556 ) ) ;
#31930=CARTESIAN_POINT ( 'NONE',  ( 6.883866601413089370, 3.754588506078606613, 7.883091392499333772 ) ) ;
#31931=ORIENTED_EDGE ( 'NONE', *, *, #27733, .T. ) ;
#31937=DIRECTION ( 'NONE',  ( 0.000000000000000000, 0.4067366430758009299, -0.9135454576426005335 ) ) ;
#31938=ORIENTED_EDGE ( 'NONE', *, *, #2113, .F. ) ;
#31939=CARTESIAN_POINT ( 'NONE',  ( -5.237550801365594033, -3.675193018007246071, 1.088641768524163167 ) ) ;
#31940=CARTESIAN_POINT ( 'NONE',  ( 7.249760686538667009, -0.7071067811864522046, -8.721381771256211834 ) ) ;
#31944=EDGE_LOOP ( 'NONE', ( #332, #8997, #5733 ) ) ;
#31948=B_SPLINE_CURVE_WITH_KNOTS ( 'NONE', 3,
 ( #5539, #850, #674, #10681, #8353, #31425, #31111, #8501, #21379, #18894 ),
 .UNSPECIFIED., .F., .F.,
 ( 4, 2, 2, 2, 4 ),
 ( 2.740849916257185138E-07, 0.0005478761651001761357, 0.001095478245208724843, 0.001643080325317273658, 0.002190682405425822474 ),
 .UNSPECIFIED. ) ;
#31953=DIRECTION ( 'NONE',  ( -1.000000000000000000, -0.000000000000000000, 0.000000000000000000 ) ) ;
#31955=CARTESIAN_POINT ( 'NONE',  ( -3.737550801365593589, -1.828967928396026510, 3.368539882008728004 ) ) ;
#31960=CARTESIAN_POINT ( 'NONE',  ( 6.356381935169119757, -2.055898738447941909, -8.357622142800108733 ) ) ;
#31962=ORIENTED_EDGE ( 'NONE', *, *, #14248, .T. ) ;
#31964=VERTEX_POINT ( 'NONE', #26583 ) ;
#31968=ORIENTED_EDGE ( 'NONE', *, *, #8162, .T. ) ;
#31969=EDGE_CURVE ( 'NONE', #27551, #10376, #1357, .T. ) ;
#31971=CARTESIAN_POINT ( 'NONE',  ( -6.156376981307135843, 0.1572233378491243172, -2.999999999999999556 ) ) ;
#31973=ORIENTED_EDGE ( 'NONE', *, *, #19564, .F. ) ;
#31975=CARTESIAN_POINT ( 'NONE',  ( 3.499999999999999556, 6.704570150426983233, 5.172265885002680363 ) ) ;
#31976=( BOUNDED_SURFACE ( )  B_SPLINE_SURFACE ( 1, 2, ( 
 ( #8520, #6339, #13701, #29416, #24055, #26923, #16033, #18721, #19222, #21730, #21581, #31786, #16228, #8857, #21244, #6193, #3379, #18914, #11195, #18567, #19065, #1509, #28926, #29105, #14195, #16715, #26263, #1011, #16377, #6512, #26444, #4027, #26586, #1360, #24392, #6031, #11380, #16531, #23903, #21401, #21096, #3690, #31298, #8370, #28759, #29255, #13849, #3857, #5849, #14031, #3543, #31610, #8698, #13545, #26739, #23754, #1180, #24243, #11535, #31939, #9005, #867, #11046, #31442, #6687, #32292, #9861, #12348, #12184, #22384, #6839, #32601, #11866, #29919, #27072, #9504, #1862, #9177, #9673, #25235, #9352, #19719, #4833, #7340, #16876, #24736, #7001, #30268, #17024, #17530, #17214, #25046, #27724, #19562, #2011, #30115, #4345, #12038, #15013, #27420, #11687, #21886, #19406, #19901, #4527, #27578, #32101, #4677, #29759, #22233, #27230, #29605, #7192, #4174, #14525, #14847, #17384, #2164, #14701, #32443, #14341 ),
 ( #24549, #22568, #1671, #24899, #32782, #20072, #22075, #339, #13029, #23235, #10167, #7496, #17696, #25559, #20875, #27911, #18195, #8000, #5024, #15203, #25404, #15354, #2859, #17887, #2514, #2665, #10512, #20388, #10357, #13177, #31089, #28402, #30606, #33090, #23050, #20724, #12682, #22737, #5519, #8180, #20569, #10665, #22886, #30924, #7688, #7847, #28079, #23378, #482, #5176, #15705, #28578, #18383, #25912, #12835, #12530, #5672, #174, #30776, #18040, #3022, #15852, #28229, #5335, #15516, #25729, #2355, #32941, #10011, #20222, #30417, #26063, #13983, #19030, #5985, #26223, #16342, #3165, #21359, #21209, #13323, #23718, #13505, #6462, #8652, #24014, #31568, #18872, #1324, #11155, #23536, #26551, #11333, #24202, #11009, #652, #16183, #11498, #31750, #21694, #29071, #31901, #31406, #10846, #3812, #13808, #8482, #21060, #18532, #8336, #31262, #28724, #28882, #26408, #8968, #3509, #15997, #13664, #832, #21543, #18681 ) ),
 .UNSPECIFIED., .F., .F., .F. ) 
 B_SPLINE_SURFACE_WITH_KNOTS ( ( 2, 2 ),
 ( 3, 2, 2, 2, 2, 2, 2, 2, 2, 2, 2, 2, 2, 2, 2, 2, 2, 2, 2, 2, 2, 2, 2, 2, 2, 2, 2, 2, 2, 2, 2, 2, 2, 2, 2, 2, 2, 2, 2, 2, 2, 2, 2, 2, 2, 2, 2, 2, 2, 2, 2, 2, 2, 2, 2, 2, 2, 2, 2, 2, 3 ),
 ( 0.000000000000000000, 1.000000000000000000 ),
 ( 0.000000000000000000, 0.01562500000000000000, 0.03125000000000000000, 0.04687500000000000000, 0.06250000000000000000, 0.07812500000000000000, 0.09375000000000000000, 0.1093750000000000000, 0.1250000000000000000, 0.1406250000000000000, 0.1562500000000000000, 0.1718750000000000000, 0.1875000000000000000, 0.2031250000000000000, 0.2187500000000000000, 0.2343750000000000000, 0.2500000000000000000, 0.2656250000000000000, 0.2812500000000000000, 0.2968750000000000000, 0.3125000000000000000, 0.3281250000000000000, 0.3437500000000000000, 0.3593750000000000000, 0.3750000000000000000, 0.3906250000000000000, 0.4062500000000000000, 0.4218750000000000000, 0.4375000000000000000, 0.4531250000000000000, 0.4687500000000000000, 0.4843750000000000000, 0.5000000000000000000, 0.5156250000000000000, 0.5312500000000000000, 0.5468750000000000000, 0.5625000000000000000, 0.5781250000000000000, 0.5937500000000000000, 0.6093750000000000000, 0.6250000000000000000, 0.6406250000000000000, 0.6562500000000000000, 0.6718750000000000000, 0.6875000000000000000, 0.7031250000000000000, 0.7187500000000000000, 0.7343750000000000000, 0.7500000000000000000, 0.7656250000000000000, 0.7812500000000000000, 0.7968750000000000000, 0.8125000000000000000, 0.8281250000000000000, 0.8437500000000000000, 0.8593750000000000000, 0.8750000000000000000, 0.8906250000000000000, 0.9062500000000000000, 0.9218750000000000000, 0.9375000000000000000 ),
 .UNSPECIFIED. ) 
 GEOMETRIC_REPRESENTATION_ITEM ( )  RATIONAL_B_SPLINE_SURFACE ( (
 ( 1.000000000000000000, 0.9238795325112867385, 1.000000000000000000, 0.9238795325112867385, 1.000000000000000000, 0.9238795325112867385, 1.000000000000000000, 0.9238795325112867385, 1.000000000000000000, 0.9238795325112867385, 1.000000000000000000, 0.9238795325112867385, 1.000000000000000000, 0.9238795325112867385, 1.000000000000000000, 0.9238795325112867385, 1.000000000000000000, 0.9238795325112867385, 1.000000000000000000, 0.9238795325112867385, 1.000000000000000000, 0.9238795325112867385, 1.000000000000000000, 0.9238795325112867385, 1.000000000000000000, 0.9238795325112867385, 1.000000000000000000, 0.9238795325112867385, 1.000000000000000000, 0.9238795325112867385, 1.000000000000000000, 0.9238795325112867385, 1.000000000000000000, 0.9238795325112867385, 1.000000000000000000, 0.9238795325112867385, 1.000000000000000000, 0.9238795325112867385, 1.000000000000000000, 0.9238795325112867385, 1.000000000000000000, 0.9238795325112867385, 1.000000000000000000, 0.9238795325112867385, 1.000000000000000000, 0.9238795325112867385, 1.000000000000000000, 0.9238795325112867385, 1.000000000000000000, 0.9238795325112867385, 1.000000000000000000, 0.9238795325112867385, 1.000000000000000000, 0.9238795325112867385, 1.000000000000000000, 0.9238795325112867385, 1.000000000000000000, 0.9238795325112867385, 1.000000000000000000, 0.9238795325112867385, 1.000000000000000000, 0.9238795325112867385, 1.000000000000000000, 0.9238795325112867385, 1.000000000000000000, 0.9238795325112867385, 1.000000000000000000, 0.9238795325112867385, 1.000000000000000000, 0.9238795325112867385, 1.000000000000000000, 0.9238795325112867385, 1.000000000000000000, 0.9238795325112867385, 1.000000000000000000, 0.9238795325112867385, 1.000000000000000000, 0.9238795325112867385, 1.000000000000000000, 0.9238795325112867385, 1.000000000000000000, 0.9238795325112867385, 1.000000000000000000, 0.9238795325112867385, 1.000000000000000000, 0.9238795325112867385, 1.000000000000000000, 0.9238795325112867385, 1.000000000000000000, 0.9238795325112867385, 1.000000000000000000, 0.9238795325112867385, 1.000000000000000000, 0.9238795325112867385, 1.000000000000000000, 0.9238795325112867385, 1.000000000000000000, 0.9238795325112867385, 1.000000000000000000, 0.9238795325112867385, 1.000000000000000000, 0.9238795325112867385, 1.000000000000000000, 0.9238795325112867385, 1.000000000000000000, 0.9238795325112867385, 1.000000000000000000, 0.9238795325112867385, 1.000000000000000000, 0.9238795325112867385, 1.000000000000000000, 0.9238795325112867385, 1.000000000000000000, 0.9238795325112867385, 1.000000000000000000, 0.9238795325112867385, 1.000000000000000000, 0.9238795325112867385, 1.000000000000000000, 0.9238795325112867385, 1.000000000000000000),
 ( 1.000000000000000000, 0.9238795325112867385, 1.000000000000000000, 0.9238795325112867385, 1.000000000000000000, 0.9238795325112867385, 1.000000000000000000, 0.9238795325112867385, 1.000000000000000000, 0.9238795325112867385, 1.000000000000000000, 0.9238795325112867385, 1.000000000000000000, 0.9238795325112867385, 1.000000000000000000, 0.9238795325112867385, 1.000000000000000000, 0.9238795325112867385, 1.000000000000000000, 0.9238795325112867385, 1.000000000000000000, 0.9238795325112867385, 1.000000000000000000, 0.9238795325112867385, 1.000000000000000000, 0.9238795325112867385, 1.000000000000000000, 0.9238795325112867385, 1.000000000000000000, 0.9238795325112867385, 1.000000000000000000, 0.9238795325112867385, 1.000000000000000000, 0.9238795325112867385, 1.000000000000000000, 0.9238795325112867385, 1.000000000000000000, 0.9238795325112867385, 1.000000000000000000, 0.9238795325112867385, 1.000000000000000000, 0.9238795325112867385, 1.000000000000000000, 0.9238795325112867385, 1.000000000000000000, 0.9238795325112867385, 1.000000000000000000, 0.9238795325112867385, 1.000000000000000000, 0.9238795325112867385, 1.000000000000000000, 0.9238795325112867385, 1.000000000000000000, 0.9238795325112867385, 1.000000000000000000, 0.9238795325112867385, 1.000000000000000000, 0.9238795325112867385, 1.000000000000000000, 0.9238795325112867385, 1.000000000000000000, 0.9238795325112867385, 1.000000000000000000, 0.9238795325112867385, 1.000000000000000000, 0.9238795325112867385, 1.000000000000000000, 0.9238795325112867385, 1.000000000000000000, 0.9238795325112867385, 1.000000000000000000, 0.9238795325112867385, 1.000000000000000000, 0.9238795325112867385, 1.000000000000000000, 0.9238795325112867385, 1.000000000000000000, 0.9238795325112867385, 1.000000000000000000, 0.9238795325112867385, 1.000000000000000000, 0.9238795325112867385, 1.000000000000000000, 0.9238795325112867385, 1.000000000000000000, 0.9238795325112867385, 1.000000000000000000, 0.9238795325112867385, 1.000000000000000000, 0.9238795325112867385, 1.000000000000000000, 0.9238795325112867385, 1.000000000000000000, 0.9238795325112867385, 1.000000000000000000, 0.9238795325112867385, 1.000000000000000000, 0.9238795325112867385, 1.000000000000000000, 0.9238795325112867385, 1.000000000000000000, 0.9238795325112867385, 1.000000000000000000, 0.9238795325112867385, 1.000000000000000000, 0.9238795325112867385, 1.000000000000000000, 0.9238795325112867385, 1.000000000000000000, 0.9238795325112867385, 1.000000000000000000, 0.9238795325112867385, 1.000000000000000000, 0.9238795325112867385, 1.000000000000000000, 0.9238795325112867385, 1.000000000000000000, 0.9238795325112867385, 1.000000000000000000, 0.9238795325112867385, 1.000000000000000000) ) ) 
 REPRESENTATION_ITEM ( '' )  SURFACE ( )  );
#31980=ORIENTED_EDGE ( 'NONE', *, *, #23617, .T. ) ;
#31981=DIRECTION ( 'NONE',  ( 0.000000000000000000, 0.000000000000000000, -1.000000000000000000 ) ) ;
#31983=PLANE ( 'NONE',  #17886 ) ;
#31987=ORIENTED_EDGE ( 'NONE', *, *, #6293, .T. ) ;
#31993=DIRECTION ( 'NONE',  ( 0.000000000000000000, -1.000000000000000000, 0.000000000000000000 ) ) ;
#31994=VERTEX_POINT ( 'NONE', #6509 ) ;
#32003=VERTEX_POINT ( 'NONE', #13359 ) ;
#32006=CARTESIAN_POINT ( 'NONE',  ( 7.064632918400240769, -7.953573330858190182, -3.647351267791651086 ) ) ;
#32010=AXIS2_PLACEMENT_3D ( 'NONE', #14955, #30539, #10296 ) ;
#32011=CARTESIAN_POINT ( 'NONE',  ( 6.880159790065803804, 0.8322990769133554734, -8.691376398188690899 ) ) ;
#32012=B_SPLINE_CURVE_WITH_KNOTS ( 'NONE', 3,
 ( #3199, #26261, #18565, #23409, #8368, #18719, #29103, #21094, #31296, #2901 ),
 .UNSPECIFIED., .F., .F.,
 ( 4, 2, 2, 2, 4 ),
 ( 2.740849916258459394E-07, 0.0005478761651001745094, 0.001095478245208723325, 0.001643080325317272140, 0.002190682405425820739 ),
 .UNSPECIFIED. ) ;
#32015=CARTESIAN_POINT ( 'NONE',  ( 6.530491751506347420, 5.074604403564672239, 7.017944781891974237 ) ) ;
#32018=FACE_OUTER_BOUND ( 'NONE', #5738, .T. ) ;
#32021=CARTESIAN_POINT ( 'NONE',  ( 3.499999999999999556, -3.573533178329615367, 5.126388750707211450 ) ) ;
#32022=CARTESIAN_POINT ( 'NONE',  ( 7.064632918400241657, 7.953573330858215940, 3.647351267791597351 ) ) ;
#32023=B_SPLINE_CURVE_WITH_KNOTS ( 'NONE', 3,
 ( #18985, #32006, #14265, #3760, #11454, #16949, #16611, #4246, #24629, #18816 ),
 .UNSPECIFIED., .F., .F.,
 ( 4, 2, 2, 2, 4 ),
 ( 1.968338519012340724E-07, 0.0005467927057105486386, 0.001093388577569196071, 0.001639984449427843612, 0.002186580321286490936 ),
 .UNSPECIFIED. ) ;
#32026=EDGE_CURVE ( 'NONE', #32858, #19214, #5021, .T. ) ;
#32028=CARTESIAN_POINT ( 'NONE',  ( -5.250050802731188071, 2.331437884370912705, -1.887961173149511618 ) ) ;
#32029=ORIENTED_EDGE ( 'NONE', *, *, #2861, .T. ) ;
#32030=CARTESIAN_POINT ( 'NONE',  ( -6.600050800000000883, 1.887961173149511618, 2.331437884370912705 ) ) ;
#32031=VECTOR ( 'NONE', #32950, 1000.000000000000000 ) ;
#32033=EDGE_CURVE ( 'NONE', #9995, #4314, #666, .T. ) ;
#32036=DIRECTION ( 'NONE',  ( 0.000000000000000000, 0.8191520442889912434, -0.5735764363510469366 ) ) ;
#32042=CARTESIAN_POINT ( 'NONE',  ( 7.064423669210280643, 6.147671362330681788, 6.226446564518065330 ) ) ;
#32046=ADVANCED_FACE ( 'NONE', ( #5173 ), #25556, .F. ) ;
#32052=CIRCLE ( 'NONE', #17089, 8.500000000000000000 ) ;
#32055=CARTESIAN_POINT ( 'NONE',  ( 5.489343958331425632, -7.593062460271018388, 2.874233210898338609 ) ) ;
#32062=CARTESIAN_POINT ( 'NONE',  ( -4.500050802731188071, 1.549418761218566143, -2.853674364686379583 ) ) ;
#32064=DIRECTION ( 'NONE',  ( 0.000000000000000000, -0.9063077870366542665, 0.4226182617406900044 ) ) ;
#32068=CARTESIAN_POINT ( 'NONE',  ( 4.749760686538667009, 7.530955069117513112, 2.741043480754951744 ) ) ;
#32071=CARTESIAN_POINT ( 'NONE',  ( 5.377543748152549874, 2.741043480754926875, 7.530955069117522882 ) ) ;
#32078=DIRECTION ( 'NONE',  ( 0.000000000000000000, -0.7431448254773862505, -0.6691306063588670083 ) ) ;
#32079=PLANE ( 'NONE',  #22620 ) ;
#32080=ORIENTED_EDGE ( 'NONE', *, *, #25936, .T. ) ;
#32083=AXIS2_PLACEMENT_3D ( 'NONE', #12148, #5421, #25010 ) ;
#32096=DIRECTION ( 'NONE',  ( 0.000000000000000000, -0.2588190451025291217, 0.9659258262890659807 ) ) ;
#32101=CARTESIAN_POINT ( 'NONE',  ( -2.887550801365593500, -2.752080473201636845, 2.228590825266444586 ) ) ;
#32116=DIRECTION ( 'NONE',  ( 0.000000000000000000, 0.000000000000000000, -1.000000000000000000 ) ) ;
#32122=CARTESIAN_POINT ( 'NONE',  ( -2.387550801365593056, 3.521866450007987037, 0.3701630799359328372 ) ) ;
#32123=ORIENTED_EDGE ( 'NONE', *, *, #25393, .T. ) ;
#32125=ORIENTED_EDGE ( 'NONE', *, *, #3772, .F. ) ;
#32127=CARTESIAN_POINT ( 'NONE',  ( 0.000000000000000000, 1.106368468154540263, -8.427689411260562480 ) ) ;
#32131=CARTESIAN_POINT ( 'NONE',  ( 6.880159790065803804, 2.190520500543487348, 8.451885315426432399 ) ) ;
#32134=AXIS2_PLACEMENT_3D ( 'NONE', #19145, #16961, #16633 ) ;
#32139=DIRECTION ( 'NONE',  ( -0.000000000000000000, 0.08715574274765541807, -0.9961946980917457672 ) ) ;
#32144=CARTESIAN_POINT ( 'NONE',  ( 6.883866621640342132, 6.123537914202324295, -6.224335161394955129 ) ) ;
#32151=FACE_OUTER_BOUND ( 'NONE', #5890, .T. ) ;
#32152=CARTESIAN_POINT ( 'NONE',  ( 5.887530024394193262, -3.218326717262310677, 7.753515897409877233 ) ) ;
#32162=AXIS2_PLACEMENT_3D ( 'NONE', #30245, #32576, #14322 ) ;
#32166=DIRECTION ( 'NONE',  ( 0.000000000000000000, 0.8191520442889936859, -0.5735764363510433839 ) ) ;
#32173=CARTESIAN_POINT ( 'NONE',  ( 5.377543748152550762, 7.530955069117551304, -2.741043480754851380 ) ) ;
#32174=ORIENTED_EDGE ( 'NONE', *, *, #26122, .F. ) ;
#32175=EDGE_CURVE ( 'NONE', #26433, #28422, #1881, .T. ) ;
#32176=AXIS2_PLACEMENT_3D ( 'NONE', #17826, #28028, #30875 ) ;
#32177=EDGE_CURVE ( 'NONE', #30224, #22455, #12909, .T. ) ;
#32178=CARTESIAN_POINT ( 'NONE',  ( 7.249760686538667009, 4.007137495034812424, 6.940565734314612101 ) ) ;
#32185=AXIS2_PLACEMENT_3D ( 'NONE', #195, #4852, #10374 ) ;
#32186=CARTESIAN_POINT ( 'NONE',  ( 5.377543748152548098, -6.940565734314625423, 4.007137495034787555 ) ) ;
#32190=AXIS2_PLACEMENT_3D ( 'NONE', #28851, #20844, #18350 ) ;
#32194=CARTESIAN_POINT ( 'NONE',  ( 7.249760686538667009, -7.892520144992443143, 1.391664247347202288 ) ) ;
#32199=AXIS2_PLACEMENT_3D ( 'NONE', #8559, #8743, #13888 ) ;
#32200=( GEOMETRIC_REPRESENTATION_CONTEXT ( 3 ) GLOBAL_UNCERTAINTY_ASSIGNED_CONTEXT ( ( #5478 ) ) GLOBAL_UNIT_ASSIGNED_CONTEXT ( ( #5446, #10610, #28525 ) ) REPRESENTATION_CONTEXT ( 'NONE', 'WORKASPACE' ) );
#32206=DIRECTION ( 'NONE',  ( 1.000000000000000000, 0.000000000000000000, 0.000000000000000000 ) ) ;
#32213=CIRCLE ( 'NONE', #17781, 6.248999999999999666 ) ;
#32216=CARTESIAN_POINT ( 'NONE',  ( -5.050050802731187005, 1.887961173149511618, 2.331437884370912705 ) ) ;
#32220=CARTESIAN_POINT ( 'NONE',  ( -7.587550801365593678, -3.521866450007987037, -0.3701630799359323931 ) ) ;
#32221=CIRCLE ( 'NONE', #3397, 6.249000000000001442 ) ;
#32245=CARTESIAN_POINT ( 'NONE',  ( 3.499999999999999556, 0.000000000000000000, 0.000000000000000000 ) ) ;
#32247=CARTESIAN_POINT ( 'NONE',  ( -8.000050800000000351, 3.673940397442060361E-16, 3.000000000000000444 ) ) ;
#32251=DIRECTION ( 'NONE',  ( -1.000000000000000000, -0.000000000000000000, -0.000000000000000000 ) ) ;
#32254=CARTESIAN_POINT ( 'NONE',  ( 6.530491712438075247, -3.778856441136667854, -7.792522225867680952 ) ) ;
#32255=CARTESIAN_POINT ( 'NONE',  ( 3.499999999999999556, -7.009698679648292519, 0.7308381473896670144 ) ) ;
#32258=CARTESIAN_POINT ( 'NONE',  ( -8.000050800000000351, 3.450593544762993847, 0.6811748426398763767 ) ) ;
#32259=CARTESIAN_POINT ( 'NONE',  ( 5.612974441954674099, -6.163896661468935001, -5.432722698947220152 ) ) ;
#32260=CARTESIAN_POINT ( 'NONE',  ( 5.377543748152548986, 4.007137495034812424, 6.940565734314612101 ) ) ;
#32264=CARTESIAN_POINT ( 'NONE',  ( -2.750050802731187627, 2.983565686104819648, 0.3135853898029609677 ) ) ;
#32266=CARTESIAN_POINT ( 'NONE',  ( -7.904531657079157725, -2.975847129947406522, -0.3127741368606805072 ) ) ;
#32271=CARTESIAN_POINT ( 'NONE',  ( 3.499999999999999556, 8.265874651078016555, 1.981241088980809639 ) ) ;
#32284=ORIENTED_EDGE ( 'NONE', *, *, #28572, .T. ) ;
#32286=CARTESIAN_POINT ( 'NONE',  ( -2.312550801365593767, 3.675193018007246959, -1.088641768524161391 ) ) ;
#32289=CARTESIAN_POINT ( 'NONE',  ( 5.489344046532323773, 3.969101778624022803, -7.082516960462276856 ) ) ;
#32292=CARTESIAN_POINT ( 'NONE',  ( -4.937550801365593323, 1.828967928396027176, -3.368539882008727115 ) ) ;
#32293=CARTESIAN_POINT ( 'NONE',  ( 3.499999999999999556, -5.848742439617878652, -6.167836887841044557 ) ) ;
#32294=CARTESIAN_POINT ( 'NONE',  ( 3.499999999999999556, 1.459547570502463198, -6.894905428400257996 ) ) ;
#32297=CARTESIAN_POINT ( 'NONE',  ( 5.887530180601100227, -7.076866030741283176, -4.515817126386082236 ) ) ;
#32309=CARTESIAN_POINT ( 'NONE',  ( -3.887550801365593500, 2.228590825266444142, 2.752080473201636845 ) ) ;
#32311=EDGE_CURVE ( 'NONE', #33059, #16776, #17239, .T. ) ;
#32312=VERTEX_POINT ( 'NONE', #17550 ) ;
#32316=CARTESIAN_POINT ( 'NONE',  ( 7.249760686538667009, 6.147671362329219846, 6.226446564517938320 ) ) ;
#32322=ORIENTED_EDGE ( 'NONE', *, *, #16663, .T. ) ;
#32327=CARTESIAN_POINT ( 'NONE',  ( 5.377543748152549874, 5.151476664237558900, -6.139290821770204687 ) ) ;
#32341=DIRECTION ( 'NONE',  ( 0.000000000000000000, 0.000000000000000000, -1.000000000000000000 ) ) ;
#32347=VERTEX_POINT ( 'NONE', #27933 ) ;
#32361=B_SPLINE_CURVE_WITH_KNOTS ( 'NONE', 3,
 ( #16841, #16667, #24689, #29878, #14478, #1818, #30063, #4299, #3994, #19683 ),
 .UNSPECIFIED., .F., .F.,
 ( 4, 2, 2, 2, 4 ),
 ( 1.968338519010778477E-07, 0.0005467930078056964724, 0.001093389181759491739, 0.001639985355713287222, 0.002186581529667082704 ),
 .UNSPECIFIED. ) ;
#32363=LINE ( 'NONE', #9423, #24094 ) ;
#32364=CARTESIAN_POINT ( 'NONE',  ( -8.000050800000000351, 0.000000000000000000, 0.000000000000000000 ) ) ;
#32369=CARTESIAN_POINT ( 'NONE',  ( 5.612974044843316968, 1.229732182294900555, 8.123783100924550027 ) ) ;
#32381=CARTESIAN_POINT ( 'NONE',  ( -4.500050802731188071, 1.549418761218566143, -2.853674364686379583 ) ) ;
#32383=CARTESIAN_POINT ( 'NONE',  ( -3.750050800000001239, -0.9222479816126459840, -3.113457007523259268 ) ) ;
#32387=CARTESIAN_POINT ( 'NONE',  ( 3.499999999999999556, 4.438567988583181467, -7.249076783337631724 ) ) ;
#32397=CARTESIAN_POINT ( 'NONE',  ( 6.357667697713671018, -2.056386458247330129, 8.357963647880069402 ) ) ;
#32398=CYLINDRICAL_SURFACE ( 'NONE', #18708, 2.999999999999999112 ) ;
#32409=CARTESIAN_POINT ( 'NONE',  ( 5.887530180601099339, -3.870837198608047203, -7.449245365665835727 ) ) ;
#32419=CARTESIAN_POINT ( 'NONE',  ( -6.954531657079158435, -0.9198621039125872700, -3.105402419394638791 ) ) ;
#32420=DIRECTION ( 'NONE',  ( -1.000000000000000000, 0.000000000000000000, 0.000000000000000000 ) ) ;
#32424=VERTEX_POINT ( 'NONE', #25576 ) ;
#32427=EDGE_LOOP ( 'NONE', ( #26062, #32546, #9627, #3508 ) ) ;
#32435=FACE_OUTER_BOUND ( 'NONE', #30792, .T. ) ;
#32436=CARTESIAN_POINT ( 'NONE',  ( 5.612718761614564400, -7.212912035758782814, -3.934162523501308684 ) ) ;
#32443=CARTESIAN_POINT ( 'NONE',  ( -2.237550801365593589, 1.088641768524161613, 3.675193018007247403 ) ) ;
#32457=CARTESIAN_POINT ( 'NONE',  ( 5.377543748152548098, 6.940565734314597002, 4.007137495034836405 ) ) ;
#32465=EDGE_CURVE ( 'NONE', #11793, #27801, #15622, .T. ) ;
#32475=ADVANCED_FACE ( 'NONE', ( #13342 ), #11176, .T. ) ;
#32476=EDGE_CURVE ( 'NONE', #22878, #29891, #31948, .T. ) ;
#32483=DIRECTION ( 'NONE',  ( 0.000000000000000000, -0.9510565162951504226, -0.3090169943749573322 ) ) ;
#32489=DIRECTION ( 'NONE',  ( 0.000000000000000000, 0.08715574274765135188, 0.9961946980917461003 ) ) ;
#32492=EDGE_CURVE ( 'NONE', #32878, #12355, #4415, .T. ) ;
#32498=CARTESIAN_POINT ( 'NONE',  ( -5.437550801365593323, 1.088641768524161613, 3.675193018007246959 ) ) ;
#32502=FACE_BOUND ( 'NONE', #13322, .T. ) ;
#32504=VERTEX_POINT ( 'NONE', #18701 ) ;
#32516=CYLINDRICAL_SURFACE ( 'NONE', #1241, 3.000000000000000444 ) ;
#32533=CARTESIAN_POINT ( 'NONE',  ( -7.050050802731187893, -1.887961173149512062, -2.331437884370912261 ) ) ;
#32535=CARTESIAN_POINT ( 'NONE',  ( -2.600050800000000883, 1.887961173149511618, 2.331437884370912705 ) ) ;
#32539=DIRECTION ( 'NONE',  ( -1.000000000000000000, 0.000000000000000000, -0.000000000000000000 ) ) ;
#32541=VERTEX_POINT ( 'NONE', #16015 ) ;
#32546=ORIENTED_EDGE ( 'NONE', *, *, #7944, .T. ) ;
#32548=ORIENTED_EDGE ( 'NONE', *, *, #9409, .F. ) ;
#32552=CARTESIAN_POINT ( 'NONE',  ( 7.249760686538667009, -3.647351267791625773, 7.953573330858203505 ) ) ;
#32558=DIRECTION ( 'NONE',  ( -1.000000000000000000, 0.000000000000000000, 0.000000000000000000 ) ) ;
#32560=CARTESIAN_POINT ( 'NONE',  ( 0.000000000000000000, 0.000000000000000000, 0.000000000000000000 ) ) ;
#32562=CARTESIAN_POINT ( 'NONE',  ( 7.064632940817597628, -3.748318449932240615, -7.906491560603705615 ) ) ;
#32566=CARTESIAN_POINT ( 'NONE',  ( -8.000050800000000351, 3.202524238648755350, 1.313925200161312423 ) ) ;
#32574=ORIENTED_EDGE ( 'NONE', *, *, #24435, .T. ) ;
#32575=CARTESIAN_POINT ( 'NONE',  ( -7.254531657079158258, -1.545410377633946286, 2.846291840500174697 ) ) ;
#32576=DIRECTION ( 'NONE',  ( 0.000000000000000000, -0.9961946980917467664, 0.08715574274764384399 ) ) ;
#32577=CARTESIAN_POINT ( 'NONE',  ( -8.000050800000000351, 0.000000000000000000, 0.000000000000000000 ) ) ;
#32580=ORIENTED_EDGE ( 'NONE', *, *, #27448, .F. ) ;
#32582=DIRECTION ( 'NONE',  ( 0.000000000000000000, 0.000000000000000000, 1.000000000000000000 ) ) ;
#32590=VECTOR ( 'NONE', #5460, 1000.000000000000000 ) ;
#32591=CARTESIAN_POINT ( 'NONE',  ( 5.885541806331895387, 7.447669719165333824, 3.871259391815477624 ) ) ;
#32593=EDGE_LOOP ( 'NONE', ( #27932, #29813, #12109 ) ) ;
#32595=CYLINDRICAL_SURFACE ( 'NONE', #26213, 3.000000000000000000 ) ;
#32601=CARTESIAN_POINT ( 'NONE',  ( -4.637550801365592612, 1.088641768524161613, 3.675193018007247403 ) ) ;
#32606=DIRECTION ( 'NONE',  ( 0.000000000000000000, -0.2079116908177663647, 0.9781476007338042455 ) ) ;
#32608=CYLINDRICAL_SURFACE ( 'NONE', #18753, 6.000000000000000000 ) ;
#32609=CARTESIAN_POINT ( 'NONE',  ( 6.530491482054473273, 8.398420403995373817, 2.114164693852618182 ) ) ;
#32621=DIRECTION ( 'NONE',  ( 0.000000000000000000, 0.5877852522924689183, 0.8090169943749504489 ) ) ;
#32624=LINE ( 'NONE', #9702, #31625 ) ;
#32634=VECTOR ( 'NONE', #31516, 1000.000000000000114 ) ;
#32640=CARTESIAN_POINT ( 'NONE',  ( 6.356382399260308347, 4.790388219480560927, 7.150437133400945555 ) ) ;
#32644=DIRECTION ( 'NONE',  ( -1.000000000000000000, 0.000000000000000000, 0.000000000000000000 ) ) ;
#32646=ORIENTED_EDGE ( 'NONE', *, *, #1821, .F. ) ;
#32649=ADVANCED_FACE ( 'NONE', ( #17010 ), #4161, .T. ) ;
#32650=CARTESIAN_POINT ( 'NONE',  ( 6.357667873252800028, -2.398098878660900102, -8.266402141659465741 ) ) ;
#32654=ORIENTED_EDGE ( 'NONE', *, *, #16049, .F. ) ;
#32656=AXIS2_PLACEMENT_3D ( 'NONE', #1032, #11557, #6060 ) ;
#32657=EDGE_CURVE ( 'NONE', #21064, #12879, #28441, .T. ) ;
#32658=DIRECTION ( 'NONE',  ( 0.000000000000000000, -0.8660254037844432595, 0.4999999999999918399 ) ) ;
#32660=CARTESIAN_POINT ( 'NONE',  ( -5.087550801365593678, -2.228590825266444586, -2.752080473201636401 ) ) ;
#32662=AXIS2_PLACEMENT_3D ( 'NONE', #19230, #26931, #4034 ) ;
#32665=( BOUNDED_CURVE ( )  B_SPLINE_CURVE ( 2, ( #30699, #10435, #3095, #20486, #17963, #20147, #265, #30342, #7412, #17795, #15275 ),
 .UNSPECIFIED., .F., .F. ) 
 B_SPLINE_CURVE_WITH_KNOTS ( ( 3, 2, 2, 2, 2, 3 ),
 ( 0.4353822619934377136, 0.4375000000000000000, 0.4531250000000000000, 0.4687500000000000000, 0.4843750000000000000, 0.4978822619934377136 ),
 .UNSPECIFIED. ) 
 CURVE ( )  GEOMETRIC_REPRESENTATION_ITEM ( )  RATIONAL_B_SPLINE_CURVE ( ( 0.9821626249036857770, 0.9896829947469991673, 1.000000000000000000, 0.9238795325112867385, 1.000000000000000000, 0.9238795325112867385, 1.000000000000000000, 0.9238795325112867385, 1.000000000000000000, 0.9341965377642874602, 0.9821626249036857770 ) ) 
 REPRESENTATION_ITEM ( '' )  );
#32666=PLANE ( 'NONE',  #29583 ) ;
#32669=CIRCLE ( 'NONE', #8694, 8.750000000000000000 ) ;
#32676=DIRECTION ( 'NONE',  ( -0.000000000000000000, 0.2588190451025185190, -0.9659258262890689783 ) ) ;
#32690=CYLINDRICAL_SURFACE ( 'NONE', #24745, 2.999999999999999112 ) ;
#32700=CARTESIAN_POINT ( 'NONE',  ( 3.499999999999999556, 2.871924938129881699, 6.435996203144517480 ) ) ;
#32704=EDGE_CURVE ( 'NONE', #21921, #29082, #31770, .T. ) ;
#32705=CARTESIAN_POINT ( 'NONE',  ( -2.400050802731187094, -3.113457007523259268, 0.9222479816126455399 ) ) ;
#32707=CARTESIAN_POINT ( 'NONE',  ( -2.700050800000000084, 2.983565686104819648, 0.3135853898029609677 ) ) ;
#32708=AXIS2_PLACEMENT_3D ( 'NONE', #7876, #4249, #30455 ) ;
#32736=CARTESIAN_POINT ( 'NONE',  ( 3.499999999999999556, 6.704570150426983233, 2.172265885002680808 ) ) ;
#32748=AXIS2_PLACEMENT_3D ( 'NONE', #10412, #20621, #30828 ) ;
#32749=CARTESIAN_POINT ( 'NONE',  ( -8.000050800000002127, 2.386805812962781825, 2.383467509112250138 ) ) ;
#32755=CARTESIAN_POINT ( 'NONE',  ( -5.412550801365593856, 3.368539882008727115, 1.828967928396026954 ) ) ;
#32757=CARTESIAN_POINT ( 'NONE',  ( -7.404531657079157725, 1.883076972206379374, 2.325406398514293205 ) ) ;
#32761=FACE_OUTER_BOUND ( 'NONE', #12011, .T. ) ;
#32766=CARTESIAN_POINT ( 'NONE',  ( 5.885541838704151374, -5.105720535585458464, 6.662285765435201235 ) ) ;
#32773=DIRECTION ( 'NONE',  ( 1.000000000000000000, -0.000000000000000000, -0.000000000000000000 ) ) ;
#32774=ORIENTED_EDGE ( 'NONE', *, *, #12498, .T. ) ;
#32782=CARTESIAN_POINT ( 'NONE',  ( -7.862550801365593145, 3.521866450007987037, 0.3701630799359328372 ) ) ;
#32785=CARTESIAN_POINT ( 'NONE',  ( 3.499999999999999556, 2.871924938129968741, -6.435996203144479288 ) ) ;
#32790=EDGE_CURVE ( 'NONE', #22104, #21443, #13998, .T. ) ;
#32802=B_SPLINE_CURVE_WITH_KNOTS ( 'NONE', 3,
 ( #21130, #23303, #69, #20483, #15604, #17792, #18279, #7769, #5742, #31329 ),
 .UNSPECIFIED., .F., .F.,
 ( 4, 2, 2, 2, 4 ),
 ( 2.571685856657688708E-07, 0.0005478592107668812028, 0.001095461252948096761, 0.001643063295129312210, 0.002190665337310527660 ),
 .UNSPECIFIED. ) ;
#32824=DIRECTION ( 'NONE',  ( 0.000000000000000000, 0.000000000000000000, 1.000000000000000000 ) ) ;
#32834=DIRECTION ( 'NONE',  ( 1.000000000000000000, -0.000000000000000000, -0.000000000000000000 ) ) ;
#32835=DIRECTION ( 'NONE',  ( -1.000000000000000000, -0.000000000000000000, 0.000000000000000000 ) ) ;
#32840=CARTESIAN_POINT ( 'NONE',  ( -1.773875666770781789, -0.3178988483021056854, 3.024605502323848949 ) ) ;
#32841=CARTESIAN_POINT ( 'NONE',  ( -6.487550801365593145, 2.752080473201636845, -2.228590825266444142 ) ) ;
#32845=DIRECTION ( 'NONE',  ( -0.000000000000000000, 0.000000000000000000, 1.000000000000000000 ) ) ;
#32847=ORIENTED_EDGE ( 'NONE', *, *, #29075, .T. ) ;
#32848=DIRECTION ( 'NONE',  ( 0.000000000000000000, -0.7071067811865495711, 0.7071067811865454633 ) ) ;
#32849=EDGE_LOOP ( 'NONE', ( #12963, #23430, #10486 ) ) ;
#32855=ORIENTED_EDGE ( 'NONE', *, *, #18751, .F. ) ;
#32858=VERTEX_POINT ( 'NONE', #25707 ) ;
#32860=ADVANCED_FACE ( 'NONE', ( #22867 ), #30400, .T. ) ;
#32863=CARTESIAN_POINT ( 'NONE',  ( 1.750000000000000222, -7.851777359434023218, 3.255701506262406841 ) ) ;
#32865=PLANE ( 'NONE',  #3407 ) ;
#32866=CARTESIAN_POINT ( 'NONE',  ( 7.249760686538667009, 0.7071067811866343922, -8.721381771256197624 ) ) ;
#32867=EDGE_CURVE ( 'NONE', #22455, #31994, #22573, .T. ) ;
#32870=CARTESIAN_POINT ( 'NONE',  ( 7.249760686538667009, 4.973063321323977881, -7.199384779417068891 ) ) ;
#32872=CARTESIAN_POINT ( 'NONE',  ( 6.356381935169121533, 8.556754636093206301, 0.9265622495396070857 ) ) ;
#32877=CARTESIAN_POINT ( 'NONE',  ( -4.000050802731187183, -3.113457007523259268, 0.9222479816126455399 ) ) ;
#32878=VERTEX_POINT ( 'NONE', #7473 ) ;
#32879=CARTESIAN_POINT ( 'NONE',  ( -2.550050800000000173, 0.9222479816126443186, 3.113457007523260156 ) ) ;
#32892=VERTEX_POINT ( 'NONE', #960 ) ;
#32894=EDGE_LOOP ( 'NONE', ( #22784, #5932, #7582 ) ) ;
#32902=ADVANCED_FACE ( 'NONE', ( #5657 ), #15685, .T. ) ;
#32904=ORIENTED_EDGE ( 'NONE', *, *, #15383, .F. ) ;
#32905=CARTESIAN_POINT ( 'NONE',  ( 7.249760686538667009, -6.226446564517957860, 6.147671362329200306 ) ) ;
#32907=CARTESIAN_POINT ( 'NONE',  ( 4.749760686538667009, -1.391664247347281780, 7.892520144992429820 ) ) ;
#32909=EDGE_CURVE ( 'NONE', #22878, #5480, #11139, .T. ) ;
#32910=CARTESIAN_POINT ( 'NONE',  ( 1.750000000000000222, -7.673322273190700926, -3.656518192455154193 ) ) ;
#32914=CARTESIAN_POINT ( 'NONE',  ( -6.012550801365594388, -1.828967928396026510, 3.368539882008728004 ) ) ;
#32917=CARTESIAN_POINT ( 'NONE',  ( -5.754531657079158258, 0.9198621039125853827, 3.105402419394639235 ) ) ;
#32919=DIRECTION ( 'NONE',  ( -1.000000000000000000, -0.000000000000000000, -0.000000000000000000 ) ) ;
#32926=CARTESIAN_POINT ( 'NONE',  ( -3.312942406915326377, -5.022711880624455567E-15, 2.999999999999999556 ) ) ;
#32932=DIRECTION ( 'NONE',  ( 0.000000000000000000, -0.8191520442889824727, -0.5735764363510594821 ) ) ;
#32934=EDGE_CURVE ( 'NONE', #25317, #2704, #20457, .T. ) ;
#32936=DIRECTION ( 'NONE',  ( -1.000000000000000000, 0.000000000000000000, 0.000000000000000000 ) ) ;
#32939=CARTESIAN_POINT ( 'NONE',  ( 7.064632879756604034, 8.711672189281438605, -0.8180878109960962874 ) ) ;
#32940=ORIENTED_EDGE ( 'NONE', *, *, #32492, .F. ) ;
#32941=CARTESIAN_POINT ( 'NONE',  ( -4.712550801365592790, 3.675193018007247403, -1.088641768524161391 ) ) ;
#32942=DIRECTION ( 'NONE',  ( -1.000000000000000000, -0.000000000000000000, -0.000000000000000000 ) ) ;
#32943=FACE_OUTER_BOUND ( 'NONE', #11913, .T. ) ;
#32947=ORIENTED_EDGE ( 'NONE', *, *, #13829, .T. ) ;
#32948=EDGE_CURVE ( 'NONE', #4058, #21466, #8183, .T. ) ;
#32950=DIRECTION ( 'NONE',  ( 1.000000000000000000, -0.000000000000000000, -0.000000000000000000 ) ) ;
#32956=CARTESIAN_POINT ( 'NONE',  ( 6.883866601413089370, 7.193114723270807254, 4.949663153219556300 ) ) ;
#32966=ORIENTED_EDGE ( 'NONE', *, *, #32657, .F. ) ;
#32973=CARTESIAN_POINT ( 'NONE',  ( -6.962550801365593678, 2.228590825266444142, 2.752080473201636845 ) ) ;
#32975=PLANE ( 'NONE',  #31101 ) ;
#32981=DIRECTION ( 'NONE',  ( 0.000000000000000000, 0.000000000000000000, 1.000000000000000000 ) ) ;
#32987=CYLINDRICAL_SURFACE ( 'NONE', #4372, 3.000000000000000444 ) ;
#32989=EDGE_LOOP ( 'NONE', ( #16429, #2124, #11527, #13563 ) ) ;
#32991=CARTESIAN_POINT ( 'NONE',  ( -5.737550801365594033, 1.828967928396027398, -3.368539882008727115 ) ) ;
#32992=EDGE_LOOP ( 'NONE', ( #5277, #29547, #5200 ) ) ;
#32993=CARTESIAN_POINT ( 'NONE',  ( 7.249760686538667009, 6.940565734314653845, -4.007137495034738706 ) ) ;
#32999=ORIENTED_EDGE ( 'NONE', *, *, #31552, .F. ) ;
#33000=EDGE_CURVE ( 'NONE', #21466, #11105, #29540, .T. ) ;
#33004=LINE ( 'NONE', #24964, #9050 ) ;
#33011=VERTEX_POINT ( 'NONE', #4276 ) ;
#33015=DIRECTION ( 'NONE',  ( -1.000000000000000000, 0.000000000000000000, 0.000000000000000000 ) ) ;
#33024=CARTESIAN_POINT ( 'NONE',  ( -2.850050802731187716, 2.331437884370912705, -1.887961173149511618 ) ) ;
#33026=CARTESIAN_POINT ( 'NONE',  ( -5.737550801365594033, 1.828967928396027176, -3.368539882008727115 ) ) ;
#33027=EDGE_CURVE ( 'NONE', #24941, #9919, #26856, .T. ) ;
#33030=CYLINDRICAL_SURFACE ( 'NONE', #28518, 6.248999999999999666 ) ;
#33032=CARTESIAN_POINT ( 'NONE',  ( 5.887530252753763627, -5.105578361685870981, -6.663910820542635172 ) ) ;
#33033=CARTESIAN_POINT ( 'NONE',  ( 7.249760686538667009, -6.147671362329178102, -6.226446564517978288 ) ) ;
#33044=CARTESIAN_POINT ( 'NONE',  ( 5.377543748152548986, 7.892520144992435149, 1.391664247347255134 ) ) ;
#33045=CARTESIAN_POINT ( 'NONE',  ( 3.499999999999999556, 1.459547570502463198, -6.894905428400257996 ) ) ;
#33046=EDGE_CURVE ( 'NONE', #32312, #19070, #12608, .T. ) ;
#33053=DIRECTION ( 'NONE',  ( 0.000000000000000000, 0.8191520442889956843, -0.5735764363510406083 ) ) ;
#33055=CARTESIAN_POINT ( 'NONE',  ( -8.000050800000002127, -1.808230216471487184, 2.469696313123094011 ) ) ;
#33059=VERTEX_POINT ( 'NONE', #22682 ) ;
#33061=CARTESIAN_POINT ( 'NONE',  ( -5.962550801365593678, -2.752080473201636845, 2.228590825266444586 ) ) ;
#33063=CARTESIAN_POINT ( 'NONE',  ( -5.154531657079158613, 3.105402419394639235, -0.9198621039125850496 ) ) ;
#33065=FACE_OUTER_BOUND ( 'NONE', #20137, .T. ) ;
#33068=DIRECTION ( 'NONE',  ( -1.000000000000000000, -0.000000000000000000, -0.000000000000000000 ) ) ;
#33070=CARTESIAN_POINT ( 'NONE',  ( 3.499999999999999556, -6.106419733535023653, 3.518755179752782958 ) ) ;
#33074=CARTESIAN_POINT ( 'NONE',  ( -3.550050800000000173, 3.113457007523260156, -0.9222479816126439855 ) ) ;
#33080=CARTESIAN_POINT ( 'NONE',  ( 3.499999999999999556, 2.429606751577043422, 5.757344182232919216 ) ) ;
#33081=VERTEX_POINT ( 'NONE', #30534 ) ;
#33082=CARTESIAN_POINT ( 'NONE',  ( -7.998722633285748174, -2.371517779863575370, 1.837526800715260533 ) ) ;
#33085=EDGE_CURVE ( 'NONE', #27844, #4589, #29518, .T. ) ;
#33089=ORIENTED_EDGE ( 'NONE', *, *, #23075, .T. ) ;
#33090=CARTESIAN_POINT ( 'NONE',  ( -6.412550801365592967, 1.828967928396027176, -3.368539882008727115 ) ) ;
#33092=CIRCLE ( 'NONE', #9022, 6.248999999999998778 ) ;
#33093=CARTESIAN_POINT ( 'NONE',  ( 6.530491751506349196, -7.017944781891989336, 5.074604403564646482 ) ) ;
#33095=ORIENTED_EDGE ( 'NONE', *, *, #11152, .F. ) ;
#33097=DIRECTION ( 'NONE',  ( -1.000000000000000000, 0.000000000000000000, 0.000000000000000000 ) ) ;
#33120=COLOUR_RGB('Sky Blue', 0.40784314, 0.44705882, 0.49803922);
#33121=FILL_AREA_STYLE_COLOUR('',#33120);
#33122=FILL_AREA_STYLE('',(#33121));
#33123=SURFACE_STYLE_FILL_AREA(#33122);
#33124=SURFACE_SIDE_STYLE('',(#33123));
#33125=SURFACE_STYLE_USAGE(.BOTH.,#33124);
#33126=PRESENTATION_STYLE_ASSIGNMENT((#33125));
#33152=STYLED_ITEM('',(#33126),#10515);
#33153=MECHANICAL_DESIGN_GEOMETRIC_PRESENTATION_REPRESENTATION('',(#33152),#32200);
ENDSEC;
END-ISO-10303-21;
